ISO-10303-21;
HEADER;
/* Generated by software containing ST-Developer
 * from STEP Tools, Inc. (www.steptools.com) 
 */

FILE_DESCRIPTION(
/* description */ ('Independent pair of monolithic parallel-leaf compliant finger modules.
 Shared native part/module instances; external gripper actuator outsid
e scope. Whole-mm geometry,1mm webs,56mm straight span,12mm depth,32mm
 nominal contact gap. Undeformed CAD reference; material condition, el
astic range, fatigue and gripping force unassigned.'),
/* implementation_level */ '2;1');

FILE_NAME(
/* name */ 'Socket head cap screw M5x25.step',
/* time_stamp */ '2026-11-07T22:36:16-08:00',
/* author */ (''),
/* organization */ (''),
/* preprocessor_version */ 'ST-DEVELOPER v20.2',
/* originating_system */ 'Autodesk Translation Framework v15.17.0.0',
/* authorisation */ '');

FILE_SCHEMA (('AUTOMOTIVE_DESIGN { 1 0 10303 214 3 1 1 }'));
ENDSEC;

DATA;
#10=MECHANICAL_DESIGN_GEOMETRIC_PRESENTATION_REPRESENTATION('',(#333),#13801);
#55=CONICAL_SURFACE('',#4004,2.,0.785398163397448);
#60=B_SPLINE_SURFACE_WITH_KNOTS('',3,3,((#11906,#11907,#11908,#11909,#11910,
#11911,#11912,#11913,#11914,#11915,#11916,#11917,#11918,#11919,#11920,#11921,
#11922,#11923,#11924,#11925,#11926,#11927,#11928,#11929,#11930,#11931,#11932,
#11933,#11934,#11935,#11936,#11937,#11938,#11939,#11940,#11941,#11942,#11943,
#11944,#11945,#11946,#11947,#11948,#11949,#11950,#11951,#11952,#11953,#11954,
#11955,#11956,#11957,#11958,#11959,#11960,#11961,#11962,#11963,#11964,#11965,
#11966,#11967,#11968,#11969,#11970,#11971,#11972,#11973,#11974,#11975,#11976,
#11977,#11978,#11979,#11980,#11981,#11982,#11983,#11984,#11985,#11986,#11987,
#11988,#11989,#11990,#11991,#11992,#11993,#11994,#11995,#11996,#11997,#11998,
#11999,#12000,#12001,#12002,#12003,#12004,#12005,#12006,#12007,#12008,#12009,
#12010,#12011,#12012,#12013,#12014,#12015,#12016,#12017,#12018,#12019,#12020,
#12021,#12022,#12023,#12024,#12025,#12026,#12027,#12028,#12029,#12030,#12031,
#12032,#12033,#12034,#12035,#12036,#12037,#12038,#12039,#12040,#12041,#12042,
#12043,#12044,#12045,#12046,#12047,#12048,#12049,#12050,#12051,#12052,#12053,
#12054,#12055,#12056,#12057,#12058,#12059,#12060,#12061,#12062,#12063,#12064,
#12065,#12066,#12067,#12068,#12069,#12070,#12071,#12072,#12073,#12074,#12075,
#12076,#12077,#12078,#12079,#12080,#12081,#12082,#12083,#12084,#12085,#12086,
#12087,#12088,#12089,#12090,#12091,#12092,#12093,#12094,#12095,#12096,#12097,
#12098,#12099,#12100,#12101),(#12102,#12103,#12104,#12105,#12106,#12107,
#12108,#12109,#12110,#12111,#12112,#12113,#12114,#12115,#12116,#12117,#12118,
#12119,#12120,#12121,#12122,#12123,#12124,#12125,#12126,#12127,#12128,#12129,
#12130,#12131,#12132,#12133,#12134,#12135,#12136,#12137,#12138,#12139,#12140,
#12141,#12142,#12143,#12144,#12145,#12146,#12147,#12148,#12149,#12150,#12151,
#12152,#12153,#12154,#12155,#12156,#12157,#12158,#12159,#12160,#12161,#12162,
#12163,#12164,#12165,#12166,#12167,#12168,#12169,#12170,#12171,#12172,#12173,
#12174,#12175,#12176,#12177,#12178,#12179,#12180,#12181,#12182,#12183,#12184,
#12185,#12186,#12187,#12188,#12189,#12190,#12191,#12192,#12193,#12194,#12195,
#12196,#12197,#12198,#12199,#12200,#12201,#12202,#12203,#12204,#12205,#12206,
#12207,#12208,#12209,#12210,#12211,#12212,#12213,#12214,#12215,#12216,#12217,
#12218,#12219,#12220,#12221,#12222,#12223,#12224,#12225,#12226,#12227,#12228,
#12229,#12230,#12231,#12232,#12233,#12234,#12235,#12236,#12237,#12238,#12239,
#12240,#12241,#12242,#12243,#12244,#12245,#12246,#12247,#12248,#12249,#12250,
#12251,#12252,#12253,#12254,#12255,#12256,#12257,#12258,#12259,#12260,#12261,
#12262,#12263,#12264,#12265,#12266,#12267,#12268,#12269,#12270,#12271,#12272,
#12273,#12274,#12275,#12276,#12277,#12278,#12279,#12280,#12281,#12282,#12283,
#12284,#12285,#12286,#12287,#12288,#12289,#12290,#12291,#12292,#12293,#12294,
#12295,#12296,#12297),(#12298,#12299,#12300,#12301,#12302,#12303,#12304,
#12305,#12306,#12307,#12308,#12309,#12310,#12311,#12312,#12313,#12314,#12315,
#12316,#12317,#12318,#12319,#12320,#12321,#12322,#12323,#12324,#12325,#12326,
#12327,#12328,#12329,#12330,#12331,#12332,#12333,#12334,#12335,#12336,#12337,
#12338,#12339,#12340,#12341,#12342,#12343,#12344,#12345,#12346,#12347,#12348,
#12349,#12350,#12351,#12352,#12353,#12354,#12355,#12356,#12357,#12358,#12359,
#12360,#12361,#12362,#12363,#12364,#12365,#12366,#12367,#12368,#12369,#12370,
#12371,#12372,#12373,#12374,#12375,#12376,#12377,#12378,#12379,#12380,#12381,
#12382,#12383,#12384,#12385,#12386,#12387,#12388,#12389,#12390,#12391,#12392,
#12393,#12394,#12395,#12396,#12397,#12398,#12399,#12400,#12401,#12402,#12403,
#12404,#12405,#12406,#12407,#12408,#12409,#12410,#12411,#12412,#12413,#12414,
#12415,#12416,#12417,#12418,#12419,#12420,#12421,#12422,#12423,#12424,#12425,
#12426,#12427,#12428,#12429,#12430,#12431,#12432,#12433,#12434,#12435,#12436,
#12437,#12438,#12439,#12440,#12441,#12442,#12443,#12444,#12445,#12446,#12447,
#12448,#12449,#12450,#12451,#12452,#12453,#12454,#12455,#12456,#12457,#12458,
#12459,#12460,#12461,#12462,#12463,#12464,#12465,#12466,#12467,#12468,#12469,
#12470,#12471,#12472,#12473,#12474,#12475,#12476,#12477,#12478,#12479,#12480,
#12481,#12482,#12483,#12484,#12485,#12486,#12487,#12488,#12489,#12490,#12491,
#12492,#12493),(#12494,#12495,#12496,#12497,#12498,#12499,#12500,#12501,
#12502,#12503,#12504,#12505,#12506,#12507,#12508,#12509,#12510,#12511,#12512,
#12513,#12514,#12515,#12516,#12517,#12518,#12519,#12520,#12521,#12522,#12523,
#12524,#12525,#12526,#12527,#12528,#12529,#12530,#12531,#12532,#12533,#12534,
#12535,#12536,#12537,#12538,#12539,#12540,#12541,#12542,#12543,#12544,#12545,
#12546,#12547,#12548,#12549,#12550,#12551,#12552,#12553,#12554,#12555,#12556,
#12557,#12558,#12559,#12560,#12561,#12562,#12563,#12564,#12565,#12566,#12567,
#12568,#12569,#12570,#12571,#12572,#12573,#12574,#12575,#12576,#12577,#12578,
#12579,#12580,#12581,#12582,#12583,#12584,#12585,#12586,#12587,#12588,#12589,
#12590,#12591,#12592,#12593,#12594,#12595,#12596,#12597,#12598,#12599,#12600,
#12601,#12602,#12603,#12604,#12605,#12606,#12607,#12608,#12609,#12610,#12611,
#12612,#12613,#12614,#12615,#12616,#12617,#12618,#12619,#12620,#12621,#12622,
#12623,#12624,#12625,#12626,#12627,#12628,#12629,#12630,#12631,#12632,#12633,
#12634,#12635,#12636,#12637,#12638,#12639,#12640,#12641,#12642,#12643,#12644,
#12645,#12646,#12647,#12648,#12649,#12650,#12651,#12652,#12653,#12654,#12655,
#12656,#12657,#12658,#12659,#12660,#12661,#12662,#12663,#12664,#12665,#12666,
#12667,#12668,#12669,#12670,#12671,#12672,#12673,#12674,#12675,#12676,#12677,
#12678,#12679,#12680,#12681,#12682,#12683,#12684,#12685,#12686,#12687,#12688,
#12689)),.UNSPECIFIED.,.F.,.F.,.F.,(4,4),(4,1,1,1,1,1,1,1,1,1,1,1,1,1,1,
1,1,1,1,1,1,1,1,1,1,1,1,1,1,1,1,1,1,1,1,1,1,1,1,1,1,1,1,1,1,1,1,1,1,1,1,
1,1,1,1,1,1,1,1,1,1,1,1,1,1,1,1,1,1,1,1,1,1,1,1,1,1,1,1,1,1,1,1,1,1,1,1,
1,1,1,1,1,1,1,1,1,1,1,1,1,1,1,1,1,1,1,1,1,1,1,1,1,1,1,1,1,1,1,1,1,1,1,1,
1,1,1,1,1,1,1,1,1,1,1,1,1,1,1,1,1,1,1,1,1,1,1,1,1,1,1,1,1,1,1,1,1,1,1,1,
1,1,1,1,1,1,1,1,1,1,1,1,1,1,1,1,1,1,1,1,1,1,1,1,1,1,1,1,1,1,1,1,1,1,4),
(0.,0.0526254770366344),(11.6163931973417,12.6136148731756,13.6108365490096,
14.6080582248435,15.6052799006775,16.6025015765114,17.5997232523454,18.5969449281793,
19.5941666040133,20.5913882798473,21.5886099556812,22.5858316315152,23.5830533073491,
24.5802749831831,25.577496659017,26.574718334851,27.5719400106849,28.5691616865189,
29.5663833623529,30.5636050381868,31.5608267140208,32.5580483898547,33.5552700656887,
34.5524917415226,35.5497134173566,36.5469350931905,37.5441567690245,38.5413784448584,
39.5386001206924,40.5358217965264,41.5330434723603,42.5302651481943,43.5274868240282,
44.5247084998622,45.5219301756961,46.5191518515301,47.516373527364,48.513595203198,
49.5108168790319,50.5080385548659,51.5052602306999,52.5024819065338,53.4997035823678,
54.4969252582017,55.4941469340357,56.4913686098696,57.4885902857036,58.4858119615375,
59.4830336373715,60.4802553132055,61.4774769890394,62.4746986648734,63.4719203407073,
64.4691420165413,65.4663636923752,66.4635853682092,67.4608070440431,68.4580287198771,
69.455250395711,70.452472071545,71.4496937473789,72.4469154232129,73.4441370990469,
74.4413587748808,75.4385804507148,76.4358021265487,77.4330238023827,78.4302454782166,
79.4274671540506,80.4246888298845,81.4219105057185,82.4191321815525,83.4163538573864,
84.4135755332204,85.4107972090543,86.4080188848883,87.4052405607222,88.4024622365562,
89.3996839123901,90.3969055882241,91.3941272640581,92.391348939892,93.388570615726,
94.3857922915599,95.3830139673939,96.3802356432278,97.3774573190618,98.3746789948957,
99.3719006707297,100.369122346564,101.366344022398,102.363565698232,103.360787374066,
104.358009049899,105.355230725733,106.352452401567,107.349674077401,108.346895753235,
109.344117429069,110.341339104903,111.338560780737,112.335782456571,113.333004132405,
114.330225808239,115.327447484073,116.324669159907,117.321890835741,118.319112511575,
119.316334187409,120.313555863243,121.310777539077,122.307999214911,123.305220890745,
124.302442566579,125.299664242413,126.296885918246,127.29410759408,128.291329269914,
129.288550945748,130.285772621582,131.282994297416,132.28021597325,133.277437649084,
134.274659324918,135.271881000752,136.269102676586,137.26632435242,138.263546028254,
139.260767704088,140.257989379922,141.255211055756,142.25243273159,143.249654407424,
144.246876083258,145.244097759092,146.241319434926,147.23854111076,148.235762786593,
149.232984462427,150.230206138261,151.227427814095,152.224649489929,153.221871165763,
154.219092841597,155.216314517431,156.213536193265,157.210757869099,158.207979544933,
159.205201220767,160.202422896601,161.199644572435,162.196866248269,163.194087924103,
164.191309599937,165.188531275771,166.185752951605,167.182974627439,168.180196303273,
169.177417979107,170.17463965494,171.171861330774,172.169083006608,173.166304682442,
174.163526358276,175.16074803411,176.157969709944,177.155191385778,178.152413061612,
179.149634737446,180.14685641328,181.144078089114,182.141299764948,183.138521440782,
184.135743116616,185.13296479245,186.130186468284,187.127408144118,188.124629819952,
189.121851495786,190.11907317162,191.116294847454,192.113516523288,193.110738199121,
194.107959874955,195.105181550789,196.102403226623,197.099624902457,198.096846578291,
199.094068254125,200.091289929959,201.088511605793,202.085733281627,203.082954957461,
204.080176633295),.UNSPECIFIED.);
#61=B_SPLINE_SURFACE_WITH_KNOTS('',3,3,((#12818,#12819,#12820,#12821,#12822,
#12823,#12824,#12825,#12826,#12827,#12828,#12829,#12830,#12831,#12832,#12833,
#12834,#12835,#12836,#12837,#12838,#12839,#12840,#12841,#12842,#12843,#12844,
#12845,#12846,#12847,#12848,#12849,#12850,#12851,#12852,#12853,#12854,#12855,
#12856,#12857,#12858,#12859,#12860,#12861,#12862,#12863,#12864,#12865,#12866,
#12867,#12868,#12869,#12870,#12871,#12872,#12873,#12874,#12875,#12876,#12877,
#12878,#12879,#12880,#12881,#12882,#12883,#12884,#12885,#12886,#12887,#12888,
#12889,#12890,#12891,#12892,#12893,#12894,#12895,#12896,#12897,#12898,#12899,
#12900,#12901,#12902,#12903,#12904,#12905,#12906,#12907,#12908,#12909,#12910,
#12911,#12912,#12913,#12914,#12915,#12916,#12917,#12918,#12919,#12920,#12921,
#12922,#12923,#12924,#12925,#12926,#12927,#12928,#12929,#12930,#12931,#12932,
#12933,#12934,#12935,#12936,#12937,#12938,#12939,#12940,#12941,#12942,#12943,
#12944,#12945,#12946,#12947,#12948,#12949,#12950,#12951,#12952,#12953,#12954,
#12955,#12956,#12957,#12958,#12959,#12960,#12961,#12962,#12963,#12964,#12965,
#12966,#12967,#12968,#12969,#12970,#12971,#12972,#12973,#12974,#12975,#12976,
#12977,#12978,#12979,#12980,#12981,#12982,#12983,#12984,#12985,#12986,#12987,
#12988,#12989,#12990,#12991,#12992,#12993,#12994,#12995,#12996,#12997,#12998,
#12999,#13000,#13001,#13002,#13003,#13004,#13005,#13006,#13007,#13008,#13009,
#13010,#13011,#13012,#13013,#13014,#13015),(#13016,#13017,#13018,#13019,
#13020,#13021,#13022,#13023,#13024,#13025,#13026,#13027,#13028,#13029,#13030,
#13031,#13032,#13033,#13034,#13035,#13036,#13037,#13038,#13039,#13040,#13041,
#13042,#13043,#13044,#13045,#13046,#13047,#13048,#13049,#13050,#13051,#13052,
#13053,#13054,#13055,#13056,#13057,#13058,#13059,#13060,#13061,#13062,#13063,
#13064,#13065,#13066,#13067,#13068,#13069,#13070,#13071,#13072,#13073,#13074,
#13075,#13076,#13077,#13078,#13079,#13080,#13081,#13082,#13083,#13084,#13085,
#13086,#13087,#13088,#13089,#13090,#13091,#13092,#13093,#13094,#13095,#13096,
#13097,#13098,#13099,#13100,#13101,#13102,#13103,#13104,#13105,#13106,#13107,
#13108,#13109,#13110,#13111,#13112,#13113,#13114,#13115,#13116,#13117,#13118,
#13119,#13120,#13121,#13122,#13123,#13124,#13125,#13126,#13127,#13128,#13129,
#13130,#13131,#13132,#13133,#13134,#13135,#13136,#13137,#13138,#13139,#13140,
#13141,#13142,#13143,#13144,#13145,#13146,#13147,#13148,#13149,#13150,#13151,
#13152,#13153,#13154,#13155,#13156,#13157,#13158,#13159,#13160,#13161,#13162,
#13163,#13164,#13165,#13166,#13167,#13168,#13169,#13170,#13171,#13172,#13173,
#13174,#13175,#13176,#13177,#13178,#13179,#13180,#13181,#13182,#13183,#13184,
#13185,#13186,#13187,#13188,#13189,#13190,#13191,#13192,#13193,#13194,#13195,
#13196,#13197,#13198,#13199,#13200,#13201,#13202,#13203,#13204,#13205,#13206,
#13207,#13208,#13209,#13210,#13211,#13212,#13213),(#13214,#13215,#13216,
#13217,#13218,#13219,#13220,#13221,#13222,#13223,#13224,#13225,#13226,#13227,
#13228,#13229,#13230,#13231,#13232,#13233,#13234,#13235,#13236,#13237,#13238,
#13239,#13240,#13241,#13242,#13243,#13244,#13245,#13246,#13247,#13248,#13249,
#13250,#13251,#13252,#13253,#13254,#13255,#13256,#13257,#13258,#13259,#13260,
#13261,#13262,#13263,#13264,#13265,#13266,#13267,#13268,#13269,#13270,#13271,
#13272,#13273,#13274,#13275,#13276,#13277,#13278,#13279,#13280,#13281,#13282,
#13283,#13284,#13285,#13286,#13287,#13288,#13289,#13290,#13291,#13292,#13293,
#13294,#13295,#13296,#13297,#13298,#13299,#13300,#13301,#13302,#13303,#13304,
#13305,#13306,#13307,#13308,#13309,#13310,#13311,#13312,#13313,#13314,#13315,
#13316,#13317,#13318,#13319,#13320,#13321,#13322,#13323,#13324,#13325,#13326,
#13327,#13328,#13329,#13330,#13331,#13332,#13333,#13334,#13335,#13336,#13337,
#13338,#13339,#13340,#13341,#13342,#13343,#13344,#13345,#13346,#13347,#13348,
#13349,#13350,#13351,#13352,#13353,#13354,#13355,#13356,#13357,#13358,#13359,
#13360,#13361,#13362,#13363,#13364,#13365,#13366,#13367,#13368,#13369,#13370,
#13371,#13372,#13373,#13374,#13375,#13376,#13377,#13378,#13379,#13380,#13381,
#13382,#13383,#13384,#13385,#13386,#13387,#13388,#13389,#13390,#13391,#13392,
#13393,#13394,#13395,#13396,#13397,#13398,#13399,#13400,#13401,#13402,#13403,
#13404,#13405,#13406,#13407,#13408,#13409,#13410,#13411),(#13412,#13413,
#13414,#13415,#13416,#13417,#13418,#13419,#13420,#13421,#13422,#13423,#13424,
#13425,#13426,#13427,#13428,#13429,#13430,#13431,#13432,#13433,#13434,#13435,
#13436,#13437,#13438,#13439,#13440,#13441,#13442,#13443,#13444,#13445,#13446,
#13447,#13448,#13449,#13450,#13451,#13452,#13453,#13454,#13455,#13456,#13457,
#13458,#13459,#13460,#13461,#13462,#13463,#13464,#13465,#13466,#13467,#13468,
#13469,#13470,#13471,#13472,#13473,#13474,#13475,#13476,#13477,#13478,#13479,
#13480,#13481,#13482,#13483,#13484,#13485,#13486,#13487,#13488,#13489,#13490,
#13491,#13492,#13493,#13494,#13495,#13496,#13497,#13498,#13499,#13500,#13501,
#13502,#13503,#13504,#13505,#13506,#13507,#13508,#13509,#13510,#13511,#13512,
#13513,#13514,#13515,#13516,#13517,#13518,#13519,#13520,#13521,#13522,#13523,
#13524,#13525,#13526,#13527,#13528,#13529,#13530,#13531,#13532,#13533,#13534,
#13535,#13536,#13537,#13538,#13539,#13540,#13541,#13542,#13543,#13544,#13545,
#13546,#13547,#13548,#13549,#13550,#13551,#13552,#13553,#13554,#13555,#13556,
#13557,#13558,#13559,#13560,#13561,#13562,#13563,#13564,#13565,#13566,#13567,
#13568,#13569,#13570,#13571,#13572,#13573,#13574,#13575,#13576,#13577,#13578,
#13579,#13580,#13581,#13582,#13583,#13584,#13585,#13586,#13587,#13588,#13589,
#13590,#13591,#13592,#13593,#13594,#13595,#13596,#13597,#13598,#13599,#13600,
#13601,#13602,#13603,#13604,#13605,#13606,#13607,#13608,#13609)),
 .UNSPECIFIED.,.F.,.F.,.F.,(4,4),(4,1,1,1,1,1,1,1,1,1,1,1,1,1,1,1,1,1,1,
1,1,1,1,1,1,1,1,1,1,1,1,1,1,1,1,1,1,1,1,1,1,1,1,1,1,1,1,1,1,1,1,1,1,1,1,
1,1,1,1,1,1,1,1,1,1,1,1,1,1,1,1,1,1,1,1,1,1,1,1,1,1,1,1,1,1,1,1,1,1,1,1,
1,1,1,1,1,1,1,1,1,1,1,1,1,1,1,1,1,1,1,1,1,1,1,1,1,1,1,1,1,1,1,1,1,1,1,1,
1,1,1,1,1,1,1,1,1,1,1,1,1,1,1,1,1,1,1,1,1,1,1,1,1,1,1,1,1,1,1,1,1,1,1,1,
1,1,1,1,1,1,1,1,1,1,1,1,1,1,1,1,1,1,1,1,1,1,1,1,1,1,1,1,1,1,1,1,4),(0.,
0.0526254770366344),(8.30815772716282,9.3057494250427,10.3033411229226,
11.3009328208025,12.2985245186824,13.2961162165622,14.2937079144421,15.291299612322,
16.2888913102019,17.2864830080818,18.2840747059617,19.2816664038415,20.2792581017214,
21.2768497996013,22.2744414974812,23.2720331953611,24.269624893241,25.2672165911209,
26.2648082890007,27.2623999868806,28.2599916847605,29.2575833826404,30.2551750805203,
31.2527667784002,32.2503584762801,33.2479501741599,34.2455418720398,35.2431335699197,
36.2407252677996,37.2383169656795,38.2359086635594,39.2335003614392,40.2310920593191,
41.228683757199,42.2262754550789,43.2238671529588,44.2214588508387,45.2190505487186,
46.2166422465984,47.2142339444783,48.2118256423582,49.2094173402381,50.207009038118,
51.2046007359979,52.2021924338777,53.1997841317576,54.1973758296375,55.1949675275174,
56.1925592253973,57.1901509232772,58.1877426211571,59.1853343190369,60.1829260169168,
61.1805177147967,62.1781094126766,63.1757011105565,64.1732928084364,65.1708845063163,
66.1684762041961,67.166067902076,68.1636595999559,69.1612512978358,70.1588429957157,
71.1564346935956,72.1540263914755,73.1516180893553,74.1492097872352,75.1468014851151,
76.144393182995,77.1419848808749,78.1395765787548,79.1371682766347,80.1347599745145,
81.1323516723944,82.1299433702743,83.1275350681542,84.1251267660341,85.122718463914,
86.1203101617938,87.1179018596737,88.1154935575536,89.1130852554335,90.1106769533134,
91.1082686511933,92.1058603490732,93.103452046953,94.1010437448329,95.0986354427128,
96.0962271405927,97.0938188384726,98.0914105363525,99.0890022342324,100.086593932112,
101.084185629992,102.081777327872,103.079369025752,104.076960723632,105.074552421512,
106.072144119392,107.069735817271,108.067327515151,109.064919213031,110.062510910911,
111.060102608791,112.057694306671,113.055286004551,114.052877702431,115.050469400311,
116.04806109819,117.04565279607,118.04324449395,119.04083619183,120.03842788971,
121.03601958759,122.03361128547,123.03120298335,124.028794681229,125.026386379109,
126.023978076989,127.021569774869,128.019161472749,129.016753170629,130.014344868509,
131.011936566389,132.009528264269,133.007119962148,134.004711660028,135.002303357908,
135.999895055788,136.997486753668,137.995078451548,138.992670149428,139.990261847308,
140.987853545188,141.985445243067,142.983036940947,143.980628638827,144.978220336707,
145.975812034587,146.973403732467,147.970995430347,148.968587128227,149.966178826106,
150.963770523986,151.961362221866,152.958953919746,153.956545617626,154.954137315506,
155.951729013386,156.949320711266,157.946912409146,158.944504107025,159.942095804905,
160.939687502785,161.937279200665,162.934870898545,163.932462596425,164.930054294305,
165.927645992185,166.925237690065,167.922829387944,168.920421085824,169.918012783704,
170.915604481584,171.913196179464,172.910787877344,173.908379575224,174.905971273104,
175.903562970983,176.901154668863,177.898746366743,178.896338064623,179.893929762503,
180.891521460383,181.889113158263,182.886704856143,183.884296554023,184.881888251902,
185.879479949782,186.877071647662,187.874663345542,188.872255043422,189.869846741302,
190.867438439182,191.865030137062,192.862621834942,193.860213532821,194.857805230701,
195.855396928581,196.852988626461,197.850580324341,198.848172022221,199.845763720101,
200.843355417981,201.84094711586,202.83853881374),.UNSPECIFIED.);
#188=B_SPLINE_CURVE_WITH_KNOTS('',3,(#9401,#9402,#9403,#9404,#9405,#9406,
#9407,#9408,#9409,#9410),.UNSPECIFIED.,.F.,.F.,(4,3,3,4),(-4.09157007060747,
-3.98888670333582,-2.99166502750187,-2.06659765062436),.UNSPECIFIED.);
#189=B_SPLINE_CURVE_WITH_KNOTS('',3,(#9413,#9414,#9415,#9416,#9417,#9418,
#9419),.UNSPECIFIED.,.F.,.F.,(4,3,4),(0.,0.997591697879869,1.11662023360685),
 .UNSPECIFIED.);
#190=B_SPLINE_CURVE_WITH_KNOTS('',3,(#9424,#9425,#9426,#9427,#9428,#9429,
#9430,#9431,#9432,#9433,#9434,#9435,#9436,#9437,#9438,#9439,#9440,#9441,
#9442,#9443,#9444,#9445),.UNSPECIFIED.,.F.,.F.,(4,3,3,3,3,3,3,4),(-10.3747553777871,
-9.97221675833955,-8.9749950825056,-7.97777340667164,-6.98055173083769,
-5.98333005500373,-4.98610837916977,-4.09157007060747),.UNSPECIFIED.);
#191=B_SPLINE_CURVE_WITH_KNOTS('',3,(#9446,#9447,#9448,#9449,#9450,#9451,
#9452,#9453,#9454,#9455,#9456,#9457,#9458,#9459,#9460,#9461,#9462,#9463,
#9464,#9465,#9466,#9467),.UNSPECIFIED.,.F.,.F.,(4,3,3,3,3,3,3,4),(1.11662023360685,
1.99518339575976,2.99277509363965,3.99036679151954,4.98795848939943,5.98555018727932,
6.98314188515921,7.39980554078643),.UNSPECIFIED.);
#192=B_SPLINE_CURVE_WITH_KNOTS('',3,(#9472,#9473,#9474,#9475,#9476,#9477,
#9478,#9479,#9480,#9481,#9482,#9483,#9484,#9485,#9486,#9487,#9488,#9489,
#9490,#9491,#9492,#9493),.UNSPECIFIED.,.F.,.F.,(4,3,3,3,3,3,3,4),(-16.6579406849666,
-15.9555468133433,-14.9583251375093,-13.9611034616754,-12.9638817858414,
-11.9666601100075,-10.9694384341735,-10.3747553777871),.UNSPECIFIED.);
#193=B_SPLINE_CURVE_WITH_KNOTS('',3,(#9494,#9495,#9496,#9497,#9498,#9499,
#9500,#9501,#9502,#9503,#9504,#9505,#9506,#9507,#9508,#9509,#9510,#9511,
#9512,#9513,#9514,#9515),.UNSPECIFIED.,.F.,.F.,(4,3,3,3,3,3,3,4),(7.39980554078643,
7.9807335830391,8.97832528091898,9.97591697879886,10.9735086766787,11.9711003745586,
12.9686920724385,13.682990847966),.UNSPECIFIED.);
#194=B_SPLINE_CURVE_WITH_KNOTS('',3,(#9520,#9521,#9522,#9523,#9524,#9525,
#9526,#9527,#9528,#9529,#9530,#9531,#9532,#9533,#9534,#9535,#9536,#9537,
#9538,#9539,#9540,#9541,#9542,#9543,#9544),.UNSPECIFIED.,.F.,.F.,(4,3,3,
3,3,3,3,3,4),(-22.9411259921462,-22.936098544181,-21.938876868347,-20.941655192513,
-19.9444335166791,-18.9472118408451,-17.9499901650112,-16.9527684891772,
-16.6579406849666),.UNSPECIFIED.);
#195=B_SPLINE_CURVE_WITH_KNOTS('',3,(#9545,#9546,#9547,#9548,#9549,#9550,
#9551,#9552,#9553,#9554,#9555,#9556,#9557,#9558,#9559,#9560,#9561,#9562,
#9563,#9564,#9565,#9566,#9567,#9568,#9569),.UNSPECIFIED.,.F.,.F.,(4,3,3,
3,3,3,3,3,4),(13.682990847966,13.9662837703184,14.9638754681983,15.9614671660782,
16.959058863958,17.9566505618379,18.9542422597178,19.9518339575977,19.9661761551456),
 .UNSPECIFIED.);
#196=B_SPLINE_CURVE_WITH_KNOTS('',3,(#9574,#9575,#9576,#9577,#9578,#9579,
#9580,#9581,#9582,#9583,#9584,#9585,#9586,#9587,#9588,#9589,#9590,#9591,
#9592,#9593,#9594,#9595),.UNSPECIFIED.,.F.,.F.,(4,3,3,3,3,3,3,4),(-29.2243112993258,
-28.9194285991847,-27.9222069233507,-26.9249852475168,-25.9277635716828,
-24.9305418958489,-23.9333202200149,-22.9411259921462),.UNSPECIFIED.);
#197=B_SPLINE_CURVE_WITH_KNOTS('',3,(#9596,#9597,#9598,#9599,#9600,#9601,
#9602,#9603,#9604,#9605,#9606,#9607,#9608,#9609,#9610,#9611,#9612,#9613,
#9614,#9615,#9616,#9617),.UNSPECIFIED.,.F.,.F.,(4,3,3,3,3,3,3,4),(19.9661761551456,
20.9494256554776,21.9470173533575,22.9446090512374,23.9422007491172,24.9397924469971,
25.937384144877,26.2493614623252),.UNSPECIFIED.);
#198=B_SPLINE_CURVE_WITH_KNOTS('',3,(#9622,#9623,#9624,#9625,#9626,#9627,
#9628,#9629,#9630,#9631,#9632,#9633,#9634,#9635,#9636,#9637,#9638,#9639,
#9640,#9641,#9642,#9643),.UNSPECIFIED.,.F.,.F.,(4,3,3,3,3,3,3,4),(-35.5074966065054,
-34.9027586541884,-33.9055369783545,-32.9083153025205,-31.9110936266866,
-30.9138719508526,-29.9166502750186,-29.2243112993258),.UNSPECIFIED.);
#199=B_SPLINE_CURVE_WITH_KNOTS('',3,(#9644,#9645,#9646,#9647,#9648,#9649,
#9650,#9651,#9652,#9653,#9654,#9655,#9656,#9657,#9658,#9659,#9660,#9661,
#9662,#9663,#9664,#9665),.UNSPECIFIED.,.F.,.F.,(4,3,3,3,3,3,3,4),(26.2493614623252,
26.9349758427569,27.9325675406368,28.9301592385167,29.9277509363966,30.9253426342764,
31.9229343321563,32.5325467695048),.UNSPECIFIED.);
#200=B_SPLINE_CURVE_WITH_KNOTS('',3,(#9670,#9671,#9672,#9673,#9674,#9675,
#9676,#9677,#9678,#9679,#9680,#9681,#9682,#9683,#9684,#9685,#9686,#9687,
#9688,#9689,#9690,#9691),.UNSPECIFIED.,.F.,.F.,(4,3,3,3,3,3,3,4),(-41.790681913685,
-40.8860887091922,-39.8888670333582,-38.8916453575242,-37.8944236816903,
-36.8972020058563,-35.8999803300224,-35.5074966065054),.UNSPECIFIED.);
#201=B_SPLINE_CURVE_WITH_KNOTS('',3,(#9692,#9693,#9694,#9695,#9696,#9697,
#9698,#9699,#9700,#9701,#9702,#9703,#9704,#9705,#9706,#9707,#9708,#9709,
#9710,#9711,#9712,#9713),.UNSPECIFIED.,.F.,.F.,(4,3,3,3,3,3,3,4),(32.5325467695048,
32.9205260300362,33.9181177279161,34.915709425796,35.9133011236759,36.9108928215558,
37.9084845194357,38.8157320766844),.UNSPECIFIED.);
#202=B_SPLINE_CURVE_WITH_KNOTS('',3,(#9718,#9719,#9720,#9721,#9722,#9723,
#9724,#9725,#9726,#9727,#9728,#9729,#9730,#9731,#9732,#9733,#9734,#9735,
#9736,#9737,#9738,#9739,#9740,#9741,#9742),.UNSPECIFIED.,.F.,.F.,(4,3,3,
3,3,3,3,3,4),(-48.0738672208646,-47.8666404400298,-46.8694187641959,-45.8721970883619,
-44.874975412528,-43.877753736694,-42.8805320608601,-41.8833103850261,-41.790681913685),
 .UNSPECIFIED.);
#203=B_SPLINE_CURVE_WITH_KNOTS('',3,(#9743,#9744,#9745,#9746,#9747,#9748,
#9749,#9750,#9751,#9752,#9753,#9754,#9755,#9756,#9757,#9758,#9759,#9760,
#9761,#9762,#9763,#9764,#9765,#9766,#9767),.UNSPECIFIED.,.F.,.F.,(4,3,3,
3,3,3,3,3,4),(38.8157320766844,38.9060762173155,39.9036679151954,40.9012596130753,
41.8988513109552,42.8964430088351,43.8940347067149,44.8916264045948,45.098917383864),
 .UNSPECIFIED.);
#204=B_SPLINE_CURVE_WITH_KNOTS('',3,(#9772,#9773,#9774,#9775,#9776,#9777,
#9778,#9779,#9780,#9781,#9782,#9783,#9784,#9785,#9786,#9787,#9788,#9789,
#9790,#9791,#9792,#9793),.UNSPECIFIED.,.F.,.F.,(4,3,3,3,3,3,3,4),(-54.3570525280442,
-53.8499704950336,-52.8527488191996,-51.8555271433657,-50.8583054675317,
-49.8610837916978,-48.8638621158638,-48.0738672208646),.UNSPECIFIED.);
#205=B_SPLINE_CURVE_WITH_KNOTS('',3,(#9794,#9795,#9796,#9797,#9798,#9799,
#9800,#9801,#9802,#9803,#9804,#9805,#9806,#9807,#9808,#9809,#9810,#9811,
#9812,#9813,#9814,#9815),.UNSPECIFIED.,.F.,.F.,(4,3,3,3,3,3,3,4),(45.098917383864,
45.8892181024747,46.8868098003546,47.8844014982345,48.8819931961144,49.8795848939942,
50.8771765918741,51.3821026910436),.UNSPECIFIED.);
#206=B_SPLINE_CURVE_WITH_KNOTS('',3,(#9820,#9821,#9822,#9823,#9824,#9825,
#9826,#9827,#9828,#9829,#9830,#9831,#9832,#9833,#9834,#9835,#9836,#9837,
#9838,#9839,#9840,#9841),.UNSPECIFIED.,.F.,.F.,(4,3,3,3,3,3,3,4),(-60.6402378352238,
-59.8333005500373,-58.8360788742033,-57.8388571983694,-56.8416355225354,
-55.8444138467015,-54.8471921708675,-54.3570525280442),.UNSPECIFIED.);
#207=B_SPLINE_CURVE_WITH_KNOTS('',3,(#9842,#9843,#9844,#9845,#9846,#9847,
#9848,#9849,#9850,#9851,#9852,#9853,#9854,#9855,#9856,#9857,#9858,#9859,
#9860,#9861,#9862,#9863),.UNSPECIFIED.,.F.,.F.,(4,3,3,3,3,3,3,4),(51.3821026910436,
51.874768289754,52.8723599876339,53.8699516855138,54.8675433833937,55.8651350812736,
56.8627267791534,57.6652879982231),.UNSPECIFIED.);
#208=B_SPLINE_CURVE_WITH_KNOTS('',3,(#9868,#9869,#9870,#9871,#9872,#9873,
#9874,#9875,#9876,#9877,#9878,#9879,#9880,#9881,#9882,#9883,#9884,#9885,
#9886,#9887,#9888,#9889,#9890,#9891,#9892),.UNSPECIFIED.,.F.,.F.,(4,3,3,
3,3,3,3,3,4),(-66.9234231424034,-66.813852280875,-65.816630605041,-64.8194089292071,
-63.8221872533731,-62.8249655775391,-61.8277439017052,-60.8305222258712,
-60.6402378352238),.UNSPECIFIED.);
#209=B_SPLINE_CURVE_WITH_KNOTS('',3,(#9893,#9894,#9895,#9896,#9897,#9898,
#9899,#9900,#9901,#9902,#9903,#9904,#9905,#9906,#9907,#9908,#9909,#9910,
#9911,#9912,#9913,#9914,#9915,#9916,#9917),.UNSPECIFIED.,.F.,.F.,(4,3,3,
3,3,3,3,3,4),(57.6652879982231,57.8603184770333,58.8579101749132,59.8555018727931,
60.853093570673,61.8506852685529,62.8482769664328,63.8458686643126,63.9484733054027),
 .UNSPECIFIED.);
#210=B_SPLINE_CURVE_WITH_KNOTS('',3,(#9922,#9923,#9924,#9925,#9926,#9927,
#9928,#9929,#9930,#9931,#9932,#9933,#9934,#9935,#9936,#9937,#9938,#9939,
#9940,#9941,#9942,#9943),.UNSPECIFIED.,.F.,.F.,(4,3,3,3,3,3,3,4),(-73.206608449583,
-72.7971823358787,-71.7999606600447,-70.8027389842108,-69.8055173083768,
-68.8082956325429,-67.8110739567089,-66.9234231424034),.UNSPECIFIED.);
#211=B_SPLINE_CURVE_WITH_KNOTS('',3,(#9944,#9945,#9946,#9947,#9948,#9949,
#9950,#9951,#9952,#9953,#9954,#9955,#9956,#9957,#9958,#9959,#9960,#9961,
#9962,#9963,#9964,#9965),.UNSPECIFIED.,.F.,.F.,(4,3,3,3,3,3,3,4),(63.9484733054027,
64.8434603621925,65.8410520600724,66.8386437579523,67.8362354558322,68.8338271537121,
69.8314188515919,70.2316586125823),.UNSPECIFIED.);
#212=B_SPLINE_CURVE_WITH_KNOTS('',3,(#9970,#9971,#9972,#9973,#9974,#9975,
#9976,#9977,#9978,#9979,#9980,#9981,#9982,#9983,#9984,#9985,#9986,#9987,
#9988,#9989,#9990,#9991),.UNSPECIFIED.,.F.,.F.,(4,3,3,3,3,3,3,4),(-79.4897937567626,
-78.7805123908824,-77.7832907150485,-76.7860690392145,-75.7888473633806,
-74.7916256875466,-73.7944040117127,-73.206608449583),.UNSPECIFIED.);
#213=B_SPLINE_CURVE_WITH_KNOTS('',3,(#9992,#9993,#9994,#9995,#9996,#9997,
#9998,#9999,#10000,#10001,#10002,#10003,#10004,#10005,#10006,#10007,#10008,
#10009,#10010,#10011,#10012,#10013),.UNSPECIFIED.,.F.,.F.,(4,3,3,3,3,3,
3,4),(70.2316586125823,70.8290105494718,71.8266022473517,72.8241939452316,
73.8217856431115,74.8193773409914,75.8169690388713,76.5148439197619),
 .UNSPECIFIED.);
#214=B_SPLINE_CURVE_WITH_KNOTS('',3,(#10018,#10019,#10020,#10021,#10022,
#10023,#10024,#10025,#10026,#10027,#10028,#10029,#10030,#10031,#10032,#10033,
#10034,#10035,#10036,#10037,#10038,#10039,#10040,#10041,#10042),
 .UNSPECIFIED.,.F.,.F.,(4,3,3,3,3,3,3,3,4),(-85.7729790639421,-85.7610641217201,
-84.7638424458862,-83.7666207700522,-82.7693990942182,-81.7721774183843,
-80.7749557425504,-79.7777340667164,-79.4897937567626),.UNSPECIFIED.);
#215=B_SPLINE_CURVE_WITH_KNOTS('',3,(#10043,#10044,#10045,#10046,#10047,
#10048,#10049,#10050,#10051,#10052,#10053,#10054,#10055,#10056,#10057,#10058,
#10059,#10060,#10061,#10062,#10063,#10064),.UNSPECIFIED.,.F.,.F.,(4,3,3,
3,3,3,3,4),(76.5148439197619,76.8145607367511,77.812152434631,78.8097441325109,
79.8073358303908,80.8049275282707,81.8025192261506,82.7980292269415),
 .UNSPECIFIED.);
#216=B_SPLINE_CURVE_WITH_KNOTS('',3,(#10069,#10070,#10071,#10072,#10073,
#10074,#10075,#10076,#10077,#10078,#10079,#10080,#10081,#10082,#10083,#10084,
#10085,#10086,#10087,#10088,#10089,#10090),.UNSPECIFIED.,.F.,.F.,(4,3,3,
3,3,3,3,4),(-92.0561643711217,-91.7443941767238,-90.7471725008899,-89.7499508250559,
-88.752729149222,-87.755507473388,-86.7582857975541,-85.7729790639421),
 .UNSPECIFIED.);
#217=B_SPLINE_CURVE_WITH_KNOTS('',3,(#10091,#10092,#10093,#10094,#10095,
#10096,#10097,#10098,#10099,#10100,#10101,#10102,#10103,#10104,#10105,#10106,
#10107,#10108,#10109,#10110,#10111,#10112),.UNSPECIFIED.,.F.,.F.,(4,3,3,
3,3,3,3,4),(82.7980292269415,83.7977026219104,84.7952943197902,85.7928860176701,
86.79047771555,87.7880694134299,88.7856611113098,89.0812145341211),
 .UNSPECIFIED.);
#218=B_SPLINE_CURVE_WITH_KNOTS('',3,(#10117,#10118,#10119,#10120,#10121,
#10122,#10123,#10124,#10125,#10126,#10127,#10128,#10129,#10130,#10131,#10132,
#10133,#10134,#10135,#10136,#10137,#10138),.UNSPECIFIED.,.F.,.F.,(4,3,3,
3,3,3,3,4),(-98.3393496783013,-97.7277242317276,-96.7305025558936,-95.7332808800597,
-94.7360592042257,-93.7388375283918,-92.7416158525578,-92.0561643711217),
 .UNSPECIFIED.);
#219=B_SPLINE_CURVE_WITH_KNOTS('',3,(#10139,#10140,#10141,#10142,#10143,
#10144,#10145,#10146,#10147,#10148,#10149,#10150,#10151,#10152,#10153,#10154,
#10155,#10156,#10157,#10158,#10159,#10160),.UNSPECIFIED.,.F.,.F.,(4,3,3,
3,3,3,3,4),(89.0812145341211,89.7832528091896,90.7808445070695,91.7784362049494,
92.7760279028293,93.7736196007092,94.771211298589,95.3643998413007),
 .UNSPECIFIED.);
#220=B_SPLINE_CURVE_WITH_KNOTS('',3,(#10165,#10166,#10167,#10168,#10169,
#10170,#10171,#10172,#10173,#10174,#10175,#10176,#10177,#10178,#10179,#10180,
#10181,#10182,#10183,#10184,#10185,#10186),.UNSPECIFIED.,.F.,.F.,(4,3,3,
3,3,3,3,4),(-104.622534985481,-103.711054286731,-102.713832610897,-101.716610935063,
-100.719389259229,-99.7221675833955,-98.7249459075615,-98.3393496783013),
 .UNSPECIFIED.);
#221=B_SPLINE_CURVE_WITH_KNOTS('',3,(#10187,#10188,#10189,#10190,#10191,
#10192,#10193,#10194,#10195,#10196,#10197,#10198,#10199,#10200,#10201,#10202,
#10203,#10204,#10205,#10206,#10207,#10208),.UNSPECIFIED.,.F.,.F.,(4,3,3,
3,3,3,3,4),(95.3643998413007,95.7688029964689,96.7663946943488,97.7639863922287,
98.7615780901086,99.7591697879885,100.756761485868,101.64758514848),
 .UNSPECIFIED.);
#222=B_SPLINE_CURVE_WITH_KNOTS('',3,(#10213,#10214,#10215,#10216,#10217,
#10218,#10219,#10220,#10221,#10222,#10223,#10224,#10225,#10226,#10227,#10228,
#10229,#10230,#10231,#10232,#10233,#10234,#10235,#10236,#10237),
 .UNSPECIFIED.,.F.,.F.,(4,3,3,3,3,3,3,3,4),(-110.905720292661,-110.691606017569,
-109.694384341735,-108.697162665901,-107.699940990067,-106.702719314233,
-105.705497638399,-104.708275962565,-104.622534985481),.UNSPECIFIED.);
#223=B_SPLINE_CURVE_WITH_KNOTS('',3,(#10238,#10239,#10240,#10241,#10242,
#10243,#10244,#10245,#10246,#10247,#10248,#10249,#10250,#10251,#10252,#10253,
#10254,#10255,#10256,#10257,#10258,#10259,#10260,#10261,#10262),
 .UNSPECIFIED.,.F.,.F.,(4,3,3,3,3,3,3,3,4),(101.64758514848,101.754353183748,
102.751944881628,103.749536579508,104.747128277388,105.744719975268,106.742311673148,
107.739903371028,107.93077045566),.UNSPECIFIED.);
#224=B_SPLINE_CURVE_WITH_KNOTS('',3,(#10267,#10268,#10269,#10270,#10271,
#10272,#10273,#10274,#10275,#10276,#10277,#10278,#10279,#10280,#10281,#10282,
#10283,#10284,#10285,#10286,#10287,#10288),.UNSPECIFIED.,.F.,.F.,(4,3,3,
3,3,3,3,4),(-117.18890559984,-116.674936072573,-115.677714396739,-114.680492720905,
-113.683271045071,-112.686049369237,-111.688827693403,-110.905720292661),
 .UNSPECIFIED.);
#225=B_SPLINE_CURVE_WITH_KNOTS('',3,(#10289,#10290,#10291,#10292,#10293,
#10294,#10295,#10296,#10297,#10298,#10299,#10300,#10301,#10302,#10303,#10304,
#10305,#10306,#10307,#10308,#10309,#10310),.UNSPECIFIED.,.F.,.F.,(4,3,3,
3,3,3,3,4),(107.93077045566,108.737495068907,109.735086766787,110.732678464667,
111.730270162547,112.727861860427,113.725453558307,114.213955762839),
 .UNSPECIFIED.);
#226=B_SPLINE_CURVE_WITH_KNOTS('',3,(#10315,#10316,#10317,#10318,#10319,
#10320,#10321,#10322,#10323,#10324,#10325,#10326,#10327,#10328,#10329,#10330,
#10331,#10332,#10333,#10334,#10335,#10336),.UNSPECIFIED.,.F.,.F.,(4,3,3,
3,3,3,3,4),(-123.47209090702,-122.658266127576,-121.661044451742,-120.663822775909,
-119.666601100075,-118.669379424241,-117.672157748407,-117.18890559984),
 .UNSPECIFIED.);
#227=B_SPLINE_CURVE_WITH_KNOTS('',3,(#10337,#10338,#10339,#10340,#10341,
#10342,#10343,#10344,#10345,#10346,#10347,#10348,#10349,#10350,#10351,#10352,
#10353,#10354,#10355,#10356,#10357,#10358),.UNSPECIFIED.,.F.,.F.,(4,3,3,
3,3,3,3,4),(114.213955762839,114.723045256187,115.720636954067,116.718228651947,
117.715820349826,118.713412047706,119.711003745586,120.497141070019),
 .UNSPECIFIED.);
#228=B_SPLINE_CURVE_WITH_KNOTS('',3,(#10363,#10364,#10365,#10366,#10367,
#10368,#10369,#10370,#10371,#10372,#10373,#10374,#10375,#10376,#10377,#10378,
#10379,#10380,#10381,#10382,#10383,#10384,#10385,#10386,#10387),
 .UNSPECIFIED.,.F.,.F.,(4,3,3,3,3,3,3,3,4),(-129.755276214199,-129.638817858414,
-128.64159618258,-127.644374506746,-126.647152830912,-125.649931155078,
-124.652709479244,-123.65548780341,-123.47209090702),.UNSPECIFIED.);
#229=B_SPLINE_CURVE_WITH_KNOTS('',3,(#10388,#10389,#10390,#10391,#10392,
#10393,#10394,#10395,#10396,#10397,#10398,#10399,#10400,#10401,#10402,#10403,
#10404,#10405,#10406,#10407,#10408,#10409,#10410,#10411,#10412),
 .UNSPECIFIED.,.F.,.F.,(4,3,3,3,3,3,3,3,4),(120.497141070019,120.708595443466,
121.706187141346,122.703778839226,123.701370537106,124.698962234986,125.696553932865,
126.694145630745,126.780326377199),.UNSPECIFIED.);
#230=B_SPLINE_CURVE_WITH_KNOTS('',3,(#10417,#10418,#10419,#10420,#10421,
#10422,#10423,#10424,#10425,#10426,#10427,#10428,#10429,#10430,#10431,#10432,
#10433,#10434,#10435,#10436,#10437,#10438),.UNSPECIFIED.,.F.,.F.,(4,3,3,
3,3,3,3,4),(-136.038461521379,-135.622147913418,-134.624926237584,-133.62770456175,
-132.630482885916,-131.633261210082,-130.636039534248,-129.755276214199),
 .UNSPECIFIED.);
#231=B_SPLINE_CURVE_WITH_KNOTS('',3,(#10439,#10440,#10441,#10442,#10443,
#10444,#10445,#10446,#10447,#10448,#10449,#10450,#10451,#10452,#10453,#10454,
#10455,#10456,#10457,#10458,#10459,#10460),.UNSPECIFIED.,.F.,.F.,(4,3,3,
3,3,3,3,4),(126.780326377199,127.691737328625,128.689329026505,129.686920724385,
130.684512422265,131.682104120145,132.679695818025,133.063511684378),
 .UNSPECIFIED.);
#232=B_SPLINE_CURVE_WITH_KNOTS('',3,(#10465,#10466,#10467,#10468,#10469,
#10470,#10471,#10472,#10473,#10474,#10475,#10476,#10477,#10478,#10479,#10480,
#10481,#10482,#10483,#10484,#10485,#10486),.UNSPECIFIED.,.F.,.F.,(4,3,3,
3,3,3,3,4),(-142.321646828558,-141.605477968422,-140.608256292588,-139.611034616754,
-138.61381294092,-137.616591265086,-136.619369589252,-136.038461521379),
 .UNSPECIFIED.);
#233=B_SPLINE_CURVE_WITH_KNOTS('',3,(#10487,#10488,#10489,#10490,#10491,
#10492,#10493,#10494,#10495,#10496,#10497,#10498,#10499,#10500,#10501,#10502,
#10503,#10504,#10505,#10506,#10507,#10508),.UNSPECIFIED.,.F.,.F.,(4,3,3,
3,3,3,3,4),(133.063511684378,133.677287515905,134.674879213784,135.672470911664,
136.670062609544,137.667654307424,138.665246005304,139.346696991558),
 .UNSPECIFIED.);
#234=B_SPLINE_CURVE_WITH_KNOTS('',3,(#10513,#10514,#10515,#10516,#10517,
#10518,#10519,#10520,#10521,#10522,#10523,#10524,#10525,#10526,#10527,#10528,
#10529,#10530,#10531,#10532,#10533,#10534,#10535,#10536,#10537),
 .UNSPECIFIED.,.F.,.F.,(4,3,3,3,3,3,3,3,4),(-148.604832135738,-148.586029699259,
-147.588808023425,-146.591586347591,-145.594364671757,-144.597142995923,
-143.599921320089,-142.602699644256,-142.321646828558),.UNSPECIFIED.);
#235=B_SPLINE_CURVE_WITH_KNOTS('',3,(#10538,#10539,#10540,#10541,#10542,
#10543,#10544,#10545,#10546,#10547,#10548,#10549,#10550,#10551,#10552,#10553,
#10554,#10555,#10556,#10557,#10558,#10559),.UNSPECIFIED.,.F.,.F.,(4,3,3,
3,3,3,3,4),(139.346696991558,139.662837703184,140.660429401064,141.658021098944,
142.655612796824,143.653204494703,144.650796192583,145.629882298737),
 .UNSPECIFIED.);
#236=B_SPLINE_CURVE_WITH_KNOTS('',3,(#10564,#10565,#10566,#10567,#10568,
#10569,#10570,#10571,#10572,#10573,#10574,#10575,#10576,#10577,#10578,#10579,
#10580,#10581,#10582,#10583,#10584,#10585),.UNSPECIFIED.,.F.,.F.,(4,3,3,
3,3,3,3,4),(-154.888017442918,-154.569359754263,-153.572138078429,-152.574916402595,
-151.577694726761,-150.580473050927,-149.583251375093,-148.604832135738),
 .UNSPECIFIED.);
#237=B_SPLINE_CURVE_WITH_KNOTS('',3,(#10586,#10587,#10588,#10589,#10590,
#10591,#10592,#10593,#10594,#10595,#10596,#10597,#10598,#10599,#10600,#10601,
#10602,#10603,#10604,#10605,#10606,#10607,#10608,#10609,#10610),
 .UNSPECIFIED.,.F.,.F.,(4,3,3,3,3,3,3,3,4),(145.629882298737,145.648387890463,
146.645979588343,147.643571286223,148.641162984103,149.638754681983,150.636346379863,
151.633938077743,151.913067605917),.UNSPECIFIED.);
#238=B_SPLINE_CURVE_WITH_KNOTS('',3,(#10615,#10616,#10617,#10618,#10619,
#10620,#10621,#10622,#10623,#10624,#10625,#10626,#10627,#10628,#10629,#10630,
#10631,#10632,#10633,#10634,#10635,#10636),.UNSPECIFIED.,.F.,.F.,(4,3,3,
3,3,3,3,4),(-161.171202750097,-160.552689809267,-159.555468133433,-158.558246457599,
-157.561024781765,-156.563803105931,-155.566581430097,-154.888017442918),
 .UNSPECIFIED.);
#239=B_SPLINE_CURVE_WITH_KNOTS('',3,(#10637,#10638,#10639,#10640,#10641,
#10642,#10643,#10644,#10645,#10646,#10647,#10648,#10649,#10650,#10651,#10652,
#10653,#10654,#10655,#10656,#10657,#10658),.UNSPECIFIED.,.F.,.F.,(4,3,3,
3,3,3,3,4),(151.913067605917,152.631529775622,153.629121473502,154.626713171382,
155.624304869262,156.621896567142,157.619488265022,158.196252913097),
 .UNSPECIFIED.);
#240=B_SPLINE_CURVE_WITH_KNOTS('',3,(#10663,#10664,#10665,#10666,#10667,
#10668,#10669,#10670,#10671,#10672,#10673,#10674,#10675,#10676,#10677,#10678,
#10679,#10680,#10681,#10682,#10683,#10684),.UNSPECIFIED.,.F.,.F.,(4,3,3,
3,3,3,3,4),(-167.454388057277,-166.53601986427,-165.538798188436,-164.541576512603,
-163.544354836769,-162.547133160935,-161.549911485101,-161.171202750097),
 .UNSPECIFIED.);
#241=B_SPLINE_CURVE_WITH_KNOTS('',3,(#10685,#10686,#10687,#10688,#10689,
#10690,#10691,#10692,#10693,#10694,#10695,#10696,#10697,#10698,#10699,#10700,
#10701,#10702,#10703,#10704,#10705,#10706),.UNSPECIFIED.,.F.,.F.,(4,3,3,
3,3,3,3,4),(158.196252913097,158.617079962902,159.614671660782,160.612263358661,
161.609855056541,162.607446754421,163.605038452301,164.479438220276),
 .UNSPECIFIED.);
#242=B_SPLINE_CURVE_WITH_KNOTS('',3,(#10711,#10712,#10713,#10714,#10715,
#10716,#10717,#10718,#10719,#10720,#10721,#10722,#10723,#10724,#10725,#10726,
#10727,#10728,#10729,#10730,#10731,#10732,#10733,#10734,#10735),
 .UNSPECIFIED.,.F.,.F.,(4,3,3,3,3,3,3,3,4),(-173.737573364456,-173.516571595108,
-172.519349919274,-171.52212824344,-170.524906567606,-169.527684891772,
-168.530463215938,-167.533241540104,-167.454388057277),.UNSPECIFIED.);
#243=B_SPLINE_CURVE_WITH_KNOTS('',3,(#10736,#10737,#10738,#10739,#10740,
#10741,#10742,#10743,#10744,#10745,#10746,#10747,#10748,#10749,#10750,#10751,
#10752,#10753,#10754,#10755,#10756,#10757,#10758,#10759,#10760),
 .UNSPECIFIED.,.F.,.F.,(4,3,3,3,3,3,3,3,4),(164.479438220276,164.602630150181,
165.600221848061,166.597813545941,167.595405243821,168.592996941701,169.59058863958,
170.58818033746,170.762623527456),.UNSPECIFIED.);
#244=B_SPLINE_CURVE_WITH_KNOTS('',3,(#10765,#10766,#10767,#10768,#10769,
#10770,#10771,#10772,#10773,#10774,#10775,#10776,#10777,#10778,#10779,#10780,
#10781,#10782,#10783,#10784,#10785,#10786),.UNSPECIFIED.,.F.,.F.,(4,3,3,
3,3,3,3,4),(-180.020758671636,-179.499901650112,-178.502679974278,-177.505458298444,
-176.50823662261,-175.511014946776,-174.513793270942,-173.737573364456),
 .UNSPECIFIED.);
#245=B_SPLINE_CURVE_WITH_KNOTS('',3,(#10787,#10788,#10789,#10790,#10791,
#10792,#10793,#10794,#10795,#10796,#10797,#10798,#10799,#10800,#10801,#10802,
#10803,#10804,#10805,#10806,#10807,#10808),.UNSPECIFIED.,.F.,.F.,(4,3,3,
3,3,3,3,4),(170.762623527456,171.58577203534,172.58336373322,173.5809554311,
174.57854712898,175.57613882686,176.57373052474,177.045808834635),
 .UNSPECIFIED.);
#246=B_SPLINE_CURVE_WITH_KNOTS('',3,(#10813,#10814,#10815,#10816,#10817,
#10818,#10819,#10820,#10821,#10822,#10823,#10824,#10825,#10826,#10827,#10828,
#10829,#10830,#10831,#10832,#10833,#10834),.UNSPECIFIED.,.F.,.F.,(4,3,3,
3,3,3,3,4),(-186.303943978815,-185.483231705116,-184.486010029282,-183.488788353448,
-182.491566677614,-181.49434500178,-180.497123325946,-180.020758671636),
 .UNSPECIFIED.);
#247=B_SPLINE_CURVE_WITH_KNOTS('',3,(#10835,#10836,#10837,#10838,#10839,
#10840,#10841,#10842,#10843,#10844,#10845,#10846,#10847,#10848,#10849,#10850,
#10851,#10852,#10853,#10854,#10855,#10856),.UNSPECIFIED.,.F.,.F.,(4,3,3,
3,3,3,3,4),(177.045808834635,177.57132222262,178.568913920499,179.566505618379,
180.564097316259,181.561689014139,182.559280712019,183.328994141815),
 .UNSPECIFIED.);
#248=B_SPLINE_CURVE_WITH_KNOTS('',3,(#10862,#10863,#10864,#10865,#10866,
#10867,#10868,#10869,#10870,#10871),.UNSPECIFIED.,.F.,.F.,(4,1,1,1,1,1,
1,4),(197.920337176157,198.096846578291,199.094068254125,200.091289929959,
201.088511605793,202.085733281627,203.082954957461,204.080176633295),
 .UNSPECIFIED.);
#249=B_SPLINE_CURVE_WITH_KNOTS('',3,(#10874,#10875,#10876,#10877,#10878,
#10879,#10880,#10881),.UNSPECIFIED.,.F.,.F.,(4,1,1,1,1,4),(197.920337176157,
198.848172022221,199.845763720101,200.843355417981,201.84094711586,202.83853881374),
 .UNSPECIFIED.);
#250=B_SPLINE_CURVE_WITH_KNOTS('',3,(#10886,#10887,#10888,#10889,#10890,
#10891,#10892,#10893,#10894,#10895),.UNSPECIFIED.,.F.,.F.,(4,1,1,1,1,1,
1,4),(191.637151868977,192.113516523288,193.110738199121,194.107959874955,
195.105181550789,196.102403226623,197.099624902457,197.920337176157),
 .UNSPECIFIED.);
#251=B_SPLINE_CURVE_WITH_KNOTS('',3,(#10896,#10897,#10898,#10899,#10900,
#10901,#10902,#10903,#10904,#10905,#10906),.UNSPECIFIED.,.F.,.F.,(4,1,1,
1,1,1,1,1,4),(191.637151868977,191.865030137062,192.862621834942,193.860213532821,
194.857805230701,195.855396928581,196.852988626461,197.850580324341,197.920337176157),
 .UNSPECIFIED.);
#252=B_SPLINE_CURVE_WITH_KNOTS('',3,(#10911,#10912,#10913,#10914,#10915,
#10916,#10917,#10918,#10919,#10920),.UNSPECIFIED.,.F.,.F.,(4,1,1,1,1,1,
1,4),(185.353966561798,186.130186468284,187.127408144118,188.124629819952,
189.121851495786,190.11907317162,191.116294847454,191.637151868977),
 .UNSPECIFIED.);
#253=B_SPLINE_CURVE_WITH_KNOTS('',3,(#10921,#10922,#10923,#10924,#10925,
#10926,#10927,#10928,#10929,#10930),.UNSPECIFIED.,.F.,.F.,(4,1,1,1,1,1,
1,4),(185.353966561798,185.879479949782,186.877071647662,187.874663345542,
188.872255043422,189.869846741302,190.867438439182,191.637151868977),
 .UNSPECIFIED.);
#254=B_SPLINE_CURVE_WITH_KNOTS('',3,(#10935,#10936,#10937,#10938,#10939,
#10940,#10941,#10942,#10943,#10944,#10945),.UNSPECIFIED.,.F.,.F.,(4,1,1,
1,1,1,1,1,4),(179.070781254618,179.149634737446,180.14685641328,181.144078089114,
182.141299764948,183.138521440782,184.135743116616,185.13296479245,185.353966561798),
 .UNSPECIFIED.);
#255=B_SPLINE_CURVE_WITH_KNOTS('',3,(#10946,#10947,#10948,#10949,#10950,
#10951,#10952,#10953,#10954,#10955),.UNSPECIFIED.,.F.,.F.,(4,1,1,1,1,1,
1,4),(179.070781254618,179.893929762503,180.891521460383,181.889113158263,
182.886704856143,183.884296554023,184.881888251902,185.353966561798),
 .UNSPECIFIED.);
#256=B_SPLINE_CURVE_WITH_KNOTS('',3,(#10960,#10961,#10962,#10963,#10964,
#10965,#10966,#10967,#10968,#10969),.UNSPECIFIED.,.F.,.F.,(4,1,1,1,1,1,
1,4),(172.787595947439,173.166304682442,174.163526358276,175.16074803411,
176.157969709944,177.155191385778,178.152413061612,179.070781254618),
 .UNSPECIFIED.);
#257=B_SPLINE_CURVE_WITH_KNOTS('',3,(#10970,#10971,#10972,#10973,#10974,
#10975,#10976,#10977,#10978,#10979,#10980),.UNSPECIFIED.,.F.,.F.,(4,1,1,
1,1,1,1,1,4),(172.787595947439,172.910787877344,173.908379575224,174.905971273104,
175.903562970983,176.901154668863,177.898746366743,178.896338064623,179.070781254618),
 .UNSPECIFIED.);
#258=B_SPLINE_CURVE_WITH_KNOTS('',3,(#10985,#10986,#10987,#10988,#10989,
#10990,#10991,#10992,#10993,#10994),.UNSPECIFIED.,.F.,.F.,(4,1,1,1,1,1,
1,4),(166.504410640259,167.182974627439,168.180196303273,169.177417979107,
170.17463965494,171.171861330774,172.169083006608,172.787595947439),
 .UNSPECIFIED.);
#259=B_SPLINE_CURVE_WITH_KNOTS('',3,(#10995,#10996,#10997,#10998,#10999,
#11000,#11001,#11002,#11003,#11004),.UNSPECIFIED.,.F.,.F.,(4,1,1,1,1,1,
1,4),(166.504410640259,166.925237690065,167.922829387944,168.920421085824,
169.918012783704,170.915604481584,171.913196179464,172.787595947439),
 .UNSPECIFIED.);
#260=B_SPLINE_CURVE_WITH_KNOTS('',3,(#11009,#11010,#11011,#11012,#11013,
#11014,#11015,#11016,#11017,#11018),.UNSPECIFIED.,.F.,.F.,(4,1,1,1,1,1,
1,4),(160.22122533308,161.199644572435,162.196866248269,163.194087924103,
164.191309599937,165.188531275771,166.185752951605,166.504410640259),
 .UNSPECIFIED.);
#261=B_SPLINE_CURVE_WITH_KNOTS('',3,(#11019,#11020,#11021,#11022,#11023,
#11024,#11025,#11026,#11027,#11028),.UNSPECIFIED.,.F.,.F.,(4,1,1,1,1,1,
1,4),(160.22122533308,160.939687502785,161.937279200665,162.934870898545,
163.932462596425,164.930054294305,165.927645992185,166.504410640259),
 .UNSPECIFIED.);
#262=B_SPLINE_CURVE_WITH_KNOTS('',3,(#11033,#11034,#11035,#11036,#11037,
#11038,#11039,#11040,#11041,#11042,#11043),.UNSPECIFIED.,.F.,.F.,(4,1,1,
1,1,1,1,1,4),(153.9380400259,154.219092841597,155.216314517431,156.213536193265,
157.210757869099,158.207979544933,159.205201220767,160.202422896601,160.22122533308),
 .UNSPECIFIED.);
#263=B_SPLINE_CURVE_WITH_KNOTS('',3,(#11044,#11045,#11046,#11047,#11048,
#11049,#11050,#11051,#11052,#11053,#11054),.UNSPECIFIED.,.F.,.F.,(4,1,1,
1,1,1,1,1,4),(153.9380400259,153.956545617626,154.954137315506,155.951729013386,
156.949320711266,157.946912409146,158.944504107025,159.942095804905,160.22122533308),
 .UNSPECIFIED.);
#264=B_SPLINE_CURVE_WITH_KNOTS('',3,(#11059,#11060,#11061,#11062,#11063,
#11064,#11065,#11066,#11067,#11068),.UNSPECIFIED.,.F.,.F.,(4,1,1,1,1,1,
1,4),(147.65485471872,148.235762786593,149.232984462427,150.230206138261,
151.227427814095,152.224649489929,153.221871165763,153.9380400259),
 .UNSPECIFIED.);
#265=B_SPLINE_CURVE_WITH_KNOTS('',3,(#11069,#11070,#11071,#11072,#11073,
#11074,#11075,#11076,#11077,#11078),.UNSPECIFIED.,.F.,.F.,(4,1,1,1,1,1,
1,4),(147.65485471872,147.970995430347,148.968587128227,149.966178826106,
150.963770523986,151.961362221866,152.958953919746,153.9380400259),
 .UNSPECIFIED.);
#266=B_SPLINE_CURVE_WITH_KNOTS('',3,(#11083,#11084,#11085,#11086,#11087,
#11088,#11089,#11090,#11091,#11092),.UNSPECIFIED.,.F.,.F.,(4,1,1,1,1,1,
1,4),(141.371669411541,142.25243273159,143.249654407424,144.246876083258,
145.244097759092,146.241319434926,147.23854111076,147.65485471872),
 .UNSPECIFIED.);
#267=B_SPLINE_CURVE_WITH_KNOTS('',3,(#11093,#11094,#11095,#11096,#11097,
#11098,#11099,#11100,#11101,#11102),.UNSPECIFIED.,.F.,.F.,(4,1,1,1,1,1,
1,4),(141.371669411541,141.985445243067,142.983036940947,143.980628638827,
144.978220336707,145.975812034587,146.973403732467,147.65485471872),
 .UNSPECIFIED.);
#268=B_SPLINE_CURVE_WITH_KNOTS('',3,(#11107,#11108,#11109,#11110,#11111,
#11112,#11113,#11114,#11115,#11116,#11117),.UNSPECIFIED.,.F.,.F.,(4,1,1,
1,1,1,1,1,4),(135.088484104361,135.271881000752,136.269102676586,137.26632435242,
138.263546028254,139.260767704088,140.257989379922,141.255211055756,141.371669411541),
 .UNSPECIFIED.);
#269=B_SPLINE_CURVE_WITH_KNOTS('',3,(#11118,#11119,#11120,#11121,#11122,
#11123,#11124,#11125,#11126,#11127),.UNSPECIFIED.,.F.,.F.,(4,1,1,1,1,1,
1,4),(135.088484104361,135.999895055788,136.997486753668,137.995078451548,
138.992670149428,139.990261847308,140.987853545188,141.371669411541),
 .UNSPECIFIED.);
#270=B_SPLINE_CURVE_WITH_KNOTS('',3,(#11132,#11133,#11134,#11135,#11136,
#11137,#11138,#11139,#11140,#11141),.UNSPECIFIED.,.F.,.F.,(4,1,1,1,1,1,
1,4),(128.805298797182,129.288550945748,130.285772621582,131.282994297416,
132.28021597325,133.277437649084,134.274659324918,135.088484104361),
 .UNSPECIFIED.);
#271=B_SPLINE_CURVE_WITH_KNOTS('',3,(#11142,#11143,#11144,#11145,#11146,
#11147,#11148,#11149,#11150,#11151,#11152),.UNSPECIFIED.,.F.,.F.,(4,1,1,
1,1,1,1,1,4),(128.805298797182,129.016753170629,130.014344868509,131.011936566389,
132.009528264269,133.007119962148,134.004711660028,135.002303357908,135.088484104361),
 .UNSPECIFIED.);
#272=B_SPLINE_CURVE_WITH_KNOTS('',3,(#11157,#11158,#11159,#11160,#11161,
#11162,#11163,#11164,#11165,#11166),.UNSPECIFIED.,.F.,.F.,(4,1,1,1,1,1,
1,4),(122.522113490002,123.305220890745,124.302442566579,125.299664242413,
126.296885918246,127.29410759408,128.291329269914,128.805298797182),
 .UNSPECIFIED.);
#273=B_SPLINE_CURVE_WITH_KNOTS('',3,(#11167,#11168,#11169,#11170,#11171,
#11172,#11173,#11174,#11175,#11176),.UNSPECIFIED.,.F.,.F.,(4,1,1,1,1,1,
1,4),(122.522113490002,123.03120298335,124.028794681229,125.026386379109,
126.023978076989,127.021569774869,128.019161472749,128.805298797182),
 .UNSPECIFIED.);
#274=B_SPLINE_CURVE_WITH_KNOTS('',3,(#11181,#11182,#11183,#11184,#11185,
#11186,#11187,#11188,#11189,#11190,#11191),.UNSPECIFIED.,.F.,.F.,(4,1,1,
1,1,1,1,1,4),(116.238928182823,116.324669159907,117.321890835741,118.319112511575,
119.316334187409,120.313555863243,121.310777539077,122.307999214911,122.522113490002),
 .UNSPECIFIED.);
#275=B_SPLINE_CURVE_WITH_KNOTS('',3,(#11192,#11193,#11194,#11195,#11196,
#11197,#11198,#11199,#11200,#11201),.UNSPECIFIED.,.F.,.F.,(4,1,1,1,1,1,
1,4),(116.238928182823,117.04565279607,118.04324449395,119.04083619183,
120.03842788971,121.03601958759,122.03361128547,122.522113490002),
 .UNSPECIFIED.);
#276=B_SPLINE_CURVE_WITH_KNOTS('',3,(#11206,#11207,#11208,#11209,#11210,
#11211,#11212,#11213,#11214,#11215),.UNSPECIFIED.,.F.,.F.,(4,1,1,1,1,1,
1,4),(109.955742875643,110.341339104903,111.338560780737,112.335782456571,
113.333004132405,114.330225808239,115.327447484073,116.238928182823),
 .UNSPECIFIED.);
#277=B_SPLINE_CURVE_WITH_KNOTS('',3,(#11216,#11217,#11218,#11219,#11220,
#11221,#11222,#11223,#11224,#11225,#11226),.UNSPECIFIED.,.F.,.F.,(4,1,1,
1,1,1,1,1,4),(109.955742875643,110.062510910911,111.060102608791,112.057694306671,
113.055286004551,114.052877702431,115.050469400311,116.04806109819,116.238928182823),
 .UNSPECIFIED.);
#278=B_SPLINE_CURVE_WITH_KNOTS('',3,(#11231,#11232,#11233,#11234,#11235,
#11236,#11237,#11238,#11239,#11240),.UNSPECIFIED.,.F.,.F.,(4,1,1,1,1,1,
1,4),(103.672557568463,104.358009049899,105.355230725733,106.352452401567,
107.349674077401,108.346895753235,109.344117429069,109.955742875643),
 .UNSPECIFIED.);
#279=B_SPLINE_CURVE_WITH_KNOTS('',3,(#11241,#11242,#11243,#11244,#11245,
#11246,#11247,#11248,#11249,#11250),.UNSPECIFIED.,.F.,.F.,(4,1,1,1,1,1,
1,4),(103.672557568463,104.076960723632,105.074552421512,106.072144119392,
107.069735817271,108.067327515151,109.064919213031,109.955742875643),
 .UNSPECIFIED.);
#280=B_SPLINE_CURVE_WITH_KNOTS('',3,(#11255,#11256,#11257,#11258,#11259,
#11260,#11261,#11262,#11263,#11264),.UNSPECIFIED.,.F.,.F.,(4,1,1,1,1,1,
1,4),(97.3893722612838,98.3746789948957,99.3719006707297,100.369122346564,
101.366344022398,102.363565698232,103.360787374066,103.672557568463),
 .UNSPECIFIED.);
#281=B_SPLINE_CURVE_WITH_KNOTS('',3,(#11265,#11266,#11267,#11268,#11269,
#11270,#11271,#11272,#11273,#11274),.UNSPECIFIED.,.F.,.F.,(4,1,1,1,1,1,
1,4),(97.3893722612838,98.0914105363525,99.0890022342324,100.086593932112,
101.084185629992,102.081777327872,103.079369025752,103.672557568463),
 .UNSPECIFIED.);
#282=B_SPLINE_CURVE_WITH_KNOTS('',3,(#11279,#11280,#11281,#11282,#11283,
#11284,#11285,#11286,#11287,#11288,#11289),.UNSPECIFIED.,.F.,.F.,(4,1,1,
1,1,1,1,1,4),(91.1061869541042,91.3941272640581,92.391348939892,93.388570615726,
94.3857922915599,95.3830139673939,96.3802356432278,97.3774573190618,97.3893722612838),
 .UNSPECIFIED.);
#283=B_SPLINE_CURVE_WITH_KNOTS('',3,(#11290,#11291,#11292,#11293,#11294,
#11295,#11296,#11297,#11298,#11299,#11300),.UNSPECIFIED.,.F.,.F.,(4,1,1,
1,1,1,1,1,4),(91.1061869541042,91.1082686511933,92.1058603490732,93.103452046953,
94.1010437448329,95.0986354427128,96.0962271405927,97.0938188384726,97.3893722612838),
 .UNSPECIFIED.);
#284=B_SPLINE_CURVE_WITH_KNOTS('',3,(#11305,#11306,#11307,#11308,#11309,
#11310,#11311,#11312,#11313,#11314),.UNSPECIFIED.,.F.,.F.,(4,1,1,1,1,1,
1,4),(84.8230016469246,85.4107972090543,86.4080188848883,87.4052405607222,
88.4024622365562,89.3996839123901,90.3969055882241,91.1061869541042),
 .UNSPECIFIED.);
#285=B_SPLINE_CURVE_WITH_KNOTS('',3,(#11315,#11316,#11317,#11318,#11319,
#11320,#11321,#11322,#11323,#11324),.UNSPECIFIED.,.F.,.F.,(4,1,1,1,1,1,
1,4),(84.8230016469246,85.122718463914,86.1203101617938,87.1179018596737,
88.1154935575536,89.1130852554335,90.1106769533134,91.1061869541042),
 .UNSPECIFIED.);
#286=B_SPLINE_CURVE_WITH_KNOTS('',3,(#11329,#11330,#11331,#11332,#11333,
#11334,#11335,#11336,#11337,#11338),.UNSPECIFIED.,.F.,.F.,(4,1,1,1,1,1,
1,4),(78.539816339745,79.4274671540506,80.4246888298845,81.4219105057185,
82.4191321815525,83.4163538573864,84.4135755332204,84.8230016469246),
 .UNSPECIFIED.);
#287=B_SPLINE_CURVE_WITH_KNOTS('',3,(#11339,#11340,#11341,#11342,#11343,
#11344,#11345,#11346,#11347,#11348),.UNSPECIFIED.,.F.,.F.,(4,1,1,1,1,1,
1,4),(78.539816339745,79.1371682766347,80.1347599745145,81.1323516723944,
82.1299433702743,83.1275350681542,84.1251267660341,84.8230016469246),
 .UNSPECIFIED.);
#288=B_SPLINE_CURVE_WITH_KNOTS('',3,(#11353,#11354,#11355,#11356,#11357,
#11358,#11359,#11360,#11361,#11362,#11363),.UNSPECIFIED.,.F.,.F.,(4,1,1,
1,1,1,1,1,4),(72.2566310325654,72.4469154232129,73.4441370990469,74.4413587748808,
75.4385804507148,76.4358021265487,77.4330238023827,78.4302454782166,78.539816339745),
 .UNSPECIFIED.);
#289=B_SPLINE_CURVE_WITH_KNOTS('',3,(#11364,#11365,#11366,#11367,#11368,
#11369,#11370,#11371,#11372,#11373),.UNSPECIFIED.,.F.,.F.,(4,1,1,1,1,1,
1,4),(72.2566310325654,73.1516180893553,74.1492097872352,75.1468014851151,
76.144393182995,77.1419848808749,78.1395765787548,78.539816339745),
 .UNSPECIFIED.);
#290=B_SPLINE_CURVE_WITH_KNOTS('',3,(#11378,#11379,#11380,#11381,#11382,
#11383,#11384,#11385,#11386,#11387),.UNSPECIFIED.,.F.,.F.,(4,1,1,1,1,1,
1,4),(65.9734457253858,66.4635853682092,67.4608070440431,68.4580287198771,
69.455250395711,70.452472071545,71.4496937473789,72.2566310325654),
 .UNSPECIFIED.);
#291=B_SPLINE_CURVE_WITH_KNOTS('',3,(#11388,#11389,#11390,#11391,#11392,
#11393,#11394,#11395,#11396,#11397,#11398),.UNSPECIFIED.,.F.,.F.,(4,1,1,
1,1,1,1,1,4),(65.9734457253858,66.1684762041961,67.166067902076,68.1636595999559,
69.1612512978358,70.1588429957157,71.1564346935956,72.1540263914755,72.2566310325654),
 .UNSPECIFIED.);
#292=B_SPLINE_CURVE_WITH_KNOTS('',3,(#11403,#11404,#11405,#11406,#11407,
#11408,#11409,#11410,#11411,#11412),.UNSPECIFIED.,.F.,.F.,(4,1,1,1,1,1,
1,4),(59.6902604182062,60.4802553132055,61.4774769890394,62.4746986648734,
63.4719203407073,64.4691420165413,65.4663636923752,65.9734457253858),
 .UNSPECIFIED.);
#293=B_SPLINE_CURVE_WITH_KNOTS('',3,(#11413,#11414,#11415,#11416,#11417,
#11418,#11419,#11420,#11421,#11422),.UNSPECIFIED.,.F.,.F.,(4,1,1,1,1,1,
1,4),(59.6902604182062,60.1829260169168,61.1805177147967,62.1781094126766,
63.1757011105565,64.1732928084364,65.1708845063163,65.9734457253858),
 .UNSPECIFIED.);
#294=B_SPLINE_CURVE_WITH_KNOTS('',3,(#11427,#11428,#11429,#11430,#11431,
#11432,#11433,#11434,#11435,#11436,#11437),.UNSPECIFIED.,.F.,.F.,(4,1,1,
1,1,1,1,1,4),(53.4070751110266,53.4997035823678,54.4969252582017,55.4941469340357,
56.4913686098696,57.4885902857036,58.4858119615375,59.4830336373715,59.6902604182062),
 .UNSPECIFIED.);
#295=B_SPLINE_CURVE_WITH_KNOTS('',3,(#11438,#11439,#11440,#11441,#11442,
#11443,#11444,#11445,#11446,#11447),.UNSPECIFIED.,.F.,.F.,(4,1,1,1,1,1,
1,4),(53.4070751110266,54.1973758296375,55.1949675275174,56.1925592253973,
57.1901509232772,58.1877426211571,59.1853343190369,59.6902604182062),
 .UNSPECIFIED.);
#296=B_SPLINE_CURVE_WITH_KNOTS('',3,(#11452,#11453,#11454,#11455,#11456,
#11457,#11458,#11459,#11460,#11461),.UNSPECIFIED.,.F.,.F.,(4,1,1,1,1,1,
1,4),(47.123889803847,47.516373527364,48.513595203198,49.5108168790319,
50.5080385548659,51.5052602306999,52.5024819065338,53.4070751110266),
 .UNSPECIFIED.);
#297=B_SPLINE_CURVE_WITH_KNOTS('',3,(#11462,#11463,#11464,#11465,#11466,
#11467,#11468,#11469,#11470,#11471,#11472),.UNSPECIFIED.,.F.,.F.,(4,1,1,
1,1,1,1,1,4),(47.123889803847,47.2142339444783,48.2118256423582,49.2094173402381,
50.207009038118,51.2046007359979,52.2021924338777,53.1997841317576,53.4070751110266),
 .UNSPECIFIED.);
#298=B_SPLINE_CURVE_WITH_KNOTS('',3,(#11477,#11478,#11479,#11480,#11481,
#11482,#11483,#11484,#11485,#11486),.UNSPECIFIED.,.F.,.F.,(4,1,1,1,1,1,
1,4),(40.8407044966674,41.5330434723603,42.5302651481943,43.5274868240282,
44.5247084998622,45.5219301756961,46.5191518515301,47.123889803847),
 .UNSPECIFIED.);
#299=B_SPLINE_CURVE_WITH_KNOTS('',3,(#11487,#11488,#11489,#11490,#11491,
#11492,#11493,#11494,#11495,#11496),.UNSPECIFIED.,.F.,.F.,(4,1,1,1,1,1,
1,4),(40.8407044966675,41.228683757199,42.2262754550789,43.2238671529588,
44.2214588508387,45.2190505487186,46.2166422465984,47.123889803847),
 .UNSPECIFIED.);
#300=B_SPLINE_CURVE_WITH_KNOTS('',3,(#11501,#11502,#11503,#11504,#11505,
#11506,#11507,#11508,#11509,#11510),.UNSPECIFIED.,.F.,.F.,(4,1,1,1,1,1,
1,4),(34.5575191894878,35.5497134173566,36.5469350931905,37.5441567690245,
38.5413784448584,39.5386001206924,40.5358217965264,40.8407044966674),
 .UNSPECIFIED.);
#301=B_SPLINE_CURVE_WITH_KNOTS('',3,(#11511,#11512,#11513,#11514,#11515,
#11516,#11517,#11518,#11519,#11520),.UNSPECIFIED.,.F.,.F.,(4,1,1,1,1,1,
1,4),(34.5575191894879,35.2431335699197,36.2407252677996,37.2383169656795,
38.2359086635594,39.2335003614392,40.2310920593191,40.8407044966675),
 .UNSPECIFIED.);
#302=B_SPLINE_CURVE_WITH_KNOTS('',3,(#11525,#11526,#11527,#11528,#11529,
#11530,#11531,#11532,#11533,#11534,#11535),.UNSPECIFIED.,.F.,.F.,(4,1,1,
1,1,1,1,1,4),(28.2743338823083,28.5691616865189,29.5663833623529,30.5636050381868,
31.5608267140208,32.5580483898547,33.5552700656887,34.5524917415226,34.5575191894878),
 .UNSPECIFIED.);
#303=B_SPLINE_CURVE_WITH_KNOTS('',3,(#11536,#11537,#11538,#11539,#11540,
#11541,#11542,#11543,#11544,#11545),.UNSPECIFIED.,.F.,.F.,(4,1,1,1,1,1,
1,4),(28.2743338823083,29.2575833826404,30.2551750805203,31.2527667784002,
32.2503584762801,33.2479501741599,34.2455418720398,34.5575191894879),
 .UNSPECIFIED.);
#304=B_SPLINE_CURVE_WITH_KNOTS('',3,(#11550,#11551,#11552,#11553,#11554,
#11555,#11556,#11557,#11558,#11559),.UNSPECIFIED.,.F.,.F.,(4,1,1,1,1,1,
1,4),(21.9911485751287,22.5858316315152,23.5830533073491,24.5802749831831,
25.577496659017,26.574718334851,27.5719400106849,28.2743338823083),
 .UNSPECIFIED.);
#305=B_SPLINE_CURVE_WITH_KNOTS('',3,(#11560,#11561,#11562,#11563,#11564,
#11565,#11566,#11567,#11568,#11569,#11570),.UNSPECIFIED.,.F.,.F.,(4,1,1,
1,1,1,1,1,4),(21.9911485751287,22.2744414974812,23.2720331953611,24.269624893241,
25.2672165911209,26.2648082890007,27.2623999868806,28.2599916847605,28.2743338823083),
 .UNSPECIFIED.);
#306=B_SPLINE_CURVE_WITH_KNOTS('',3,(#11575,#11576,#11577,#11578,#11579,
#11580,#11581,#11582,#11583,#11584),.UNSPECIFIED.,.F.,.F.,(4,1,1,1,1,1,
1,4),(15.7079632679491,16.6025015765114,17.5997232523454,18.5969449281793,
19.5941666040133,20.5913882798473,21.5886099556812,21.9911485751287),
 .UNSPECIFIED.);
#307=B_SPLINE_CURVE_WITH_KNOTS('',3,(#11585,#11586,#11587,#11588,#11589,
#11590,#11591,#11592,#11593,#11594),.UNSPECIFIED.,.F.,.F.,(4,1,1,1,1,1,
1,4),(15.7079632679491,16.2888913102019,17.2864830080818,18.2840747059617,
19.2816664038415,20.2792581017214,21.2768497996013,21.9911485751287),
 .UNSPECIFIED.);
#308=B_SPLINE_CURVE_WITH_KNOTS('',3,(#11597,#11598,#11599,#11600,#11601,
#11602,#11603,#11604,#11605,#11606,#11607,#11608,#11609,#11610,#11611,#11612,
#11613,#11614,#11615,#11616,#11617,#11618,#11619,#11620,#11621,#11622,#11623,
#11624,#11625,#11626,#11627,#11628,#11629,#11630,#11631,#11632,#11633,#11634,
#11635,#11636,#11637,#11638,#11639,#11640,#11641,#11642,#11643,#11644,#11645,
#11646,#11647,#11648,#11649,#11650,#11651,#11652,#11653,#11654,#11655,#11656,
#11657,#11658,#11659,#11660,#11661,#11662,#11663,#11664,#11665,#11666,#11667,
#11668,#11669,#11670,#11671,#11672,#11673,#11674,#11675,#11676,#11677,#11678,
#11679,#11680,#11681,#11682,#11683,#11684,#11685,#11686,#11687,#11688,#11689,
#11690,#11691,#11692,#11693,#11694,#11695,#11696,#11697,#11698,#11699,#11700,
#11701,#11702,#11703,#11704,#11705,#11706,#11707,#11708,#11709,#11710,#11711,
#11712,#11713,#11714,#11715,#11716,#11717,#11718,#11719,#11720,#11721,#11722,
#11723,#11724,#11725,#11726,#11727,#11728,#11729,#11730,#11731,#11732,#11733,
#11734,#11735,#11736,#11737,#11738,#11739,#11740,#11741,#11742,#11743,#11744,
#11745,#11746,#11747,#11748,#11749,#11750,#11751,#11752,#11753,#11754,#11755,
#11756,#11757,#11758,#11759,#11760,#11761,#11762,#11763,#11764,#11765,#11766,
#11767,#11768,#11769,#11770,#11771,#11772,#11773,#11774,#11775,#11776,#11777,
#11778,#11779,#11780,#11781,#11782,#11783,#11784,#11785,#11786,#11787,#11788,
#11789,#11790,#11791,#11792,#11793,#11794,#11795,#11796,#11797,#11798,#11799,
#11800,#11801,#11802,#11803,#11804,#11805,#11806,#11807,#11808,#11809,#11810),
 .UNSPECIFIED.,.F.,.F.,(4,3,3,3,3,3,3,3,3,3,3,3,3,3,3,3,3,3,3,3,3,3,3,3,
3,3,3,3,3,3,3,3,3,3,3,3,3,3,3,3,3,3,3,3,3,3,3,3,3,3,3,3,3,3,3,3,3,3,3,3,
3,3,3,3,3,3,3,3,3,3,3,4),(-1.26297767193527,-1.24123059946692,-1.21837400953358,
-1.20789928299389,-1.20383483749142,-1.19947717281857,-1.17668714612644,
-1.15373012448748,-1.14469158562245,-1.14082677203282,-1.11762638295685,
-1.0945612252029,-1.07646955260153,-1.0672475154899,-1.06334380101767,-1.05931873640602,
-1.05837788000017,-1.0361298744797,-1.01232110135027,-0.991488424862023,
-0.984594580015151,-0.980621471139353,-0.957200760573628,-0.933467886974511,
-0.91151583759195,-0.903275712213173,-0.898529224186148,-0.895168469288221,
-0.870414079366242,-0.845659689444264,-0.822099707362731,-0.813927294570445,
-0.810210042103504,-0.786549160472357,-0.762432595442628,-0.738225084576931,
-0.729837012816269,-0.725138584726005,-0.700132102528345,-0.675759915730524,
-0.651798333821953,-0.643457982208621,-0.638375085891089,-0.625112655935365,
-0.601401003403345,-0.575798341779257,-0.564089465748533,-0.554431081554694,
-0.550487592904426,-0.525821248520384,-0.500828064063021,-0.474765975649928,
-0.466687959682199,-0.461195933574007,-0.435964800569675,-0.411153539634739,
-0.396579710410647,-0.382859058578158,-0.374421643509067,-0.370946667145629,
-0.346187746128783,-0.320896710423911,-0.29540724904293,-0.285987248141239,
-0.282041885516286,-0.278125401225697,-0.252392678017214,-0.226697892801638,
-0.201873586946231,-0.191255176409111,-0.186426923186837,-0.177049281090825),
 .UNSPECIFIED.);
#309=B_SPLINE_CURVE_WITH_KNOTS('',3,(#11812,#11813,#11814,#11815,#11816,
#11817,#11818,#11819,#11820,#11821,#11822,#11823,#11824,#11825,#11826,#11827,
#11828,#11829,#11830,#11831,#11832,#11833,#11834,#11835,#11836,#11837,#11838,
#11839,#11840,#11841,#11842,#11843,#11844,#11845,#11846,#11847,#11848,#11849,
#11850,#11851,#11852,#11853,#11854,#11855,#11856,#11857,#11858,#11859,#11860,
#11861,#11862,#11863,#11864,#11865,#11866,#11867,#11868,#11869,#11870,#11871,
#11872),.UNSPECIFIED.,.F.,.F.,(4,3,3,3,3,3,3,3,3,3,3,3,3,3,3,3,3,3,3,3,
4),(-0.342658399319032,-0.317027048600994,-0.292003556185365,-0.273617043455568,
-0.259827158908221,-0.255639923465139,-0.231507037422574,-0.218457505266178,
-0.193758751297552,-0.169538907385358,-0.165763510415239,-0.141949579421655,
-0.118190761275412,-0.0948421346464585,-0.0878872820010161,-0.0819188450624042,
-0.0782990769851931,-0.055689554830121,-0.0334445595930238,-0.0118635944753777,
0.),.UNSPECIFIED.);
#310=B_SPLINE_CURVE_WITH_KNOTS('',3,(#11875,#11876,#11877,#11878,#11879,
#11880,#11881,#11882,#11883,#11884,#11885,#11886,#11887,#11888,#11889,#11890,
#11891,#11892,#11893,#11894,#11895,#11896,#11897,#11898,#11899,#11900,#11901,
#11902),.UNSPECIFIED.,.F.,.F.,(4,3,3,3,3,3,3,3,3,4),(-0.177049281090825,
-0.160264958626335,-0.134994935614823,-0.109227006060211,-0.0991214343897917,
-0.0948694657952354,-0.0690591354441416,-0.0428842165991826,-0.0167516322510638,
0.),.UNSPECIFIED.);
#311=B_SPLINE_CURVE_WITH_KNOTS('',3,(#12691,#12692,#12693,#12694,#12695,
#12696,#12697,#12698),.UNSPECIFIED.,.F.,.F.,(4,1,1,1,1,4),(11.6163931973417,
12.6136148731756,13.6108365490096,14.6080582248435,15.6052799006775,15.7079632679491),
 .UNSPECIFIED.);
#312=B_SPLINE_CURVE_WITH_KNOTS('',3,(#12699,#12700,#12701,#12702,#12703,
#12704,#12705,#12706,#12707,#12708,#12709,#12710,#12711,#12712,#12713,#12714,
#12715,#12716,#12717,#12718,#12719,#12720,#12721,#12722,#12723,#12724,#12725,
#12726,#12727,#12728,#12729,#12730,#12731,#12732,#12733,#12734,#12735,#12736,
#12737,#12738,#12739,#12740,#12741,#12742,#12743,#12744,#12745,#12746,#12747,
#12748,#12749,#12750,#12751,#12752,#12753,#12754,#12755,#12756,#12757,#12758,
#12759,#12760,#12761,#12762,#12763,#12764,#12765,#12766,#12767,#12768,#12769,
#12770,#12771,#12772,#12773,#12774,#12775,#12776,#12777,#12778,#12779,#12780,
#12781,#12782,#12783,#12784,#12785,#12786),.UNSPECIFIED.,.F.,.F.,(4,3,3,
3,3,3,3,3,3,3,3,3,3,3,3,3,3,3,3,3,3,3,3,3,3,3,3,3,3,4),(-0.461788964899783,
-0.444143511940815,-0.418515798790508,-0.405575675714164,-0.399737745646638,
-0.394846562641521,-0.369463325133089,-0.349714638187578,-0.340575547651319,
-0.336040482540573,-0.331740177580549,-0.306977516058662,-0.282755448184146,
-0.259069445882197,-0.248566190347295,-0.244441238407051,-0.220951758169334,
-0.211473829568997,-0.187512614410561,-0.164073537609241,-0.158786243270235,
-0.135430453104867,-0.112092295537671,-0.0891436133842281,-0.0803317101641952,
-0.0766176166068317,-0.0541543545622248,-0.0320549846333942,-0.0106630888452865,
0.),.UNSPECIFIED.);
#313=B_SPLINE_CURVE_WITH_KNOTS('',3,(#12787,#12788,#12789,#12790,#12791,
#12792,#12793,#12794,#12795,#12796,#12797,#12798,#12799,#12800,#12801,#12802,
#12803,#12804,#12805),.UNSPECIFIED.,.F.,.F.,(4,3,3,3,3,3,4),(-190.950928956894,
-190.469340084285,-189.472118408451,-188.474896732617,-187.477675056784,
-186.48045338095,-186.303943978815),.UNSPECIFIED.);
#314=B_SPLINE_CURVE_WITH_KNOTS('',3,(#12808,#12809,#12810,#12811,#12812,
#12813,#12814,#12815,#12816),.UNSPECIFIED.,.F.,.F.,(4,1,1,1,1,1,4),(10.3747553777872,
11.3009328208025,12.2985245186824,13.2961162165622,14.2937079144421,15.291299612322,
15.7079632679491),.UNSPECIFIED.);
#315=B_SPLINE_CURVE_WITH_KNOTS('',3,(#13610,#13611,#13612,#13613,#13614,
#13615,#13616,#13617,#13618,#13619,#13620,#13621,#13622,#13623,#13624,#13625,
#13626,#13627,#13628,#13629,#13630,#13631),.UNSPECIFIED.,.F.,.F.,(4,3,3,
3,3,3,3,4),(183.328994141815,183.556872409899,184.554464107779,185.552055805659,
186.549647503538,187.547239201418,188.544830899298,188.88433130627),
 .UNSPECIFIED.);
#316=B_SPLINE_CURVE_WITH_KNOTS('',3,(#13632,#13633,#13634,#13635,#13636,
#13637,#13638,#13639,#13640,#13641,#13642,#13643,#13644,#13645,#13646,#13647,
#13648,#13649,#13650,#13651,#13652,#13653,#13654,#13655,#13656,#13657,#13658,
#13659,#13660,#13661,#13662,#13663,#13664,#13665,#13666,#13667,#13668,#13669,
#13670,#13671,#13672,#13673,#13674,#13675,#13676,#13677,#13678,#13679,#13680,
#13681,#13682,#13683,#13684,#13685,#13686,#13687,#13688,#13689,#13690,#13691,
#13692,#13693,#13694,#13695,#13696,#13697,#13698,#13699,#13700,#13701,#13702,
#13703,#13704,#13705,#13706,#13707,#13708,#13709,#13710,#13711,#13712,#13713,
#13714,#13715,#13716),.UNSPECIFIED.,.F.,.F.,(4,3,3,3,3,3,3,3,3,3,3,3,3,
3,3,3,3,3,3,3,3,3,3,3,3,3,3,3,4),(-0.463803050843705,-0.449347192429686,
-0.427640368714011,-0.415624313505051,-0.410511273392428,-0.406061884229529,
-0.383387971324397,-0.36490408347224,-0.357542028506273,-0.352425153391359,
-0.329101137101116,-0.305332602380306,-0.287878668912014,-0.274788218810795,
-0.271229860207255,-0.246801643139605,-0.235516868507138,-0.211931397815532,
-0.187854419898393,-0.183811601979953,-0.1594364627127,-0.134555356368287,
-0.109447034007667,-0.0941298055661022,-0.0900026856982938,-0.0642548943642791,
-0.0384793716268655,-0.0132580795069667,0.),.UNSPECIFIED.);
#321=SHAPE_REPRESENTATION_RELATIONSHIP('SRR','None',#13839,#327);
#327=ADVANCED_BREP_SHAPE_REPRESENTATION('',(#339),#13799);
#333=STYLED_ITEM('',(#13882),#339);
#339=MANIFOLD_SOLID_BREP('Body1',#3698);
#363=FACE_BOUND('',#835,.T.);
#364=FACE_BOUND('',#838,.T.);
#405=PLANE('',#4010);
#406=PLANE('',#4011);
#407=PLANE('',#4012);
#408=PLANE('',#4013);
#409=PLANE('',#4014);
#410=PLANE('',#4015);
#411=PLANE('',#4016);
#412=PLANE('',#4017);
#413=PLANE('',#4021);
#414=PLANE('',#4022);
#539=FACE_OUTER_BOUND('',#762,.T.);
#540=FACE_OUTER_BOUND('',#763,.T.);
#541=FACE_OUTER_BOUND('',#764,.T.);
#542=FACE_OUTER_BOUND('',#765,.T.);
#543=FACE_OUTER_BOUND('',#766,.T.);
#544=FACE_OUTER_BOUND('',#767,.T.);
#545=FACE_OUTER_BOUND('',#768,.T.);
#546=FACE_OUTER_BOUND('',#769,.T.);
#547=FACE_OUTER_BOUND('',#770,.T.);
#548=FACE_OUTER_BOUND('',#771,.T.);
#549=FACE_OUTER_BOUND('',#772,.T.);
#550=FACE_OUTER_BOUND('',#773,.T.);
#551=FACE_OUTER_BOUND('',#774,.T.);
#552=FACE_OUTER_BOUND('',#775,.T.);
#553=FACE_OUTER_BOUND('',#776,.T.);
#554=FACE_OUTER_BOUND('',#777,.T.);
#555=FACE_OUTER_BOUND('',#778,.T.);
#556=FACE_OUTER_BOUND('',#779,.T.);
#557=FACE_OUTER_BOUND('',#780,.T.);
#558=FACE_OUTER_BOUND('',#781,.T.);
#559=FACE_OUTER_BOUND('',#782,.T.);
#560=FACE_OUTER_BOUND('',#783,.T.);
#561=FACE_OUTER_BOUND('',#784,.T.);
#562=FACE_OUTER_BOUND('',#785,.T.);
#563=FACE_OUTER_BOUND('',#786,.T.);
#564=FACE_OUTER_BOUND('',#787,.T.);
#565=FACE_OUTER_BOUND('',#788,.T.);
#566=FACE_OUTER_BOUND('',#789,.T.);
#567=FACE_OUTER_BOUND('',#790,.T.);
#568=FACE_OUTER_BOUND('',#791,.T.);
#569=FACE_OUTER_BOUND('',#792,.T.);
#570=FACE_OUTER_BOUND('',#793,.T.);
#571=FACE_OUTER_BOUND('',#794,.T.);
#572=FACE_OUTER_BOUND('',#795,.T.);
#573=FACE_OUTER_BOUND('',#796,.T.);
#574=FACE_OUTER_BOUND('',#797,.T.);
#575=FACE_OUTER_BOUND('',#798,.T.);
#576=FACE_OUTER_BOUND('',#799,.T.);
#577=FACE_OUTER_BOUND('',#800,.T.);
#578=FACE_OUTER_BOUND('',#801,.T.);
#579=FACE_OUTER_BOUND('',#802,.T.);
#580=FACE_OUTER_BOUND('',#803,.T.);
#581=FACE_OUTER_BOUND('',#804,.T.);
#582=FACE_OUTER_BOUND('',#805,.T.);
#583=FACE_OUTER_BOUND('',#806,.T.);
#584=FACE_OUTER_BOUND('',#807,.T.);
#585=FACE_OUTER_BOUND('',#808,.T.);
#586=FACE_OUTER_BOUND('',#809,.T.);
#587=FACE_OUTER_BOUND('',#810,.T.);
#588=FACE_OUTER_BOUND('',#811,.T.);
#589=FACE_OUTER_BOUND('',#812,.T.);
#590=FACE_OUTER_BOUND('',#813,.T.);
#591=FACE_OUTER_BOUND('',#814,.T.);
#592=FACE_OUTER_BOUND('',#815,.T.);
#593=FACE_OUTER_BOUND('',#816,.T.);
#594=FACE_OUTER_BOUND('',#817,.T.);
#595=FACE_OUTER_BOUND('',#818,.T.);
#596=FACE_OUTER_BOUND('',#819,.T.);
#597=FACE_OUTER_BOUND('',#820,.T.);
#598=FACE_OUTER_BOUND('',#821,.T.);
#599=FACE_OUTER_BOUND('',#822,.T.);
#600=FACE_OUTER_BOUND('',#823,.T.);
#601=FACE_OUTER_BOUND('',#824,.T.);
#602=FACE_OUTER_BOUND('',#825,.T.);
#603=FACE_OUTER_BOUND('',#826,.T.);
#604=FACE_OUTER_BOUND('',#827,.T.);
#605=FACE_OUTER_BOUND('',#828,.T.);
#606=FACE_OUTER_BOUND('',#829,.T.);
#607=FACE_OUTER_BOUND('',#830,.T.);
#608=FACE_OUTER_BOUND('',#831,.T.);
#609=FACE_OUTER_BOUND('',#832,.T.);
#610=FACE_OUTER_BOUND('',#833,.T.);
#611=FACE_OUTER_BOUND('',#834,.T.);
#612=FACE_OUTER_BOUND('',#836,.T.);
#613=FACE_OUTER_BOUND('',#837,.T.);
#614=FACE_OUTER_BOUND('',#839,.T.);
#762=EDGE_LOOP('',(#2913,#2914,#2915,#2916));
#763=EDGE_LOOP('',(#2917,#2918,#2919,#2920));
#764=EDGE_LOOP('',(#2921,#2922,#2923,#2924));
#765=EDGE_LOOP('',(#2925,#2926,#2927,#2928));
#766=EDGE_LOOP('',(#2929,#2930,#2931,#2932));
#767=EDGE_LOOP('',(#2933,#2934,#2935,#2936));
#768=EDGE_LOOP('',(#2937,#2938,#2939,#2940));
#769=EDGE_LOOP('',(#2941,#2942,#2943,#2944));
#770=EDGE_LOOP('',(#2945,#2946,#2947,#2948));
#771=EDGE_LOOP('',(#2949,#2950,#2951,#2952));
#772=EDGE_LOOP('',(#2953,#2954,#2955,#2956));
#773=EDGE_LOOP('',(#2957,#2958,#2959,#2960));
#774=EDGE_LOOP('',(#2961,#2962,#2963,#2964));
#775=EDGE_LOOP('',(#2965,#2966,#2967,#2968));
#776=EDGE_LOOP('',(#2969,#2970,#2971,#2972));
#777=EDGE_LOOP('',(#2973,#2974,#2975,#2976));
#778=EDGE_LOOP('',(#2977,#2978,#2979,#2980));
#779=EDGE_LOOP('',(#2981,#2982,#2983,#2984));
#780=EDGE_LOOP('',(#2985,#2986,#2987,#2988));
#781=EDGE_LOOP('',(#2989,#2990,#2991,#2992));
#782=EDGE_LOOP('',(#2993,#2994,#2995,#2996));
#783=EDGE_LOOP('',(#2997,#2998,#2999,#3000));
#784=EDGE_LOOP('',(#3001,#3002,#3003,#3004));
#785=EDGE_LOOP('',(#3005,#3006,#3007,#3008));
#786=EDGE_LOOP('',(#3009,#3010,#3011,#3012));
#787=EDGE_LOOP('',(#3013,#3014,#3015,#3016));
#788=EDGE_LOOP('',(#3017,#3018,#3019,#3020));
#789=EDGE_LOOP('',(#3021,#3022,#3023,#3024));
#790=EDGE_LOOP('',(#3025,#3026,#3027,#3028));
#791=EDGE_LOOP('',(#3029,#3030,#3031,#3032));
#792=EDGE_LOOP('',(#3033,#3034,#3035,#3036));
#793=EDGE_LOOP('',(#3037,#3038,#3039,#3040));
#794=EDGE_LOOP('',(#3041,#3042,#3043,#3044));
#795=EDGE_LOOP('',(#3045,#3046,#3047,#3048));
#796=EDGE_LOOP('',(#3049,#3050,#3051,#3052));
#797=EDGE_LOOP('',(#3053,#3054,#3055,#3056));
#798=EDGE_LOOP('',(#3057,#3058,#3059,#3060));
#799=EDGE_LOOP('',(#3061,#3062,#3063,#3064));
#800=EDGE_LOOP('',(#3065,#3066,#3067,#3068));
#801=EDGE_LOOP('',(#3069,#3070,#3071,#3072));
#802=EDGE_LOOP('',(#3073,#3074,#3075,#3076));
#803=EDGE_LOOP('',(#3077,#3078,#3079,#3080));
#804=EDGE_LOOP('',(#3081,#3082,#3083,#3084));
#805=EDGE_LOOP('',(#3085,#3086,#3087,#3088));
#806=EDGE_LOOP('',(#3089,#3090,#3091,#3092));
#807=EDGE_LOOP('',(#3093,#3094,#3095,#3096));
#808=EDGE_LOOP('',(#3097,#3098,#3099,#3100));
#809=EDGE_LOOP('',(#3101,#3102,#3103,#3104));
#810=EDGE_LOOP('',(#3105,#3106,#3107,#3108));
#811=EDGE_LOOP('',(#3109,#3110,#3111,#3112));
#812=EDGE_LOOP('',(#3113,#3114,#3115,#3116));
#813=EDGE_LOOP('',(#3117,#3118,#3119,#3120));
#814=EDGE_LOOP('',(#3121,#3122,#3123,#3124));
#815=EDGE_LOOP('',(#3125,#3126,#3127,#3128));
#816=EDGE_LOOP('',(#3129,#3130,#3131,#3132));
#817=EDGE_LOOP('',(#3133,#3134,#3135,#3136));
#818=EDGE_LOOP('',(#3137,#3138,#3139,#3140));
#819=EDGE_LOOP('',(#3141,#3142,#3143,#3144));
#820=EDGE_LOOP('',(#3145,#3146,#3147,#3148));
#821=EDGE_LOOP('',(#3149,#3150,#3151,#3152));
#822=EDGE_LOOP('',(#3153,#3154,#3155,#3156,#3157,#3158,#3159,#3160));
#823=EDGE_LOOP('',(#3161,#3162,#3163,#3164,#3165,#3166,#3167,#3168,#3169,
#3170,#3171,#3172,#3173,#3174,#3175,#3176,#3177,#3178,#3179,#3180,#3181,
#3182,#3183,#3184,#3185,#3186,#3187,#3188,#3189,#3190,#3191,#3192,#3193,
#3194,#3195,#3196,#3197,#3198,#3199,#3200,#3201,#3202,#3203,#3204,#3205,
#3206,#3207,#3208,#3209,#3210,#3211,#3212,#3213,#3214,#3215,#3216,#3217,
#3218,#3219,#3220,#3221,#3222,#3223,#3224));
#824=EDGE_LOOP('',(#3225,#3226,#3227,#3228));
#825=EDGE_LOOP('',(#3229,#3230,#3231,#3232,#3233,#3234,#3235,#3236,#3237,
#3238,#3239,#3240,#3241,#3242,#3243,#3244,#3245,#3246,#3247,#3248,#3249,
#3250,#3251,#3252,#3253,#3254,#3255,#3256,#3257,#3258,#3259,#3260,#3261,
#3262,#3263,#3264,#3265,#3266,#3267,#3268,#3269,#3270,#3271,#3272,#3273,
#3274,#3275,#3276,#3277,#3278,#3279,#3280,#3281,#3282,#3283,#3284,#3285,
#3286,#3287,#3288,#3289,#3290,#3291,#3292,#3293));
#826=EDGE_LOOP('',(#3294,#3295,#3296,#3297));
#827=EDGE_LOOP('',(#3298,#3299,#3300,#3301));
#828=EDGE_LOOP('',(#3302,#3303,#3304,#3305));
#829=EDGE_LOOP('',(#3306,#3307,#3308,#3309));
#830=EDGE_LOOP('',(#3310,#3311,#3312,#3313));
#831=EDGE_LOOP('',(#3314,#3315,#3316,#3317));
#832=EDGE_LOOP('',(#3318,#3319,#3320,#3321));
#833=EDGE_LOOP('',(#3322,#3323,#3324,#3325,#3326,#3327));
#834=EDGE_LOOP('',(#3328));
#835=EDGE_LOOP('',(#3329,#3330,#3331,#3332));
#836=EDGE_LOOP('',(#3333,#3334,#3335,#3336));
#837=EDGE_LOOP('',(#3337));
#838=EDGE_LOOP('',(#3338,#3339,#3340,#3341,#3342,#3343));
#839=EDGE_LOOP('',(#3344));
#991=LINE('',#9399,#1220);
#992=LINE('',#9423,#1221);
#993=LINE('',#9471,#1222);
#994=LINE('',#9519,#1223);
#995=LINE('',#9573,#1224);
#996=LINE('',#9621,#1225);
#997=LINE('',#9669,#1226);
#998=LINE('',#9717,#1227);
#999=LINE('',#9771,#1228);
#1000=LINE('',#9819,#1229);
#1001=LINE('',#9867,#1230);
#1002=LINE('',#9921,#1231);
#1003=LINE('',#9969,#1232);
#1004=LINE('',#10017,#1233);
#1005=LINE('',#10068,#1234);
#1006=LINE('',#10116,#1235);
#1007=LINE('',#10164,#1236);
#1008=LINE('',#10212,#1237);
#1009=LINE('',#10266,#1238);
#1010=LINE('',#10314,#1239);
#1011=LINE('',#10362,#1240);
#1012=LINE('',#10416,#1241);
#1013=LINE('',#10464,#1242);
#1014=LINE('',#10512,#1243);
#1015=LINE('',#10563,#1244);
#1016=LINE('',#10614,#1245);
#1017=LINE('',#10662,#1246);
#1018=LINE('',#10710,#1247);
#1019=LINE('',#10764,#1248);
#1020=LINE('',#10812,#1249);
#1021=LINE('',#10860,#1250);
#1022=LINE('',#10885,#1251);
#1023=LINE('',#10910,#1252);
#1024=LINE('',#10934,#1253);
#1025=LINE('',#10959,#1254);
#1026=LINE('',#10984,#1255);
#1027=LINE('',#11008,#1256);
#1028=LINE('',#11032,#1257);
#1029=LINE('',#11058,#1258);
#1030=LINE('',#11082,#1259);
#1031=LINE('',#11106,#1260);
#1032=LINE('',#11131,#1261);
#1033=LINE('',#11156,#1262);
#1034=LINE('',#11180,#1263);
#1035=LINE('',#11205,#1264);
#1036=LINE('',#11230,#1265);
#1037=LINE('',#11254,#1266);
#1038=LINE('',#11278,#1267);
#1039=LINE('',#11304,#1268);
#1040=LINE('',#11328,#1269);
#1041=LINE('',#11352,#1270);
#1042=LINE('',#11377,#1271);
#1043=LINE('',#11402,#1272);
#1044=LINE('',#11426,#1273);
#1045=LINE('',#11451,#1274);
#1046=LINE('',#11476,#1275);
#1047=LINE('',#11500,#1276);
#1048=LINE('',#11524,#1277);
#1049=LINE('',#11549,#1278);
#1050=LINE('',#11574,#1279);
#1051=LINE('',#11904,#1280);
#1052=LINE('',#13721,#1281);
#1053=LINE('',#13723,#1282);
#1054=LINE('',#13725,#1283);
#1055=LINE('',#13726,#1284);
#1056=LINE('',#13729,#1285);
#1057=LINE('',#13731,#1286);
#1058=LINE('',#13732,#1287);
#1059=LINE('',#13735,#1288);
#1060=LINE('',#13737,#1289);
#1061=LINE('',#13738,#1290);
#1062=LINE('',#13741,#1291);
#1063=LINE('',#13743,#1292);
#1064=LINE('',#13744,#1293);
#1065=LINE('',#13747,#1294);
#1066=LINE('',#13749,#1295);
#1067=LINE('',#13750,#1296);
#1068=LINE('',#13752,#1297);
#1069=LINE('',#13753,#1298);
#1070=LINE('',#13760,#1299);
#1220=VECTOR('',#4540,2.5);
#1221=VECTOR('',#4545,2.5);
#1222=VECTOR('',#4548,2.5);
#1223=VECTOR('',#4551,2.5);
#1224=VECTOR('',#4554,2.5);
#1225=VECTOR('',#4557,2.5);
#1226=VECTOR('',#4560,2.5);
#1227=VECTOR('',#4563,2.5);
#1228=VECTOR('',#4566,2.5);
#1229=VECTOR('',#4569,2.5);
#1230=VECTOR('',#4572,2.5);
#1231=VECTOR('',#4575,2.5);
#1232=VECTOR('',#4578,2.5);
#1233=VECTOR('',#4581,2.5);
#1234=VECTOR('',#4584,2.5);
#1235=VECTOR('',#4587,2.5);
#1236=VECTOR('',#4590,2.5);
#1237=VECTOR('',#4593,2.5);
#1238=VECTOR('',#4596,2.5);
#1239=VECTOR('',#4599,2.5);
#1240=VECTOR('',#4602,2.5);
#1241=VECTOR('',#4605,2.5);
#1242=VECTOR('',#4608,2.5);
#1243=VECTOR('',#4611,2.5);
#1244=VECTOR('',#4614,2.5);
#1245=VECTOR('',#4617,2.5);
#1246=VECTOR('',#4620,2.5);
#1247=VECTOR('',#4623,2.5);
#1248=VECTOR('',#4626,2.5);
#1249=VECTOR('',#4629,2.5);
#1250=VECTOR('',#4632,1.99475);
#1251=VECTOR('',#4637,1.99475);
#1252=VECTOR('',#4640,1.99475);
#1253=VECTOR('',#4643,1.99475);
#1254=VECTOR('',#4646,1.99475);
#1255=VECTOR('',#4649,1.99475);
#1256=VECTOR('',#4652,1.99475);
#1257=VECTOR('',#4655,1.99475);
#1258=VECTOR('',#4658,1.99475);
#1259=VECTOR('',#4661,1.99475);
#1260=VECTOR('',#4664,1.99475);
#1261=VECTOR('',#4667,1.99475);
#1262=VECTOR('',#4670,1.99475);
#1263=VECTOR('',#4673,1.99475);
#1264=VECTOR('',#4676,1.99475);
#1265=VECTOR('',#4679,1.99475);
#1266=VECTOR('',#4682,1.99475);
#1267=VECTOR('',#4685,1.99475);
#1268=VECTOR('',#4688,1.99475);
#1269=VECTOR('',#4691,1.99475);
#1270=VECTOR('',#4694,1.99475);
#1271=VECTOR('',#4697,1.99475);
#1272=VECTOR('',#4700,1.99475);
#1273=VECTOR('',#4703,1.99475);
#1274=VECTOR('',#4706,1.99475);
#1275=VECTOR('',#4709,1.99475);
#1276=VECTOR('',#4712,1.99475);
#1277=VECTOR('',#4715,1.99475);
#1278=VECTOR('',#4718,1.99475);
#1279=VECTOR('',#4721,1.99475);
#1280=VECTOR('',#4726,2.);
#1281=VECTOR('',#4737,10.);
#1282=VECTOR('',#4738,10.);
#1283=VECTOR('',#4739,10.);
#1284=VECTOR('',#4740,10.);
#1285=VECTOR('',#4743,10.);
#1286=VECTOR('',#4744,10.);
#1287=VECTOR('',#4745,10.);
#1288=VECTOR('',#4748,10.);
#1289=VECTOR('',#4749,10.);
#1290=VECTOR('',#4750,10.);
#1291=VECTOR('',#4753,10.);
#1292=VECTOR('',#4754,10.);
#1293=VECTOR('',#4755,10.);
#1294=VECTOR('',#4758,10.);
#1295=VECTOR('',#4759,10.);
#1296=VECTOR('',#4760,10.);
#1297=VECTOR('',#4763,10.);
#1298=VECTOR('',#4764,10.);
#1299=VECTOR('',#4773,4.);
#1351=CIRCLE('',#3943,2.4505);
#1352=CIRCLE('',#3974,1.99475);
#1353=CIRCLE('',#4005,2.4505);
#1354=CIRCLE('',#4006,1.5);
#1355=CIRCLE('',#4008,1.99475);
#1356=CIRCLE('',#4018,4.);
#1357=CIRCLE('',#4020,4.);
#1576=VERTEX_POINT('',#9397);
#1577=VERTEX_POINT('',#9398);
#1578=VERTEX_POINT('',#9400);
#1579=VERTEX_POINT('',#9411);
#1580=VERTEX_POINT('',#9421);
#1581=VERTEX_POINT('',#9422);
#1582=VERTEX_POINT('',#9469);
#1583=VERTEX_POINT('',#9470);
#1584=VERTEX_POINT('',#9517);
#1585=VERTEX_POINT('',#9518);
#1586=VERTEX_POINT('',#9571);
#1587=VERTEX_POINT('',#9572);
#1588=VERTEX_POINT('',#9619);
#1589=VERTEX_POINT('',#9620);
#1590=VERTEX_POINT('',#9667);
#1591=VERTEX_POINT('',#9668);
#1592=VERTEX_POINT('',#9715);
#1593=VERTEX_POINT('',#9716);
#1594=VERTEX_POINT('',#9769);
#1595=VERTEX_POINT('',#9770);
#1596=VERTEX_POINT('',#9817);
#1597=VERTEX_POINT('',#9818);
#1598=VERTEX_POINT('',#9865);
#1599=VERTEX_POINT('',#9866);
#1600=VERTEX_POINT('',#9919);
#1601=VERTEX_POINT('',#9920);
#1602=VERTEX_POINT('',#9967);
#1603=VERTEX_POINT('',#9968);
#1604=VERTEX_POINT('',#10015);
#1605=VERTEX_POINT('',#10016);
#1606=VERTEX_POINT('',#10066);
#1607=VERTEX_POINT('',#10067);
#1608=VERTEX_POINT('',#10114);
#1609=VERTEX_POINT('',#10115);
#1610=VERTEX_POINT('',#10162);
#1611=VERTEX_POINT('',#10163);
#1612=VERTEX_POINT('',#10210);
#1613=VERTEX_POINT('',#10211);
#1614=VERTEX_POINT('',#10264);
#1615=VERTEX_POINT('',#10265);
#1616=VERTEX_POINT('',#10312);
#1617=VERTEX_POINT('',#10313);
#1618=VERTEX_POINT('',#10360);
#1619=VERTEX_POINT('',#10361);
#1620=VERTEX_POINT('',#10414);
#1621=VERTEX_POINT('',#10415);
#1622=VERTEX_POINT('',#10462);
#1623=VERTEX_POINT('',#10463);
#1624=VERTEX_POINT('',#10510);
#1625=VERTEX_POINT('',#10511);
#1626=VERTEX_POINT('',#10561);
#1627=VERTEX_POINT('',#10562);
#1628=VERTEX_POINT('',#10612);
#1629=VERTEX_POINT('',#10613);
#1630=VERTEX_POINT('',#10660);
#1631=VERTEX_POINT('',#10661);
#1632=VERTEX_POINT('',#10708);
#1633=VERTEX_POINT('',#10709);
#1634=VERTEX_POINT('',#10762);
#1635=VERTEX_POINT('',#10763);
#1636=VERTEX_POINT('',#10810);
#1637=VERTEX_POINT('',#10811);
#1638=VERTEX_POINT('',#10858);
#1639=VERTEX_POINT('',#10859);
#1640=VERTEX_POINT('',#10861);
#1641=VERTEX_POINT('',#10872);
#1642=VERTEX_POINT('',#10883);
#1643=VERTEX_POINT('',#10884);
#1644=VERTEX_POINT('',#10908);
#1645=VERTEX_POINT('',#10909);
#1646=VERTEX_POINT('',#10932);
#1647=VERTEX_POINT('',#10933);
#1648=VERTEX_POINT('',#10957);
#1649=VERTEX_POINT('',#10958);
#1650=VERTEX_POINT('',#10982);
#1651=VERTEX_POINT('',#10983);
#1652=VERTEX_POINT('',#11006);
#1653=VERTEX_POINT('',#11007);
#1654=VERTEX_POINT('',#11030);
#1655=VERTEX_POINT('',#11031);
#1656=VERTEX_POINT('',#11056);
#1657=VERTEX_POINT('',#11057);
#1658=VERTEX_POINT('',#11080);
#1659=VERTEX_POINT('',#11081);
#1660=VERTEX_POINT('',#11104);
#1661=VERTEX_POINT('',#11105);
#1662=VERTEX_POINT('',#11129);
#1663=VERTEX_POINT('',#11130);
#1664=VERTEX_POINT('',#11154);
#1665=VERTEX_POINT('',#11155);
#1666=VERTEX_POINT('',#11178);
#1667=VERTEX_POINT('',#11179);
#1668=VERTEX_POINT('',#11203);
#1669=VERTEX_POINT('',#11204);
#1670=VERTEX_POINT('',#11228);
#1671=VERTEX_POINT('',#11229);
#1672=VERTEX_POINT('',#11252);
#1673=VERTEX_POINT('',#11253);
#1674=VERTEX_POINT('',#11276);
#1675=VERTEX_POINT('',#11277);
#1676=VERTEX_POINT('',#11302);
#1677=VERTEX_POINT('',#11303);
#1678=VERTEX_POINT('',#11326);
#1679=VERTEX_POINT('',#11327);
#1680=VERTEX_POINT('',#11350);
#1681=VERTEX_POINT('',#11351);
#1682=VERTEX_POINT('',#11375);
#1683=VERTEX_POINT('',#11376);
#1684=VERTEX_POINT('',#11400);
#1685=VERTEX_POINT('',#11401);
#1686=VERTEX_POINT('',#11424);
#1687=VERTEX_POINT('',#11425);
#1688=VERTEX_POINT('',#11449);
#1689=VERTEX_POINT('',#11450);
#1690=VERTEX_POINT('',#11474);
#1691=VERTEX_POINT('',#11475);
#1692=VERTEX_POINT('',#11498);
#1693=VERTEX_POINT('',#11499);
#1694=VERTEX_POINT('',#11522);
#1695=VERTEX_POINT('',#11523);
#1696=VERTEX_POINT('',#11547);
#1697=VERTEX_POINT('',#11548);
#1698=VERTEX_POINT('',#11572);
#1699=VERTEX_POINT('',#11573);
#1700=VERTEX_POINT('',#11596);
#1701=VERTEX_POINT('',#11811);
#1702=VERTEX_POINT('',#11873);
#1703=VERTEX_POINT('',#11903);
#1704=VERTEX_POINT('',#12690);
#1705=VERTEX_POINT('',#12807);
#1706=VERTEX_POINT('',#13719);
#1707=VERTEX_POINT('',#13720);
#1708=VERTEX_POINT('',#13722);
#1709=VERTEX_POINT('',#13724);
#1710=VERTEX_POINT('',#13728);
#1711=VERTEX_POINT('',#13730);
#1712=VERTEX_POINT('',#13734);
#1713=VERTEX_POINT('',#13736);
#1714=VERTEX_POINT('',#13740);
#1715=VERTEX_POINT('',#13742);
#1716=VERTEX_POINT('',#13746);
#1717=VERTEX_POINT('',#13748);
#1718=VERTEX_POINT('',#13756);
#1719=VERTEX_POINT('',#13759);
#2046=EDGE_CURVE('',#1576,#1577,#991,.T.);
#2047=EDGE_CURVE('',#1576,#1578,#188,.T.);
#2048=EDGE_CURVE('',#1578,#1579,#1351,.F.);
#2049=EDGE_CURVE('',#1579,#1577,#189,.T.);
#2050=EDGE_CURVE('',#1580,#1581,#992,.T.);
#2051=EDGE_CURVE('',#1580,#1576,#190,.T.);
#2052=EDGE_CURVE('',#1577,#1581,#191,.T.);
#2053=EDGE_CURVE('',#1582,#1583,#993,.T.);
#2054=EDGE_CURVE('',#1582,#1580,#192,.T.);
#2055=EDGE_CURVE('',#1581,#1583,#193,.T.);
#2056=EDGE_CURVE('',#1584,#1585,#994,.T.);
#2057=EDGE_CURVE('',#1584,#1582,#194,.T.);
#2058=EDGE_CURVE('',#1583,#1585,#195,.T.);
#2059=EDGE_CURVE('',#1586,#1587,#995,.T.);
#2060=EDGE_CURVE('',#1586,#1584,#196,.T.);
#2061=EDGE_CURVE('',#1585,#1587,#197,.T.);
#2062=EDGE_CURVE('',#1588,#1589,#996,.T.);
#2063=EDGE_CURVE('',#1588,#1586,#198,.T.);
#2064=EDGE_CURVE('',#1587,#1589,#199,.T.);
#2065=EDGE_CURVE('',#1590,#1591,#997,.T.);
#2066=EDGE_CURVE('',#1590,#1588,#200,.T.);
#2067=EDGE_CURVE('',#1589,#1591,#201,.T.);
#2068=EDGE_CURVE('',#1592,#1593,#998,.T.);
#2069=EDGE_CURVE('',#1592,#1590,#202,.T.);
#2070=EDGE_CURVE('',#1591,#1593,#203,.T.);
#2071=EDGE_CURVE('',#1594,#1595,#999,.T.);
#2072=EDGE_CURVE('',#1594,#1592,#204,.T.);
#2073=EDGE_CURVE('',#1593,#1595,#205,.T.);
#2074=EDGE_CURVE('',#1596,#1597,#1000,.T.);
#2075=EDGE_CURVE('',#1596,#1594,#206,.T.);
#2076=EDGE_CURVE('',#1595,#1597,#207,.T.);
#2077=EDGE_CURVE('',#1598,#1599,#1001,.T.);
#2078=EDGE_CURVE('',#1598,#1596,#208,.T.);
#2079=EDGE_CURVE('',#1597,#1599,#209,.T.);
#2080=EDGE_CURVE('',#1600,#1601,#1002,.T.);
#2081=EDGE_CURVE('',#1600,#1598,#210,.T.);
#2082=EDGE_CURVE('',#1599,#1601,#211,.T.);
#2083=EDGE_CURVE('',#1602,#1603,#1003,.T.);
#2084=EDGE_CURVE('',#1602,#1600,#212,.T.);
#2085=EDGE_CURVE('',#1601,#1603,#213,.T.);
#2086=EDGE_CURVE('',#1604,#1605,#1004,.T.);
#2087=EDGE_CURVE('',#1604,#1602,#214,.T.);
#2088=EDGE_CURVE('',#1603,#1605,#215,.T.);
#2089=EDGE_CURVE('',#1606,#1607,#1005,.T.);
#2090=EDGE_CURVE('',#1606,#1604,#216,.T.);
#2091=EDGE_CURVE('',#1605,#1607,#217,.T.);
#2092=EDGE_CURVE('',#1608,#1609,#1006,.T.);
#2093=EDGE_CURVE('',#1608,#1606,#218,.T.);
#2094=EDGE_CURVE('',#1607,#1609,#219,.T.);
#2095=EDGE_CURVE('',#1610,#1611,#1007,.T.);
#2096=EDGE_CURVE('',#1610,#1608,#220,.T.);
#2097=EDGE_CURVE('',#1609,#1611,#221,.T.);
#2098=EDGE_CURVE('',#1612,#1613,#1008,.T.);
#2099=EDGE_CURVE('',#1612,#1610,#222,.T.);
#2100=EDGE_CURVE('',#1611,#1613,#223,.T.);
#2101=EDGE_CURVE('',#1614,#1615,#1009,.T.);
#2102=EDGE_CURVE('',#1614,#1612,#224,.T.);
#2103=EDGE_CURVE('',#1613,#1615,#225,.T.);
#2104=EDGE_CURVE('',#1616,#1617,#1010,.T.);
#2105=EDGE_CURVE('',#1616,#1614,#226,.T.);
#2106=EDGE_CURVE('',#1615,#1617,#227,.T.);
#2107=EDGE_CURVE('',#1618,#1619,#1011,.T.);
#2108=EDGE_CURVE('',#1618,#1616,#228,.T.);
#2109=EDGE_CURVE('',#1617,#1619,#229,.T.);
#2110=EDGE_CURVE('',#1620,#1621,#1012,.T.);
#2111=EDGE_CURVE('',#1620,#1618,#230,.T.);
#2112=EDGE_CURVE('',#1619,#1621,#231,.T.);
#2113=EDGE_CURVE('',#1622,#1623,#1013,.T.);
#2114=EDGE_CURVE('',#1622,#1620,#232,.T.);
#2115=EDGE_CURVE('',#1621,#1623,#233,.T.);
#2116=EDGE_CURVE('',#1624,#1625,#1014,.T.);
#2117=EDGE_CURVE('',#1624,#1622,#234,.T.);
#2118=EDGE_CURVE('',#1623,#1625,#235,.T.);
#2119=EDGE_CURVE('',#1626,#1627,#1015,.T.);
#2120=EDGE_CURVE('',#1626,#1624,#236,.T.);
#2121=EDGE_CURVE('',#1625,#1627,#237,.T.);
#2122=EDGE_CURVE('',#1628,#1629,#1016,.T.);
#2123=EDGE_CURVE('',#1628,#1626,#238,.T.);
#2124=EDGE_CURVE('',#1627,#1629,#239,.T.);
#2125=EDGE_CURVE('',#1630,#1631,#1017,.T.);
#2126=EDGE_CURVE('',#1630,#1628,#240,.T.);
#2127=EDGE_CURVE('',#1629,#1631,#241,.T.);
#2128=EDGE_CURVE('',#1632,#1633,#1018,.T.);
#2129=EDGE_CURVE('',#1632,#1630,#242,.T.);
#2130=EDGE_CURVE('',#1631,#1633,#243,.T.);
#2131=EDGE_CURVE('',#1634,#1635,#1019,.T.);
#2132=EDGE_CURVE('',#1634,#1632,#244,.T.);
#2133=EDGE_CURVE('',#1633,#1635,#245,.T.);
#2134=EDGE_CURVE('',#1636,#1637,#1020,.T.);
#2135=EDGE_CURVE('',#1636,#1634,#246,.T.);
#2136=EDGE_CURVE('',#1635,#1637,#247,.T.);
#2137=EDGE_CURVE('',#1638,#1639,#1021,.T.);
#2138=EDGE_CURVE('',#1638,#1640,#248,.T.);
#2139=EDGE_CURVE('',#1640,#1641,#1352,.T.);
#2140=EDGE_CURVE('',#1639,#1641,#249,.T.);
#2141=EDGE_CURVE('',#1642,#1643,#1022,.T.);
#2142=EDGE_CURVE('',#1642,#1638,#250,.T.);
#2143=EDGE_CURVE('',#1643,#1639,#251,.T.);
#2144=EDGE_CURVE('',#1644,#1645,#1023,.T.);
#2145=EDGE_CURVE('',#1644,#1642,#252,.T.);
#2146=EDGE_CURVE('',#1645,#1643,#253,.T.);
#2147=EDGE_CURVE('',#1646,#1647,#1024,.T.);
#2148=EDGE_CURVE('',#1646,#1644,#254,.T.);
#2149=EDGE_CURVE('',#1647,#1645,#255,.T.);
#2150=EDGE_CURVE('',#1648,#1649,#1025,.T.);
#2151=EDGE_CURVE('',#1648,#1646,#256,.T.);
#2152=EDGE_CURVE('',#1649,#1647,#257,.T.);
#2153=EDGE_CURVE('',#1650,#1651,#1026,.T.);
#2154=EDGE_CURVE('',#1650,#1648,#258,.T.);
#2155=EDGE_CURVE('',#1651,#1649,#259,.T.);
#2156=EDGE_CURVE('',#1652,#1653,#1027,.T.);
#2157=EDGE_CURVE('',#1652,#1650,#260,.T.);
#2158=EDGE_CURVE('',#1653,#1651,#261,.T.);
#2159=EDGE_CURVE('',#1654,#1655,#1028,.T.);
#2160=EDGE_CURVE('',#1654,#1652,#262,.T.);
#2161=EDGE_CURVE('',#1655,#1653,#263,.T.);
#2162=EDGE_CURVE('',#1656,#1657,#1029,.T.);
#2163=EDGE_CURVE('',#1656,#1654,#264,.T.);
#2164=EDGE_CURVE('',#1657,#1655,#265,.T.);
#2165=EDGE_CURVE('',#1658,#1659,#1030,.T.);
#2166=EDGE_CURVE('',#1658,#1656,#266,.T.);
#2167=EDGE_CURVE('',#1659,#1657,#267,.T.);
#2168=EDGE_CURVE('',#1660,#1661,#1031,.T.);
#2169=EDGE_CURVE('',#1660,#1658,#268,.T.);
#2170=EDGE_CURVE('',#1661,#1659,#269,.T.);
#2171=EDGE_CURVE('',#1662,#1663,#1032,.T.);
#2172=EDGE_CURVE('',#1662,#1660,#270,.T.);
#2173=EDGE_CURVE('',#1663,#1661,#271,.T.);
#2174=EDGE_CURVE('',#1664,#1665,#1033,.T.);
#2175=EDGE_CURVE('',#1664,#1662,#272,.T.);
#2176=EDGE_CURVE('',#1665,#1663,#273,.T.);
#2177=EDGE_CURVE('',#1666,#1667,#1034,.T.);
#2178=EDGE_CURVE('',#1666,#1664,#274,.T.);
#2179=EDGE_CURVE('',#1667,#1665,#275,.T.);
#2180=EDGE_CURVE('',#1668,#1669,#1035,.T.);
#2181=EDGE_CURVE('',#1668,#1666,#276,.T.);
#2182=EDGE_CURVE('',#1669,#1667,#277,.T.);
#2183=EDGE_CURVE('',#1670,#1671,#1036,.T.);
#2184=EDGE_CURVE('',#1670,#1668,#278,.T.);
#2185=EDGE_CURVE('',#1671,#1669,#279,.T.);
#2186=EDGE_CURVE('',#1672,#1673,#1037,.T.);
#2187=EDGE_CURVE('',#1672,#1670,#280,.T.);
#2188=EDGE_CURVE('',#1673,#1671,#281,.T.);
#2189=EDGE_CURVE('',#1674,#1675,#1038,.T.);
#2190=EDGE_CURVE('',#1674,#1672,#282,.T.);
#2191=EDGE_CURVE('',#1675,#1673,#283,.T.);
#2192=EDGE_CURVE('',#1676,#1677,#1039,.T.);
#2193=EDGE_CURVE('',#1676,#1674,#284,.T.);
#2194=EDGE_CURVE('',#1677,#1675,#285,.T.);
#2195=EDGE_CURVE('',#1678,#1679,#1040,.T.);
#2196=EDGE_CURVE('',#1678,#1676,#286,.T.);
#2197=EDGE_CURVE('',#1679,#1677,#287,.T.);
#2198=EDGE_CURVE('',#1680,#1681,#1041,.T.);
#2199=EDGE_CURVE('',#1680,#1678,#288,.T.);
#2200=EDGE_CURVE('',#1681,#1679,#289,.T.);
#2201=EDGE_CURVE('',#1682,#1683,#1042,.T.);
#2202=EDGE_CURVE('',#1682,#1680,#290,.T.);
#2203=EDGE_CURVE('',#1683,#1681,#291,.T.);
#2204=EDGE_CURVE('',#1684,#1685,#1043,.T.);
#2205=EDGE_CURVE('',#1684,#1682,#292,.T.);
#2206=EDGE_CURVE('',#1685,#1683,#293,.T.);
#2207=EDGE_CURVE('',#1686,#1687,#1044,.T.);
#2208=EDGE_CURVE('',#1686,#1684,#294,.T.);
#2209=EDGE_CURVE('',#1687,#1685,#295,.T.);
#2210=EDGE_CURVE('',#1688,#1689,#1045,.T.);
#2211=EDGE_CURVE('',#1688,#1686,#296,.T.);
#2212=EDGE_CURVE('',#1689,#1687,#297,.T.);
#2213=EDGE_CURVE('',#1690,#1691,#1046,.T.);
#2214=EDGE_CURVE('',#1690,#1688,#298,.T.);
#2215=EDGE_CURVE('',#1691,#1689,#299,.T.);
#2216=EDGE_CURVE('',#1692,#1693,#1047,.T.);
#2217=EDGE_CURVE('',#1692,#1690,#300,.T.);
#2218=EDGE_CURVE('',#1693,#1691,#301,.T.);
#2219=EDGE_CURVE('',#1694,#1695,#1048,.T.);
#2220=EDGE_CURVE('',#1694,#1692,#302,.T.);
#2221=EDGE_CURVE('',#1695,#1693,#303,.T.);
#2222=EDGE_CURVE('',#1696,#1697,#1049,.T.);
#2223=EDGE_CURVE('',#1696,#1694,#304,.T.);
#2224=EDGE_CURVE('',#1697,#1695,#305,.T.);
#2225=EDGE_CURVE('',#1698,#1699,#1050,.T.);
#2226=EDGE_CURVE('',#1698,#1696,#306,.T.);
#2227=EDGE_CURVE('',#1699,#1697,#307,.T.);
#2228=EDGE_CURVE('',#1641,#1700,#308,.T.);
#2229=EDGE_CURVE('',#1701,#1640,#309,.T.);
#2230=EDGE_CURVE('',#1702,#1701,#1353,.T.);
#2231=EDGE_CURVE('',#1700,#1702,#310,.T.);
#2232=EDGE_CURVE('',#1700,#1703,#1051,.T.);
#2233=EDGE_CURVE('',#1703,#1703,#1354,.T.);
#2234=EDGE_CURVE('',#1704,#1698,#311,.T.);
#2235=EDGE_CURVE('',#1578,#1704,#312,.T.);
#2236=EDGE_CURVE('',#1701,#1636,#313,.T.);
#2237=EDGE_CURVE('',#1705,#1699,#314,.T.);
#2238=EDGE_CURVE('',#1704,#1705,#1355,.T.);
#2239=EDGE_CURVE('',#1637,#1702,#315,.T.);
#2240=EDGE_CURVE('',#1705,#1579,#316,.T.);
#2241=EDGE_CURVE('',#1706,#1707,#1052,.T.);
#2242=EDGE_CURVE('',#1706,#1708,#1053,.T.);
#2243=EDGE_CURVE('',#1708,#1709,#1054,.T.);
#2244=EDGE_CURVE('',#1707,#1709,#1055,.T.);
#2245=EDGE_CURVE('',#1710,#1706,#1056,.T.);
#2246=EDGE_CURVE('',#1710,#1711,#1057,.T.);
#2247=EDGE_CURVE('',#1711,#1708,#1058,.T.);
#2248=EDGE_CURVE('',#1712,#1710,#1059,.T.);
#2249=EDGE_CURVE('',#1712,#1713,#1060,.T.);
#2250=EDGE_CURVE('',#1713,#1711,#1061,.T.);
#2251=EDGE_CURVE('',#1714,#1712,#1062,.T.);
#2252=EDGE_CURVE('',#1714,#1715,#1063,.T.);
#2253=EDGE_CURVE('',#1715,#1713,#1064,.T.);
#2254=EDGE_CURVE('',#1716,#1714,#1065,.T.);
#2255=EDGE_CURVE('',#1716,#1717,#1066,.T.);
#2256=EDGE_CURVE('',#1717,#1715,#1067,.T.);
#2257=EDGE_CURVE('',#1707,#1716,#1068,.T.);
#2258=EDGE_CURVE('',#1709,#1717,#1069,.T.);
#2259=EDGE_CURVE('',#1718,#1718,#1356,.T.);
#2260=EDGE_CURVE('',#1718,#1719,#1070,.T.);
#2261=EDGE_CURVE('',#1719,#1719,#1357,.T.);
#2913=ORIENTED_EDGE('',*,*,#2046,.F.);
#2914=ORIENTED_EDGE('',*,*,#2047,.T.);
#2915=ORIENTED_EDGE('',*,*,#2048,.T.);
#2916=ORIENTED_EDGE('',*,*,#2049,.T.);
#2917=ORIENTED_EDGE('',*,*,#2050,.F.);
#2918=ORIENTED_EDGE('',*,*,#2051,.T.);
#2919=ORIENTED_EDGE('',*,*,#2046,.T.);
#2920=ORIENTED_EDGE('',*,*,#2052,.T.);
#2921=ORIENTED_EDGE('',*,*,#2053,.F.);
#2922=ORIENTED_EDGE('',*,*,#2054,.T.);
#2923=ORIENTED_EDGE('',*,*,#2050,.T.);
#2924=ORIENTED_EDGE('',*,*,#2055,.T.);
#2925=ORIENTED_EDGE('',*,*,#2056,.F.);
#2926=ORIENTED_EDGE('',*,*,#2057,.T.);
#2927=ORIENTED_EDGE('',*,*,#2053,.T.);
#2928=ORIENTED_EDGE('',*,*,#2058,.T.);
#2929=ORIENTED_EDGE('',*,*,#2059,.F.);
#2930=ORIENTED_EDGE('',*,*,#2060,.T.);
#2931=ORIENTED_EDGE('',*,*,#2056,.T.);
#2932=ORIENTED_EDGE('',*,*,#2061,.T.);
#2933=ORIENTED_EDGE('',*,*,#2062,.F.);
#2934=ORIENTED_EDGE('',*,*,#2063,.T.);
#2935=ORIENTED_EDGE('',*,*,#2059,.T.);
#2936=ORIENTED_EDGE('',*,*,#2064,.T.);
#2937=ORIENTED_EDGE('',*,*,#2065,.F.);
#2938=ORIENTED_EDGE('',*,*,#2066,.T.);
#2939=ORIENTED_EDGE('',*,*,#2062,.T.);
#2940=ORIENTED_EDGE('',*,*,#2067,.T.);
#2941=ORIENTED_EDGE('',*,*,#2068,.F.);
#2942=ORIENTED_EDGE('',*,*,#2069,.T.);
#2943=ORIENTED_EDGE('',*,*,#2065,.T.);
#2944=ORIENTED_EDGE('',*,*,#2070,.T.);
#2945=ORIENTED_EDGE('',*,*,#2071,.F.);
#2946=ORIENTED_EDGE('',*,*,#2072,.T.);
#2947=ORIENTED_EDGE('',*,*,#2068,.T.);
#2948=ORIENTED_EDGE('',*,*,#2073,.T.);
#2949=ORIENTED_EDGE('',*,*,#2074,.F.);
#2950=ORIENTED_EDGE('',*,*,#2075,.T.);
#2951=ORIENTED_EDGE('',*,*,#2071,.T.);
#2952=ORIENTED_EDGE('',*,*,#2076,.T.);
#2953=ORIENTED_EDGE('',*,*,#2077,.F.);
#2954=ORIENTED_EDGE('',*,*,#2078,.T.);
#2955=ORIENTED_EDGE('',*,*,#2074,.T.);
#2956=ORIENTED_EDGE('',*,*,#2079,.T.);
#2957=ORIENTED_EDGE('',*,*,#2080,.F.);
#2958=ORIENTED_EDGE('',*,*,#2081,.T.);
#2959=ORIENTED_EDGE('',*,*,#2077,.T.);
#2960=ORIENTED_EDGE('',*,*,#2082,.T.);
#2961=ORIENTED_EDGE('',*,*,#2083,.F.);
#2962=ORIENTED_EDGE('',*,*,#2084,.T.);
#2963=ORIENTED_EDGE('',*,*,#2080,.T.);
#2964=ORIENTED_EDGE('',*,*,#2085,.T.);
#2965=ORIENTED_EDGE('',*,*,#2086,.F.);
#2966=ORIENTED_EDGE('',*,*,#2087,.T.);
#2967=ORIENTED_EDGE('',*,*,#2083,.T.);
#2968=ORIENTED_EDGE('',*,*,#2088,.T.);
#2969=ORIENTED_EDGE('',*,*,#2089,.F.);
#2970=ORIENTED_EDGE('',*,*,#2090,.T.);
#2971=ORIENTED_EDGE('',*,*,#2086,.T.);
#2972=ORIENTED_EDGE('',*,*,#2091,.T.);
#2973=ORIENTED_EDGE('',*,*,#2092,.F.);
#2974=ORIENTED_EDGE('',*,*,#2093,.T.);
#2975=ORIENTED_EDGE('',*,*,#2089,.T.);
#2976=ORIENTED_EDGE('',*,*,#2094,.T.);
#2977=ORIENTED_EDGE('',*,*,#2095,.F.);
#2978=ORIENTED_EDGE('',*,*,#2096,.T.);
#2979=ORIENTED_EDGE('',*,*,#2092,.T.);
#2980=ORIENTED_EDGE('',*,*,#2097,.T.);
#2981=ORIENTED_EDGE('',*,*,#2098,.F.);
#2982=ORIENTED_EDGE('',*,*,#2099,.T.);
#2983=ORIENTED_EDGE('',*,*,#2095,.T.);
#2984=ORIENTED_EDGE('',*,*,#2100,.T.);
#2985=ORIENTED_EDGE('',*,*,#2101,.F.);
#2986=ORIENTED_EDGE('',*,*,#2102,.T.);
#2987=ORIENTED_EDGE('',*,*,#2098,.T.);
#2988=ORIENTED_EDGE('',*,*,#2103,.T.);
#2989=ORIENTED_EDGE('',*,*,#2104,.F.);
#2990=ORIENTED_EDGE('',*,*,#2105,.T.);
#2991=ORIENTED_EDGE('',*,*,#2101,.T.);
#2992=ORIENTED_EDGE('',*,*,#2106,.T.);
#2993=ORIENTED_EDGE('',*,*,#2107,.F.);
#2994=ORIENTED_EDGE('',*,*,#2108,.T.);
#2995=ORIENTED_EDGE('',*,*,#2104,.T.);
#2996=ORIENTED_EDGE('',*,*,#2109,.T.);
#2997=ORIENTED_EDGE('',*,*,#2110,.F.);
#2998=ORIENTED_EDGE('',*,*,#2111,.T.);
#2999=ORIENTED_EDGE('',*,*,#2107,.T.);
#3000=ORIENTED_EDGE('',*,*,#2112,.T.);
#3001=ORIENTED_EDGE('',*,*,#2113,.F.);
#3002=ORIENTED_EDGE('',*,*,#2114,.T.);
#3003=ORIENTED_EDGE('',*,*,#2110,.T.);
#3004=ORIENTED_EDGE('',*,*,#2115,.T.);
#3005=ORIENTED_EDGE('',*,*,#2116,.F.);
#3006=ORIENTED_EDGE('',*,*,#2117,.T.);
#3007=ORIENTED_EDGE('',*,*,#2113,.T.);
#3008=ORIENTED_EDGE('',*,*,#2118,.T.);
#3009=ORIENTED_EDGE('',*,*,#2119,.F.);
#3010=ORIENTED_EDGE('',*,*,#2120,.T.);
#3011=ORIENTED_EDGE('',*,*,#2116,.T.);
#3012=ORIENTED_EDGE('',*,*,#2121,.T.);
#3013=ORIENTED_EDGE('',*,*,#2122,.F.);
#3014=ORIENTED_EDGE('',*,*,#2123,.T.);
#3015=ORIENTED_EDGE('',*,*,#2119,.T.);
#3016=ORIENTED_EDGE('',*,*,#2124,.T.);
#3017=ORIENTED_EDGE('',*,*,#2125,.F.);
#3018=ORIENTED_EDGE('',*,*,#2126,.T.);
#3019=ORIENTED_EDGE('',*,*,#2122,.T.);
#3020=ORIENTED_EDGE('',*,*,#2127,.T.);
#3021=ORIENTED_EDGE('',*,*,#2128,.F.);
#3022=ORIENTED_EDGE('',*,*,#2129,.T.);
#3023=ORIENTED_EDGE('',*,*,#2125,.T.);
#3024=ORIENTED_EDGE('',*,*,#2130,.T.);
#3025=ORIENTED_EDGE('',*,*,#2131,.F.);
#3026=ORIENTED_EDGE('',*,*,#2132,.T.);
#3027=ORIENTED_EDGE('',*,*,#2128,.T.);
#3028=ORIENTED_EDGE('',*,*,#2133,.T.);
#3029=ORIENTED_EDGE('',*,*,#2134,.F.);
#3030=ORIENTED_EDGE('',*,*,#2135,.T.);
#3031=ORIENTED_EDGE('',*,*,#2131,.T.);
#3032=ORIENTED_EDGE('',*,*,#2136,.T.);
#3033=ORIENTED_EDGE('',*,*,#2137,.F.);
#3034=ORIENTED_EDGE('',*,*,#2138,.T.);
#3035=ORIENTED_EDGE('',*,*,#2139,.T.);
#3036=ORIENTED_EDGE('',*,*,#2140,.F.);
#3037=ORIENTED_EDGE('',*,*,#2141,.F.);
#3038=ORIENTED_EDGE('',*,*,#2142,.T.);
#3039=ORIENTED_EDGE('',*,*,#2137,.T.);
#3040=ORIENTED_EDGE('',*,*,#2143,.F.);
#3041=ORIENTED_EDGE('',*,*,#2144,.F.);
#3042=ORIENTED_EDGE('',*,*,#2145,.T.);
#3043=ORIENTED_EDGE('',*,*,#2141,.T.);
#3044=ORIENTED_EDGE('',*,*,#2146,.F.);
#3045=ORIENTED_EDGE('',*,*,#2147,.F.);
#3046=ORIENTED_EDGE('',*,*,#2148,.T.);
#3047=ORIENTED_EDGE('',*,*,#2144,.T.);
#3048=ORIENTED_EDGE('',*,*,#2149,.F.);
#3049=ORIENTED_EDGE('',*,*,#2150,.F.);
#3050=ORIENTED_EDGE('',*,*,#2151,.T.);
#3051=ORIENTED_EDGE('',*,*,#2147,.T.);
#3052=ORIENTED_EDGE('',*,*,#2152,.F.);
#3053=ORIENTED_EDGE('',*,*,#2153,.F.);
#3054=ORIENTED_EDGE('',*,*,#2154,.T.);
#3055=ORIENTED_EDGE('',*,*,#2150,.T.);
#3056=ORIENTED_EDGE('',*,*,#2155,.F.);
#3057=ORIENTED_EDGE('',*,*,#2156,.F.);
#3058=ORIENTED_EDGE('',*,*,#2157,.T.);
#3059=ORIENTED_EDGE('',*,*,#2153,.T.);
#3060=ORIENTED_EDGE('',*,*,#2158,.F.);
#3061=ORIENTED_EDGE('',*,*,#2159,.F.);
#3062=ORIENTED_EDGE('',*,*,#2160,.T.);
#3063=ORIENTED_EDGE('',*,*,#2156,.T.);
#3064=ORIENTED_EDGE('',*,*,#2161,.F.);
#3065=ORIENTED_EDGE('',*,*,#2162,.F.);
#3066=ORIENTED_EDGE('',*,*,#2163,.T.);
#3067=ORIENTED_EDGE('',*,*,#2159,.T.);
#3068=ORIENTED_EDGE('',*,*,#2164,.F.);
#3069=ORIENTED_EDGE('',*,*,#2165,.F.);
#3070=ORIENTED_EDGE('',*,*,#2166,.T.);
#3071=ORIENTED_EDGE('',*,*,#2162,.T.);
#3072=ORIENTED_EDGE('',*,*,#2167,.F.);
#3073=ORIENTED_EDGE('',*,*,#2168,.F.);
#3074=ORIENTED_EDGE('',*,*,#2169,.T.);
#3075=ORIENTED_EDGE('',*,*,#2165,.T.);
#3076=ORIENTED_EDGE('',*,*,#2170,.F.);
#3077=ORIENTED_EDGE('',*,*,#2171,.F.);
#3078=ORIENTED_EDGE('',*,*,#2172,.T.);
#3079=ORIENTED_EDGE('',*,*,#2168,.T.);
#3080=ORIENTED_EDGE('',*,*,#2173,.F.);
#3081=ORIENTED_EDGE('',*,*,#2174,.F.);
#3082=ORIENTED_EDGE('',*,*,#2175,.T.);
#3083=ORIENTED_EDGE('',*,*,#2171,.T.);
#3084=ORIENTED_EDGE('',*,*,#2176,.F.);
#3085=ORIENTED_EDGE('',*,*,#2177,.F.);
#3086=ORIENTED_EDGE('',*,*,#2178,.T.);
#3087=ORIENTED_EDGE('',*,*,#2174,.T.);
#3088=ORIENTED_EDGE('',*,*,#2179,.F.);
#3089=ORIENTED_EDGE('',*,*,#2180,.F.);
#3090=ORIENTED_EDGE('',*,*,#2181,.T.);
#3091=ORIENTED_EDGE('',*,*,#2177,.T.);
#3092=ORIENTED_EDGE('',*,*,#2182,.F.);
#3093=ORIENTED_EDGE('',*,*,#2183,.F.);
#3094=ORIENTED_EDGE('',*,*,#2184,.T.);
#3095=ORIENTED_EDGE('',*,*,#2180,.T.);
#3096=ORIENTED_EDGE('',*,*,#2185,.F.);
#3097=ORIENTED_EDGE('',*,*,#2186,.F.);
#3098=ORIENTED_EDGE('',*,*,#2187,.T.);
#3099=ORIENTED_EDGE('',*,*,#2183,.T.);
#3100=ORIENTED_EDGE('',*,*,#2188,.F.);
#3101=ORIENTED_EDGE('',*,*,#2189,.F.);
#3102=ORIENTED_EDGE('',*,*,#2190,.T.);
#3103=ORIENTED_EDGE('',*,*,#2186,.T.);
#3104=ORIENTED_EDGE('',*,*,#2191,.F.);
#3105=ORIENTED_EDGE('',*,*,#2192,.F.);
#3106=ORIENTED_EDGE('',*,*,#2193,.T.);
#3107=ORIENTED_EDGE('',*,*,#2189,.T.);
#3108=ORIENTED_EDGE('',*,*,#2194,.F.);
#3109=ORIENTED_EDGE('',*,*,#2195,.F.);
#3110=ORIENTED_EDGE('',*,*,#2196,.T.);
#3111=ORIENTED_EDGE('',*,*,#2192,.T.);
#3112=ORIENTED_EDGE('',*,*,#2197,.F.);
#3113=ORIENTED_EDGE('',*,*,#2198,.F.);
#3114=ORIENTED_EDGE('',*,*,#2199,.T.);
#3115=ORIENTED_EDGE('',*,*,#2195,.T.);
#3116=ORIENTED_EDGE('',*,*,#2200,.F.);
#3117=ORIENTED_EDGE('',*,*,#2201,.F.);
#3118=ORIENTED_EDGE('',*,*,#2202,.T.);
#3119=ORIENTED_EDGE('',*,*,#2198,.T.);
#3120=ORIENTED_EDGE('',*,*,#2203,.F.);
#3121=ORIENTED_EDGE('',*,*,#2204,.F.);
#3122=ORIENTED_EDGE('',*,*,#2205,.T.);
#3123=ORIENTED_EDGE('',*,*,#2201,.T.);
#3124=ORIENTED_EDGE('',*,*,#2206,.F.);
#3125=ORIENTED_EDGE('',*,*,#2207,.F.);
#3126=ORIENTED_EDGE('',*,*,#2208,.T.);
#3127=ORIENTED_EDGE('',*,*,#2204,.T.);
#3128=ORIENTED_EDGE('',*,*,#2209,.F.);
#3129=ORIENTED_EDGE('',*,*,#2210,.F.);
#3130=ORIENTED_EDGE('',*,*,#2211,.T.);
#3131=ORIENTED_EDGE('',*,*,#2207,.T.);
#3132=ORIENTED_EDGE('',*,*,#2212,.F.);
#3133=ORIENTED_EDGE('',*,*,#2213,.F.);
#3134=ORIENTED_EDGE('',*,*,#2214,.T.);
#3135=ORIENTED_EDGE('',*,*,#2210,.T.);
#3136=ORIENTED_EDGE('',*,*,#2215,.F.);
#3137=ORIENTED_EDGE('',*,*,#2216,.F.);
#3138=ORIENTED_EDGE('',*,*,#2217,.T.);
#3139=ORIENTED_EDGE('',*,*,#2213,.T.);
#3140=ORIENTED_EDGE('',*,*,#2218,.F.);
#3141=ORIENTED_EDGE('',*,*,#2219,.F.);
#3142=ORIENTED_EDGE('',*,*,#2220,.T.);
#3143=ORIENTED_EDGE('',*,*,#2216,.T.);
#3144=ORIENTED_EDGE('',*,*,#2221,.F.);
#3145=ORIENTED_EDGE('',*,*,#2222,.F.);
#3146=ORIENTED_EDGE('',*,*,#2223,.T.);
#3147=ORIENTED_EDGE('',*,*,#2219,.T.);
#3148=ORIENTED_EDGE('',*,*,#2224,.F.);
#3149=ORIENTED_EDGE('',*,*,#2225,.F.);
#3150=ORIENTED_EDGE('',*,*,#2226,.T.);
#3151=ORIENTED_EDGE('',*,*,#2222,.T.);
#3152=ORIENTED_EDGE('',*,*,#2227,.F.);
#3153=ORIENTED_EDGE('',*,*,#2228,.F.);
#3154=ORIENTED_EDGE('',*,*,#2139,.F.);
#3155=ORIENTED_EDGE('',*,*,#2229,.F.);
#3156=ORIENTED_EDGE('',*,*,#2230,.F.);
#3157=ORIENTED_EDGE('',*,*,#2231,.F.);
#3158=ORIENTED_EDGE('',*,*,#2232,.T.);
#3159=ORIENTED_EDGE('',*,*,#2233,.F.);
#3160=ORIENTED_EDGE('',*,*,#2232,.F.);
#3161=ORIENTED_EDGE('',*,*,#2229,.T.);
#3162=ORIENTED_EDGE('',*,*,#2138,.F.);
#3163=ORIENTED_EDGE('',*,*,#2142,.F.);
#3164=ORIENTED_EDGE('',*,*,#2145,.F.);
#3165=ORIENTED_EDGE('',*,*,#2148,.F.);
#3166=ORIENTED_EDGE('',*,*,#2151,.F.);
#3167=ORIENTED_EDGE('',*,*,#2154,.F.);
#3168=ORIENTED_EDGE('',*,*,#2157,.F.);
#3169=ORIENTED_EDGE('',*,*,#2160,.F.);
#3170=ORIENTED_EDGE('',*,*,#2163,.F.);
#3171=ORIENTED_EDGE('',*,*,#2166,.F.);
#3172=ORIENTED_EDGE('',*,*,#2169,.F.);
#3173=ORIENTED_EDGE('',*,*,#2172,.F.);
#3174=ORIENTED_EDGE('',*,*,#2175,.F.);
#3175=ORIENTED_EDGE('',*,*,#2178,.F.);
#3176=ORIENTED_EDGE('',*,*,#2181,.F.);
#3177=ORIENTED_EDGE('',*,*,#2184,.F.);
#3178=ORIENTED_EDGE('',*,*,#2187,.F.);
#3179=ORIENTED_EDGE('',*,*,#2190,.F.);
#3180=ORIENTED_EDGE('',*,*,#2193,.F.);
#3181=ORIENTED_EDGE('',*,*,#2196,.F.);
#3182=ORIENTED_EDGE('',*,*,#2199,.F.);
#3183=ORIENTED_EDGE('',*,*,#2202,.F.);
#3184=ORIENTED_EDGE('',*,*,#2205,.F.);
#3185=ORIENTED_EDGE('',*,*,#2208,.F.);
#3186=ORIENTED_EDGE('',*,*,#2211,.F.);
#3187=ORIENTED_EDGE('',*,*,#2214,.F.);
#3188=ORIENTED_EDGE('',*,*,#2217,.F.);
#3189=ORIENTED_EDGE('',*,*,#2220,.F.);
#3190=ORIENTED_EDGE('',*,*,#2223,.F.);
#3191=ORIENTED_EDGE('',*,*,#2226,.F.);
#3192=ORIENTED_EDGE('',*,*,#2234,.F.);
#3193=ORIENTED_EDGE('',*,*,#2235,.F.);
#3194=ORIENTED_EDGE('',*,*,#2047,.F.);
#3195=ORIENTED_EDGE('',*,*,#2051,.F.);
#3196=ORIENTED_EDGE('',*,*,#2054,.F.);
#3197=ORIENTED_EDGE('',*,*,#2057,.F.);
#3198=ORIENTED_EDGE('',*,*,#2060,.F.);
#3199=ORIENTED_EDGE('',*,*,#2063,.F.);
#3200=ORIENTED_EDGE('',*,*,#2066,.F.);
#3201=ORIENTED_EDGE('',*,*,#2069,.F.);
#3202=ORIENTED_EDGE('',*,*,#2072,.F.);
#3203=ORIENTED_EDGE('',*,*,#2075,.F.);
#3204=ORIENTED_EDGE('',*,*,#2078,.F.);
#3205=ORIENTED_EDGE('',*,*,#2081,.F.);
#3206=ORIENTED_EDGE('',*,*,#2084,.F.);
#3207=ORIENTED_EDGE('',*,*,#2087,.F.);
#3208=ORIENTED_EDGE('',*,*,#2090,.F.);
#3209=ORIENTED_EDGE('',*,*,#2093,.F.);
#3210=ORIENTED_EDGE('',*,*,#2096,.F.);
#3211=ORIENTED_EDGE('',*,*,#2099,.F.);
#3212=ORIENTED_EDGE('',*,*,#2102,.F.);
#3213=ORIENTED_EDGE('',*,*,#2105,.F.);
#3214=ORIENTED_EDGE('',*,*,#2108,.F.);
#3215=ORIENTED_EDGE('',*,*,#2111,.F.);
#3216=ORIENTED_EDGE('',*,*,#2114,.F.);
#3217=ORIENTED_EDGE('',*,*,#2117,.F.);
#3218=ORIENTED_EDGE('',*,*,#2120,.F.);
#3219=ORIENTED_EDGE('',*,*,#2123,.F.);
#3220=ORIENTED_EDGE('',*,*,#2126,.F.);
#3221=ORIENTED_EDGE('',*,*,#2129,.F.);
#3222=ORIENTED_EDGE('',*,*,#2132,.F.);
#3223=ORIENTED_EDGE('',*,*,#2135,.F.);
#3224=ORIENTED_EDGE('',*,*,#2236,.F.);
#3225=ORIENTED_EDGE('',*,*,#2225,.T.);
#3226=ORIENTED_EDGE('',*,*,#2237,.F.);
#3227=ORIENTED_EDGE('',*,*,#2238,.F.);
#3228=ORIENTED_EDGE('',*,*,#2234,.T.);
#3229=ORIENTED_EDGE('',*,*,#2228,.T.);
#3230=ORIENTED_EDGE('',*,*,#2231,.T.);
#3231=ORIENTED_EDGE('',*,*,#2239,.F.);
#3232=ORIENTED_EDGE('',*,*,#2136,.F.);
#3233=ORIENTED_EDGE('',*,*,#2133,.F.);
#3234=ORIENTED_EDGE('',*,*,#2130,.F.);
#3235=ORIENTED_EDGE('',*,*,#2127,.F.);
#3236=ORIENTED_EDGE('',*,*,#2124,.F.);
#3237=ORIENTED_EDGE('',*,*,#2121,.F.);
#3238=ORIENTED_EDGE('',*,*,#2118,.F.);
#3239=ORIENTED_EDGE('',*,*,#2115,.F.);
#3240=ORIENTED_EDGE('',*,*,#2112,.F.);
#3241=ORIENTED_EDGE('',*,*,#2109,.F.);
#3242=ORIENTED_EDGE('',*,*,#2106,.F.);
#3243=ORIENTED_EDGE('',*,*,#2103,.F.);
#3244=ORIENTED_EDGE('',*,*,#2100,.F.);
#3245=ORIENTED_EDGE('',*,*,#2097,.F.);
#3246=ORIENTED_EDGE('',*,*,#2094,.F.);
#3247=ORIENTED_EDGE('',*,*,#2091,.F.);
#3248=ORIENTED_EDGE('',*,*,#2088,.F.);
#3249=ORIENTED_EDGE('',*,*,#2085,.F.);
#3250=ORIENTED_EDGE('',*,*,#2082,.F.);
#3251=ORIENTED_EDGE('',*,*,#2079,.F.);
#3252=ORIENTED_EDGE('',*,*,#2076,.F.);
#3253=ORIENTED_EDGE('',*,*,#2073,.F.);
#3254=ORIENTED_EDGE('',*,*,#2070,.F.);
#3255=ORIENTED_EDGE('',*,*,#2067,.F.);
#3256=ORIENTED_EDGE('',*,*,#2064,.F.);
#3257=ORIENTED_EDGE('',*,*,#2061,.F.);
#3258=ORIENTED_EDGE('',*,*,#2058,.F.);
#3259=ORIENTED_EDGE('',*,*,#2055,.F.);
#3260=ORIENTED_EDGE('',*,*,#2052,.F.);
#3261=ORIENTED_EDGE('',*,*,#2049,.F.);
#3262=ORIENTED_EDGE('',*,*,#2240,.F.);
#3263=ORIENTED_EDGE('',*,*,#2237,.T.);
#3264=ORIENTED_EDGE('',*,*,#2227,.T.);
#3265=ORIENTED_EDGE('',*,*,#2224,.T.);
#3266=ORIENTED_EDGE('',*,*,#2221,.T.);
#3267=ORIENTED_EDGE('',*,*,#2218,.T.);
#3268=ORIENTED_EDGE('',*,*,#2215,.T.);
#3269=ORIENTED_EDGE('',*,*,#2212,.T.);
#3270=ORIENTED_EDGE('',*,*,#2209,.T.);
#3271=ORIENTED_EDGE('',*,*,#2206,.T.);
#3272=ORIENTED_EDGE('',*,*,#2203,.T.);
#3273=ORIENTED_EDGE('',*,*,#2200,.T.);
#3274=ORIENTED_EDGE('',*,*,#2197,.T.);
#3275=ORIENTED_EDGE('',*,*,#2194,.T.);
#3276=ORIENTED_EDGE('',*,*,#2191,.T.);
#3277=ORIENTED_EDGE('',*,*,#2188,.T.);
#3278=ORIENTED_EDGE('',*,*,#2185,.T.);
#3279=ORIENTED_EDGE('',*,*,#2182,.T.);
#3280=ORIENTED_EDGE('',*,*,#2179,.T.);
#3281=ORIENTED_EDGE('',*,*,#2176,.T.);
#3282=ORIENTED_EDGE('',*,*,#2173,.T.);
#3283=ORIENTED_EDGE('',*,*,#2170,.T.);
#3284=ORIENTED_EDGE('',*,*,#2167,.T.);
#3285=ORIENTED_EDGE('',*,*,#2164,.T.);
#3286=ORIENTED_EDGE('',*,*,#2161,.T.);
#3287=ORIENTED_EDGE('',*,*,#2158,.T.);
#3288=ORIENTED_EDGE('',*,*,#2155,.T.);
#3289=ORIENTED_EDGE('',*,*,#2152,.T.);
#3290=ORIENTED_EDGE('',*,*,#2149,.T.);
#3291=ORIENTED_EDGE('',*,*,#2146,.T.);
#3292=ORIENTED_EDGE('',*,*,#2143,.T.);
#3293=ORIENTED_EDGE('',*,*,#2140,.T.);
#3294=ORIENTED_EDGE('',*,*,#2134,.T.);
#3295=ORIENTED_EDGE('',*,*,#2239,.T.);
#3296=ORIENTED_EDGE('',*,*,#2230,.T.);
#3297=ORIENTED_EDGE('',*,*,#2236,.T.);
#3298=ORIENTED_EDGE('',*,*,#2241,.F.);
#3299=ORIENTED_EDGE('',*,*,#2242,.T.);
#3300=ORIENTED_EDGE('',*,*,#2243,.T.);
#3301=ORIENTED_EDGE('',*,*,#2244,.F.);
#3302=ORIENTED_EDGE('',*,*,#2245,.F.);
#3303=ORIENTED_EDGE('',*,*,#2246,.T.);
#3304=ORIENTED_EDGE('',*,*,#2247,.T.);
#3305=ORIENTED_EDGE('',*,*,#2242,.F.);
#3306=ORIENTED_EDGE('',*,*,#2248,.F.);
#3307=ORIENTED_EDGE('',*,*,#2249,.T.);
#3308=ORIENTED_EDGE('',*,*,#2250,.T.);
#3309=ORIENTED_EDGE('',*,*,#2246,.F.);
#3310=ORIENTED_EDGE('',*,*,#2251,.F.);
#3311=ORIENTED_EDGE('',*,*,#2252,.T.);
#3312=ORIENTED_EDGE('',*,*,#2253,.T.);
#3313=ORIENTED_EDGE('',*,*,#2249,.F.);
#3314=ORIENTED_EDGE('',*,*,#2254,.F.);
#3315=ORIENTED_EDGE('',*,*,#2255,.T.);
#3316=ORIENTED_EDGE('',*,*,#2256,.T.);
#3317=ORIENTED_EDGE('',*,*,#2252,.F.);
#3318=ORIENTED_EDGE('',*,*,#2257,.F.);
#3319=ORIENTED_EDGE('',*,*,#2244,.T.);
#3320=ORIENTED_EDGE('',*,*,#2258,.T.);
#3321=ORIENTED_EDGE('',*,*,#2255,.F.);
#3322=ORIENTED_EDGE('',*,*,#2258,.F.);
#3323=ORIENTED_EDGE('',*,*,#2243,.F.);
#3324=ORIENTED_EDGE('',*,*,#2247,.F.);
#3325=ORIENTED_EDGE('',*,*,#2250,.F.);
#3326=ORIENTED_EDGE('',*,*,#2253,.F.);
#3327=ORIENTED_EDGE('',*,*,#2256,.F.);
#3328=ORIENTED_EDGE('',*,*,#2259,.T.);
#3329=ORIENTED_EDGE('',*,*,#2235,.T.);
#3330=ORIENTED_EDGE('',*,*,#2238,.T.);
#3331=ORIENTED_EDGE('',*,*,#2240,.T.);
#3332=ORIENTED_EDGE('',*,*,#2048,.F.);
#3333=ORIENTED_EDGE('',*,*,#2259,.F.);
#3334=ORIENTED_EDGE('',*,*,#2260,.T.);
#3335=ORIENTED_EDGE('',*,*,#2261,.T.);
#3336=ORIENTED_EDGE('',*,*,#2260,.F.);
#3337=ORIENTED_EDGE('',*,*,#2261,.F.);
#3338=ORIENTED_EDGE('',*,*,#2241,.T.);
#3339=ORIENTED_EDGE('',*,*,#2257,.T.);
#3340=ORIENTED_EDGE('',*,*,#2254,.T.);
#3341=ORIENTED_EDGE('',*,*,#2251,.T.);
#3342=ORIENTED_EDGE('',*,*,#2248,.T.);
#3343=ORIENTED_EDGE('',*,*,#2245,.T.);
#3344=ORIENTED_EDGE('',*,*,#2233,.T.);
#3429=CYLINDRICAL_SURFACE('',#3942,2.4505);
#3430=CYLINDRICAL_SURFACE('',#3944,2.4505);
#3431=CYLINDRICAL_SURFACE('',#3945,2.4505);
#3432=CYLINDRICAL_SURFACE('',#3946,2.4505);
#3433=CYLINDRICAL_SURFACE('',#3947,2.4505);
#3434=CYLINDRICAL_SURFACE('',#3948,2.4505);
#3435=CYLINDRICAL_SURFACE('',#3949,2.4505);
#3436=CYLINDRICAL_SURFACE('',#3950,2.4505);
#3437=CYLINDRICAL_SURFACE('',#3951,2.4505);
#3438=CYLINDRICAL_SURFACE('',#3952,2.4505);
#3439=CYLINDRICAL_SURFACE('',#3953,2.4505);
#3440=CYLINDRICAL_SURFACE('',#3954,2.4505);
#3441=CYLINDRICAL_SURFACE('',#3955,2.4505);
#3442=CYLINDRICAL_SURFACE('',#3956,2.4505);
#3443=CYLINDRICAL_SURFACE('',#3957,2.4505);
#3444=CYLINDRICAL_SURFACE('',#3958,2.4505);
#3445=CYLINDRICAL_SURFACE('',#3959,2.4505);
#3446=CYLINDRICAL_SURFACE('',#3960,2.4505);
#3447=CYLINDRICAL_SURFACE('',#3961,2.4505);
#3448=CYLINDRICAL_SURFACE('',#3962,2.4505);
#3449=CYLINDRICAL_SURFACE('',#3963,2.4505);
#3450=CYLINDRICAL_SURFACE('',#3964,2.4505);
#3451=CYLINDRICAL_SURFACE('',#3965,2.4505);
#3452=CYLINDRICAL_SURFACE('',#3966,2.4505);
#3453=CYLINDRICAL_SURFACE('',#3967,2.4505);
#3454=CYLINDRICAL_SURFACE('',#3968,2.4505);
#3455=CYLINDRICAL_SURFACE('',#3969,2.4505);
#3456=CYLINDRICAL_SURFACE('',#3970,2.4505);
#3457=CYLINDRICAL_SURFACE('',#3971,2.4505);
#3458=CYLINDRICAL_SURFACE('',#3972,2.4505);
#3459=CYLINDRICAL_SURFACE('',#3973,1.99475);
#3460=CYLINDRICAL_SURFACE('',#3975,1.99475);
#3461=CYLINDRICAL_SURFACE('',#3976,1.99475);
#3462=CYLINDRICAL_SURFACE('',#3977,1.99475);
#3463=CYLINDRICAL_SURFACE('',#3978,1.99475);
#3464=CYLINDRICAL_SURFACE('',#3979,1.99475);
#3465=CYLINDRICAL_SURFACE('',#3980,1.99475);
#3466=CYLINDRICAL_SURFACE('',#3981,1.99475);
#3467=CYLINDRICAL_SURFACE('',#3982,1.99475);
#3468=CYLINDRICAL_SURFACE('',#3983,1.99475);
#3469=CYLINDRICAL_SURFACE('',#3984,1.99475);
#3470=CYLINDRICAL_SURFACE('',#3985,1.99475);
#3471=CYLINDRICAL_SURFACE('',#3986,1.99475);
#3472=CYLINDRICAL_SURFACE('',#3987,1.99475);
#3473=CYLINDRICAL_SURFACE('',#3988,1.99475);
#3474=CYLINDRICAL_SURFACE('',#3989,1.99475);
#3475=CYLINDRICAL_SURFACE('',#3990,1.99475);
#3476=CYLINDRICAL_SURFACE('',#3991,1.99475);
#3477=CYLINDRICAL_SURFACE('',#3992,1.99475);
#3478=CYLINDRICAL_SURFACE('',#3993,1.99475);
#3479=CYLINDRICAL_SURFACE('',#3994,1.99475);
#3480=CYLINDRICAL_SURFACE('',#3995,1.99475);
#3481=CYLINDRICAL_SURFACE('',#3996,1.99475);
#3482=CYLINDRICAL_SURFACE('',#3997,1.99475);
#3483=CYLINDRICAL_SURFACE('',#3998,1.99475);
#3484=CYLINDRICAL_SURFACE('',#3999,1.99475);
#3485=CYLINDRICAL_SURFACE('',#4000,1.99475);
#3486=CYLINDRICAL_SURFACE('',#4001,1.99475);
#3487=CYLINDRICAL_SURFACE('',#4002,1.99475);
#3488=CYLINDRICAL_SURFACE('',#4003,1.99475);
#3489=CYLINDRICAL_SURFACE('',#4007,1.99475);
#3490=CYLINDRICAL_SURFACE('',#4009,2.4505);
#3491=CYLINDRICAL_SURFACE('',#4019,4.);
#3615=ADVANCED_FACE('',(#539),#3429,.T.);
#3616=ADVANCED_FACE('',(#540),#3430,.T.);
#3617=ADVANCED_FACE('',(#541),#3431,.T.);
#3618=ADVANCED_FACE('',(#542),#3432,.T.);
#3619=ADVANCED_FACE('',(#543),#3433,.T.);
#3620=ADVANCED_FACE('',(#544),#3434,.T.);
#3621=ADVANCED_FACE('',(#545),#3435,.T.);
#3622=ADVANCED_FACE('',(#546),#3436,.T.);
#3623=ADVANCED_FACE('',(#547),#3437,.T.);
#3624=ADVANCED_FACE('',(#548),#3438,.T.);
#3625=ADVANCED_FACE('',(#549),#3439,.T.);
#3626=ADVANCED_FACE('',(#550),#3440,.T.);
#3627=ADVANCED_FACE('',(#551),#3441,.T.);
#3628=ADVANCED_FACE('',(#552),#3442,.T.);
#3629=ADVANCED_FACE('',(#553),#3443,.T.);
#3630=ADVANCED_FACE('',(#554),#3444,.T.);
#3631=ADVANCED_FACE('',(#555),#3445,.T.);
#3632=ADVANCED_FACE('',(#556),#3446,.T.);
#3633=ADVANCED_FACE('',(#557),#3447,.T.);
#3634=ADVANCED_FACE('',(#558),#3448,.T.);
#3635=ADVANCED_FACE('',(#559),#3449,.T.);
#3636=ADVANCED_FACE('',(#560),#3450,.T.);
#3637=ADVANCED_FACE('',(#561),#3451,.T.);
#3638=ADVANCED_FACE('',(#562),#3452,.T.);
#3639=ADVANCED_FACE('',(#563),#3453,.T.);
#3640=ADVANCED_FACE('',(#564),#3454,.T.);
#3641=ADVANCED_FACE('',(#565),#3455,.T.);
#3642=ADVANCED_FACE('',(#566),#3456,.T.);
#3643=ADVANCED_FACE('',(#567),#3457,.T.);
#3644=ADVANCED_FACE('',(#568),#3458,.T.);
#3645=ADVANCED_FACE('',(#569),#3459,.T.);
#3646=ADVANCED_FACE('',(#570),#3460,.T.);
#3647=ADVANCED_FACE('',(#571),#3461,.T.);
#3648=ADVANCED_FACE('',(#572),#3462,.T.);
#3649=ADVANCED_FACE('',(#573),#3463,.T.);
#3650=ADVANCED_FACE('',(#574),#3464,.T.);
#3651=ADVANCED_FACE('',(#575),#3465,.T.);
#3652=ADVANCED_FACE('',(#576),#3466,.T.);
#3653=ADVANCED_FACE('',(#577),#3467,.T.);
#3654=ADVANCED_FACE('',(#578),#3468,.T.);
#3655=ADVANCED_FACE('',(#579),#3469,.T.);
#3656=ADVANCED_FACE('',(#580),#3470,.T.);
#3657=ADVANCED_FACE('',(#581),#3471,.T.);
#3658=ADVANCED_FACE('',(#582),#3472,.T.);
#3659=ADVANCED_FACE('',(#583),#3473,.T.);
#3660=ADVANCED_FACE('',(#584),#3474,.T.);
#3661=ADVANCED_FACE('',(#585),#3475,.T.);
#3662=ADVANCED_FACE('',(#586),#3476,.T.);
#3663=ADVANCED_FACE('',(#587),#3477,.T.);
#3664=ADVANCED_FACE('',(#588),#3478,.T.);
#3665=ADVANCED_FACE('',(#589),#3479,.T.);
#3666=ADVANCED_FACE('',(#590),#3480,.T.);
#3667=ADVANCED_FACE('',(#591),#3481,.T.);
#3668=ADVANCED_FACE('',(#592),#3482,.T.);
#3669=ADVANCED_FACE('',(#593),#3483,.T.);
#3670=ADVANCED_FACE('',(#594),#3484,.T.);
#3671=ADVANCED_FACE('',(#595),#3485,.T.);
#3672=ADVANCED_FACE('',(#596),#3486,.T.);
#3673=ADVANCED_FACE('',(#597),#3487,.T.);
#3674=ADVANCED_FACE('',(#598),#3488,.T.);
#3675=ADVANCED_FACE('',(#599),#55,.T.);
#3676=ADVANCED_FACE('',(#600),#60,.F.);
#3677=ADVANCED_FACE('',(#601),#3489,.T.);
#3678=ADVANCED_FACE('',(#602),#61,.F.);
#3679=ADVANCED_FACE('',(#603),#3490,.T.);
#3680=ADVANCED_FACE('',(#604),#405,.F.);
#3681=ADVANCED_FACE('',(#605),#406,.F.);
#3682=ADVANCED_FACE('',(#606),#407,.F.);
#3683=ADVANCED_FACE('',(#607),#408,.F.);
#3684=ADVANCED_FACE('',(#608),#409,.F.);
#3685=ADVANCED_FACE('',(#609),#410,.F.);
#3686=ADVANCED_FACE('',(#610),#411,.F.);
#3687=ADVANCED_FACE('',(#611,#363),#412,.T.);
#3688=ADVANCED_FACE('',(#612),#3491,.T.);
#3689=ADVANCED_FACE('',(#613,#364),#413,.F.);
#3690=ADVANCED_FACE('',(#614),#414,.T.);
#3698=CLOSED_SHELL('',(#3615,#3616,#3617,#3618,#3619,#3620,#3621,#3622,
#3623,#3624,#3625,#3626,#3627,#3628,#3629,#3630,#3631,#3632,#3633,#3634,
#3635,#3636,#3637,#3638,#3639,#3640,#3641,#3642,#3643,#3644,#3645,#3646,
#3647,#3648,#3649,#3650,#3651,#3652,#3653,#3654,#3655,#3656,#3657,#3658,
#3659,#3660,#3661,#3662,#3663,#3664,#3665,#3666,#3667,#3668,#3669,#3670,
#3671,#3672,#3673,#3674,#3675,#3676,#3677,#3678,#3679,#3680,#3681,#3682,
#3683,#3684,#3685,#3686,#3687,#3688,#3689,#3690));
#3941=AXIS2_PLACEMENT_3D('',#9395,#4536,#4537);
#3942=AXIS2_PLACEMENT_3D('',#9396,#4538,#4539);
#3943=AXIS2_PLACEMENT_3D('',#9412,#4541,#4542);
#3944=AXIS2_PLACEMENT_3D('',#9420,#4543,#4544);
#3945=AXIS2_PLACEMENT_3D('',#9468,#4546,#4547);
#3946=AXIS2_PLACEMENT_3D('',#9516,#4549,#4550);
#3947=AXIS2_PLACEMENT_3D('',#9570,#4552,#4553);
#3948=AXIS2_PLACEMENT_3D('',#9618,#4555,#4556);
#3949=AXIS2_PLACEMENT_3D('',#9666,#4558,#4559);
#3950=AXIS2_PLACEMENT_3D('',#9714,#4561,#4562);
#3951=AXIS2_PLACEMENT_3D('',#9768,#4564,#4565);
#3952=AXIS2_PLACEMENT_3D('',#9816,#4567,#4568);
#3953=AXIS2_PLACEMENT_3D('',#9864,#4570,#4571);
#3954=AXIS2_PLACEMENT_3D('',#9918,#4573,#4574);
#3955=AXIS2_PLACEMENT_3D('',#9966,#4576,#4577);
#3956=AXIS2_PLACEMENT_3D('',#10014,#4579,#4580);
#3957=AXIS2_PLACEMENT_3D('',#10065,#4582,#4583);
#3958=AXIS2_PLACEMENT_3D('',#10113,#4585,#4586);
#3959=AXIS2_PLACEMENT_3D('',#10161,#4588,#4589);
#3960=AXIS2_PLACEMENT_3D('',#10209,#4591,#4592);
#3961=AXIS2_PLACEMENT_3D('',#10263,#4594,#4595);
#3962=AXIS2_PLACEMENT_3D('',#10311,#4597,#4598);
#3963=AXIS2_PLACEMENT_3D('',#10359,#4600,#4601);
#3964=AXIS2_PLACEMENT_3D('',#10413,#4603,#4604);
#3965=AXIS2_PLACEMENT_3D('',#10461,#4606,#4607);
#3966=AXIS2_PLACEMENT_3D('',#10509,#4609,#4610);
#3967=AXIS2_PLACEMENT_3D('',#10560,#4612,#4613);
#3968=AXIS2_PLACEMENT_3D('',#10611,#4615,#4616);
#3969=AXIS2_PLACEMENT_3D('',#10659,#4618,#4619);
#3970=AXIS2_PLACEMENT_3D('',#10707,#4621,#4622);
#3971=AXIS2_PLACEMENT_3D('',#10761,#4624,#4625);
#3972=AXIS2_PLACEMENT_3D('',#10809,#4627,#4628);
#3973=AXIS2_PLACEMENT_3D('',#10857,#4630,#4631);
#3974=AXIS2_PLACEMENT_3D('',#10873,#4633,#4634);
#3975=AXIS2_PLACEMENT_3D('',#10882,#4635,#4636);
#3976=AXIS2_PLACEMENT_3D('',#10907,#4638,#4639);
#3977=AXIS2_PLACEMENT_3D('',#10931,#4641,#4642);
#3978=AXIS2_PLACEMENT_3D('',#10956,#4644,#4645);
#3979=AXIS2_PLACEMENT_3D('',#10981,#4647,#4648);
#3980=AXIS2_PLACEMENT_3D('',#11005,#4650,#4651);
#3981=AXIS2_PLACEMENT_3D('',#11029,#4653,#4654);
#3982=AXIS2_PLACEMENT_3D('',#11055,#4656,#4657);
#3983=AXIS2_PLACEMENT_3D('',#11079,#4659,#4660);
#3984=AXIS2_PLACEMENT_3D('',#11103,#4662,#4663);
#3985=AXIS2_PLACEMENT_3D('',#11128,#4665,#4666);
#3986=AXIS2_PLACEMENT_3D('',#11153,#4668,#4669);
#3987=AXIS2_PLACEMENT_3D('',#11177,#4671,#4672);
#3988=AXIS2_PLACEMENT_3D('',#11202,#4674,#4675);
#3989=AXIS2_PLACEMENT_3D('',#11227,#4677,#4678);
#3990=AXIS2_PLACEMENT_3D('',#11251,#4680,#4681);
#3991=AXIS2_PLACEMENT_3D('',#11275,#4683,#4684);
#3992=AXIS2_PLACEMENT_3D('',#11301,#4686,#4687);
#3993=AXIS2_PLACEMENT_3D('',#11325,#4689,#4690);
#3994=AXIS2_PLACEMENT_3D('',#11349,#4692,#4693);
#3995=AXIS2_PLACEMENT_3D('',#11374,#4695,#4696);
#3996=AXIS2_PLACEMENT_3D('',#11399,#4698,#4699);
#3997=AXIS2_PLACEMENT_3D('',#11423,#4701,#4702);
#3998=AXIS2_PLACEMENT_3D('',#11448,#4704,#4705);
#3999=AXIS2_PLACEMENT_3D('',#11473,#4707,#4708);
#4000=AXIS2_PLACEMENT_3D('',#11497,#4710,#4711);
#4001=AXIS2_PLACEMENT_3D('',#11521,#4713,#4714);
#4002=AXIS2_PLACEMENT_3D('',#11546,#4716,#4717);
#4003=AXIS2_PLACEMENT_3D('',#11571,#4719,#4720);
#4004=AXIS2_PLACEMENT_3D('',#11595,#4722,#4723);
#4005=AXIS2_PLACEMENT_3D('',#11874,#4724,#4725);
#4006=AXIS2_PLACEMENT_3D('',#11905,#4727,#4728);
#4007=AXIS2_PLACEMENT_3D('',#12806,#4729,#4730);
#4008=AXIS2_PLACEMENT_3D('',#12817,#4731,#4732);
#4009=AXIS2_PLACEMENT_3D('',#13717,#4733,#4734);
#4010=AXIS2_PLACEMENT_3D('',#13718,#4735,#4736);
#4011=AXIS2_PLACEMENT_3D('',#13727,#4741,#4742);
#4012=AXIS2_PLACEMENT_3D('',#13733,#4746,#4747);
#4013=AXIS2_PLACEMENT_3D('',#13739,#4751,#4752);
#4014=AXIS2_PLACEMENT_3D('',#13745,#4756,#4757);
#4015=AXIS2_PLACEMENT_3D('',#13751,#4761,#4762);
#4016=AXIS2_PLACEMENT_3D('',#13754,#4765,#4766);
#4017=AXIS2_PLACEMENT_3D('',#13755,#4767,#4768);
#4018=AXIS2_PLACEMENT_3D('',#13757,#4769,#4770);
#4019=AXIS2_PLACEMENT_3D('',#13758,#4771,#4772);
#4020=AXIS2_PLACEMENT_3D('',#13761,#4774,#4775);
#4021=AXIS2_PLACEMENT_3D('',#13762,#4776,#4777);
#4022=AXIS2_PLACEMENT_3D('',#13763,#4778,#4779);
#4536=DIRECTION('axis',(0.,0.,1.));
#4537=DIRECTION('refdir',(1.,0.,0.));
#4538=DIRECTION('center_axis',(0.,0.,1.));
#4539=DIRECTION('ref_axis',(1.,0.,0.));
#4540=DIRECTION('',(0.,0.,-1.));
#4541=DIRECTION('center_axis',(0.,0.,-1.));
#4542=DIRECTION('ref_axis',(1.,0.,0.));
#4543=DIRECTION('center_axis',(0.,0.,1.));
#4544=DIRECTION('ref_axis',(1.,0.,0.));
#4545=DIRECTION('',(0.,0.,-1.));
#4546=DIRECTION('center_axis',(0.,0.,1.));
#4547=DIRECTION('ref_axis',(1.,0.,0.));
#4548=DIRECTION('',(0.,0.,-1.));
#4549=DIRECTION('center_axis',(0.,0.,1.));
#4550=DIRECTION('ref_axis',(1.,0.,0.));
#4551=DIRECTION('',(0.,0.,-1.));
#4552=DIRECTION('center_axis',(0.,0.,1.));
#4553=DIRECTION('ref_axis',(1.,0.,0.));
#4554=DIRECTION('',(0.,0.,-1.));
#4555=DIRECTION('center_axis',(0.,0.,1.));
#4556=DIRECTION('ref_axis',(1.,0.,0.));
#4557=DIRECTION('',(0.,0.,-1.));
#4558=DIRECTION('center_axis',(0.,0.,1.));
#4559=DIRECTION('ref_axis',(1.,0.,0.));
#4560=DIRECTION('',(0.,0.,-1.));
#4561=DIRECTION('center_axis',(0.,0.,1.));
#4562=DIRECTION('ref_axis',(1.,0.,0.));
#4563=DIRECTION('',(0.,0.,-1.));
#4564=DIRECTION('center_axis',(0.,0.,1.));
#4565=DIRECTION('ref_axis',(1.,0.,0.));
#4566=DIRECTION('',(0.,0.,-1.));
#4567=DIRECTION('center_axis',(0.,0.,1.));
#4568=DIRECTION('ref_axis',(1.,0.,0.));
#4569=DIRECTION('',(0.,0.,-1.));
#4570=DIRECTION('center_axis',(0.,0.,1.));
#4571=DIRECTION('ref_axis',(1.,0.,0.));
#4572=DIRECTION('',(0.,0.,-1.));
#4573=DIRECTION('center_axis',(0.,0.,1.));
#4574=DIRECTION('ref_axis',(1.,0.,0.));
#4575=DIRECTION('',(0.,0.,-1.));
#4576=DIRECTION('center_axis',(0.,0.,1.));
#4577=DIRECTION('ref_axis',(1.,0.,0.));
#4578=DIRECTION('',(0.,0.,-1.));
#4579=DIRECTION('center_axis',(0.,0.,1.));
#4580=DIRECTION('ref_axis',(1.,0.,0.));
#4581=DIRECTION('',(0.,0.,-1.));
#4582=DIRECTION('center_axis',(0.,0.,1.));
#4583=DIRECTION('ref_axis',(1.,0.,0.));
#4584=DIRECTION('',(0.,0.,-1.));
#4585=DIRECTION('center_axis',(0.,0.,1.));
#4586=DIRECTION('ref_axis',(1.,0.,0.));
#4587=DIRECTION('',(0.,0.,-1.));
#4588=DIRECTION('center_axis',(0.,0.,1.));
#4589=DIRECTION('ref_axis',(1.,0.,0.));
#4590=DIRECTION('',(0.,0.,-1.));
#4591=DIRECTION('center_axis',(0.,0.,1.));
#4592=DIRECTION('ref_axis',(1.,0.,0.));
#4593=DIRECTION('',(0.,0.,-1.));
#4594=DIRECTION('center_axis',(0.,0.,1.));
#4595=DIRECTION('ref_axis',(1.,0.,0.));
#4596=DIRECTION('',(0.,0.,-1.));
#4597=DIRECTION('center_axis',(0.,0.,1.));
#4598=DIRECTION('ref_axis',(1.,0.,0.));
#4599=DIRECTION('',(0.,0.,-1.));
#4600=DIRECTION('center_axis',(0.,0.,1.));
#4601=DIRECTION('ref_axis',(1.,0.,0.));
#4602=DIRECTION('',(0.,0.,-1.));
#4603=DIRECTION('center_axis',(0.,0.,1.));
#4604=DIRECTION('ref_axis',(1.,0.,0.));
#4605=DIRECTION('',(0.,0.,-1.));
#4606=DIRECTION('center_axis',(0.,0.,1.));
#4607=DIRECTION('ref_axis',(1.,0.,0.));
#4608=DIRECTION('',(0.,0.,-1.));
#4609=DIRECTION('center_axis',(0.,0.,1.));
#4610=DIRECTION('ref_axis',(1.,0.,0.));
#4611=DIRECTION('',(0.,0.,-1.));
#4612=DIRECTION('center_axis',(0.,0.,1.));
#4613=DIRECTION('ref_axis',(1.,0.,0.));
#4614=DIRECTION('',(0.,0.,-1.));
#4615=DIRECTION('center_axis',(0.,0.,1.));
#4616=DIRECTION('ref_axis',(1.,0.,0.));
#4617=DIRECTION('',(0.,0.,-1.));
#4618=DIRECTION('center_axis',(0.,0.,1.));
#4619=DIRECTION('ref_axis',(1.,0.,0.));
#4620=DIRECTION('',(0.,0.,-1.));
#4621=DIRECTION('center_axis',(0.,0.,1.));
#4622=DIRECTION('ref_axis',(1.,0.,0.));
#4623=DIRECTION('',(0.,0.,-1.));
#4624=DIRECTION('center_axis',(0.,0.,1.));
#4625=DIRECTION('ref_axis',(1.,0.,0.));
#4626=DIRECTION('',(0.,0.,-1.));
#4627=DIRECTION('center_axis',(0.,0.,1.));
#4628=DIRECTION('ref_axis',(1.,0.,0.));
#4629=DIRECTION('',(0.,0.,-1.));
#4630=DIRECTION('center_axis',(0.,0.,1.));
#4631=DIRECTION('ref_axis',(0.99808566179124,-0.0618466791892788,0.));
#4632=DIRECTION('',(0.,0.,1.));
#4633=DIRECTION('center_axis',(0.,0.,-1.));
#4634=DIRECTION('ref_axis',(1.,-2.02644595590483E-13,0.));
#4635=DIRECTION('center_axis',(0.,0.,1.));
#4636=DIRECTION('ref_axis',(1.,-2.02644595590483E-13,0.));
#4637=DIRECTION('',(0.,0.,1.));
#4638=DIRECTION('center_axis',(0.,0.,1.));
#4639=DIRECTION('ref_axis',(1.,-2.02644595590483E-13,0.));
#4640=DIRECTION('',(0.,0.,1.));
#4641=DIRECTION('center_axis',(0.,0.,1.));
#4642=DIRECTION('ref_axis',(1.,-2.02644595590483E-13,0.));
#4643=DIRECTION('',(0.,0.,1.));
#4644=DIRECTION('center_axis',(0.,0.,1.));
#4645=DIRECTION('ref_axis',(1.,-2.02644595590483E-13,0.));
#4646=DIRECTION('',(0.,0.,1.));
#4647=DIRECTION('center_axis',(0.,0.,1.));
#4648=DIRECTION('ref_axis',(1.,-2.02644595590483E-13,0.));
#4649=DIRECTION('',(0.,0.,1.));
#4650=DIRECTION('center_axis',(0.,0.,1.));
#4651=DIRECTION('ref_axis',(1.,-2.02644595590483E-13,0.));
#4652=DIRECTION('',(0.,0.,1.));
#4653=DIRECTION('center_axis',(0.,0.,1.));
#4654=DIRECTION('ref_axis',(1.,-2.02644595590483E-13,0.));
#4655=DIRECTION('',(0.,0.,1.));
#4656=DIRECTION('center_axis',(0.,0.,1.));
#4657=DIRECTION('ref_axis',(1.,-2.02644595590483E-13,0.));
#4658=DIRECTION('',(0.,0.,1.));
#4659=DIRECTION('center_axis',(0.,0.,1.));
#4660=DIRECTION('ref_axis',(1.,-2.02644595590483E-13,0.));
#4661=DIRECTION('',(0.,0.,1.));
#4662=DIRECTION('center_axis',(0.,0.,1.));
#4663=DIRECTION('ref_axis',(1.,-2.02644595590483E-13,0.));
#4664=DIRECTION('',(0.,0.,1.));
#4665=DIRECTION('center_axis',(0.,0.,1.));
#4666=DIRECTION('ref_axis',(1.,-2.02644595590483E-13,0.));
#4667=DIRECTION('',(0.,0.,1.));
#4668=DIRECTION('center_axis',(0.,0.,1.));
#4669=DIRECTION('ref_axis',(1.,-2.02644595590483E-13,0.));
#4670=DIRECTION('',(0.,0.,1.));
#4671=DIRECTION('center_axis',(0.,0.,1.));
#4672=DIRECTION('ref_axis',(1.,-2.02644595590483E-13,0.));
#4673=DIRECTION('',(0.,0.,1.));
#4674=DIRECTION('center_axis',(0.,0.,1.));
#4675=DIRECTION('ref_axis',(1.,-2.02644595590483E-13,0.));
#4676=DIRECTION('',(0.,0.,1.));
#4677=DIRECTION('center_axis',(0.,0.,1.));
#4678=DIRECTION('ref_axis',(1.,-2.02644595590483E-13,0.));
#4679=DIRECTION('',(0.,0.,1.));
#4680=DIRECTION('center_axis',(0.,0.,1.));
#4681=DIRECTION('ref_axis',(1.,-2.02644595590483E-13,0.));
#4682=DIRECTION('',(0.,0.,1.));
#4683=DIRECTION('center_axis',(0.,0.,1.));
#4684=DIRECTION('ref_axis',(1.,-2.02644595590483E-13,0.));
#4685=DIRECTION('',(0.,0.,1.));
#4686=DIRECTION('center_axis',(0.,0.,1.));
#4687=DIRECTION('ref_axis',(1.,-2.02644595590483E-13,0.));
#4688=DIRECTION('',(0.,0.,1.));
#4689=DIRECTION('center_axis',(0.,0.,1.));
#4690=DIRECTION('ref_axis',(1.,-2.02644595590483E-13,0.));
#4691=DIRECTION('',(0.,0.,1.));
#4692=DIRECTION('center_axis',(0.,0.,1.));
#4693=DIRECTION('ref_axis',(1.,-2.02644595590483E-13,0.));
#4694=DIRECTION('',(0.,0.,1.));
#4695=DIRECTION('center_axis',(0.,0.,1.));
#4696=DIRECTION('ref_axis',(1.,-2.02644595590483E-13,0.));
#4697=DIRECTION('',(0.,0.,1.));
#4698=DIRECTION('center_axis',(0.,0.,1.));
#4699=DIRECTION('ref_axis',(1.,-2.02644595590483E-13,0.));
#4700=DIRECTION('',(0.,0.,1.));
#4701=DIRECTION('center_axis',(0.,0.,1.));
#4702=DIRECTION('ref_axis',(1.,-2.02644595590483E-13,0.));
#4703=DIRECTION('',(0.,0.,1.));
#4704=DIRECTION('center_axis',(0.,0.,1.));
#4705=DIRECTION('ref_axis',(1.,-2.02644595590483E-13,0.));
#4706=DIRECTION('',(0.,0.,1.));
#4707=DIRECTION('center_axis',(0.,0.,1.));
#4708=DIRECTION('ref_axis',(1.,-2.02644595590483E-13,0.));
#4709=DIRECTION('',(0.,0.,1.));
#4710=DIRECTION('center_axis',(0.,0.,1.));
#4711=DIRECTION('ref_axis',(1.,-2.02644595590483E-13,0.));
#4712=DIRECTION('',(0.,0.,1.));
#4713=DIRECTION('center_axis',(0.,0.,1.));
#4714=DIRECTION('ref_axis',(1.,-2.02644595590483E-13,0.));
#4715=DIRECTION('',(0.,0.,1.));
#4716=DIRECTION('center_axis',(0.,0.,1.));
#4717=DIRECTION('ref_axis',(1.,-2.02644595590483E-13,0.));
#4718=DIRECTION('',(0.,0.,1.));
#4719=DIRECTION('center_axis',(0.,0.,1.));
#4720=DIRECTION('ref_axis',(1.,-2.02644595590483E-13,0.));
#4721=DIRECTION('',(0.,0.,1.));
#4722=DIRECTION('center_axis',(0.,0.,-1.));
#4723=DIRECTION('ref_axis',(1.,0.,0.));
#4724=DIRECTION('center_axis',(0.,0.,-1.));
#4725=DIRECTION('ref_axis',(1.,0.,0.));
#4726=DIRECTION('',(0.707106781186547,8.65956056235493E-17,0.707106781186548));
#4727=DIRECTION('center_axis',(0.,0.,1.));
#4728=DIRECTION('ref_axis',(1.,0.,0.));
#4729=DIRECTION('center_axis',(0.,0.,1.));
#4730=DIRECTION('ref_axis',(1.,-2.02644595590483E-13,0.));
#4731=DIRECTION('center_axis',(0.,0.,-1.));
#4732=DIRECTION('ref_axis',(1.,-2.02644595590483E-13,0.));
#4733=DIRECTION('center_axis',(0.,0.,1.));
#4734=DIRECTION('ref_axis',(1.,0.,0.));
#4735=DIRECTION('center_axis',(-2.40370335797945E-16,-1.,0.));
#4736=DIRECTION('ref_axis',(1.,-2.40370335797945E-16,0.));
#4737=DIRECTION('',(1.,-2.40370335797945E-16,0.));
#4738=DIRECTION('',(0.,0.,1.));
#4739=DIRECTION('',(1.,-2.40370335797945E-16,0.));
#4740=DIRECTION('',(0.,0.,1.));
#4741=DIRECTION('center_axis',(-0.866025403784439,-0.5,0.));
#4742=DIRECTION('ref_axis',(0.5,-0.866025403784439,0.));
#4743=DIRECTION('',(0.5,-0.866025403784439,0.));
#4744=DIRECTION('',(0.,0.,1.));
#4745=DIRECTION('',(0.5,-0.866025403784439,0.));
#4746=DIRECTION('center_axis',(-0.866025403784439,0.5,0.));
#4747=DIRECTION('ref_axis',(-0.5,-0.866025403784439,0.));
#4748=DIRECTION('',(-0.5,-0.866025403784439,0.));
#4749=DIRECTION('',(0.,0.,1.));
#4750=DIRECTION('',(-0.5,-0.866025403784439,0.));
#4751=DIRECTION('center_axis',(1.20185167898973E-16,1.,0.));
#4752=DIRECTION('ref_axis',(-1.,1.20185167898973E-16,0.));
#4753=DIRECTION('',(-1.,1.20185167898973E-16,0.));
#4754=DIRECTION('',(0.,0.,1.));
#4755=DIRECTION('',(-1.,1.20185167898973E-16,0.));
#4756=DIRECTION('center_axis',(0.866025403784439,0.5,0.));
#4757=DIRECTION('ref_axis',(-0.5,0.866025403784439,0.));
#4758=DIRECTION('',(-0.5,0.866025403784439,0.));
#4759=DIRECTION('',(0.,0.,1.));
#4760=DIRECTION('',(-0.5,0.866025403784439,0.));
#4761=DIRECTION('center_axis',(0.866025403784439,-0.5,0.));
#4762=DIRECTION('ref_axis',(0.5,0.866025403784439,0.));
#4763=DIRECTION('',(0.5,0.866025403784439,0.));
#4764=DIRECTION('',(0.5,0.866025403784439,0.));
#4765=DIRECTION('center_axis',(0.,0.,1.));
#4766=DIRECTION('ref_axis',(1.,0.,0.));
#4767=DIRECTION('center_axis',(0.,0.,1.));
#4768=DIRECTION('ref_axis',(1.,0.,0.));
#4769=DIRECTION('center_axis',(0.,0.,1.));
#4770=DIRECTION('ref_axis',(1.,0.,0.));
#4771=DIRECTION('center_axis',(0.,0.,1.));
#4772=DIRECTION('ref_axis',(1.,0.,0.));
#4773=DIRECTION('',(0.,0.,-1.));
#4774=DIRECTION('center_axis',(0.,0.,1.));
#4775=DIRECTION('ref_axis',(1.,0.,0.));
#4776=DIRECTION('center_axis',(0.,0.,1.));
#4777=DIRECTION('ref_axis',(1.,0.,0.));
#4778=DIRECTION('center_axis',(0.,0.,1.));
#4779=DIRECTION('ref_axis',(1.,0.,0.));
#9395=CARTESIAN_POINT('',(0.,0.,0.));
#9396=CARTESIAN_POINT('Origin',(0.,0.,0.));
#9397=CARTESIAN_POINT('',(-2.45343712965594,0.00158941762237803,0.257827496212055));
#9398=CARTESIAN_POINT('',(-2.45278840085115,0.00262419282126472,0.142172503787962));
#9399=CARTESIAN_POINT('',(-2.4505,-3.00099698131059E-16,0.));
#9400=CARTESIAN_POINT('',(1.07508846035129,2.20207516956608,0.));
#9401=CARTESIAN_POINT('Ctrl Pts',(-2.45343712965594,0.00158941762237803,
0.257827496212055));
#9402=CARTESIAN_POINT('Ctrl Pts',(-2.4540150018513,0.085172055481945,0.253469478752161));
#9403=CARTESIAN_POINT('Ctrl Pts',(-2.45011475290023,0.168696598429799,0.249111461292266));
#9404=CARTESIAN_POINT('Ctrl Pts',(-2.44155870478254,0.251737029249849,0.244753443832372));
#9405=CARTESIAN_POINT('Ctrl Pts',(-2.35846563071267,1.05819400261022,0.20243004141441));
#9406=CARTESIAN_POINT('Ctrl Pts',(-1.83625838436405,1.81899168340171,0.160106638996448));
#9407=CARTESIAN_POINT('Ctrl Pts',(-1.11361254088691,2.18710613238446,0.117783236578486));
#9408=CARTESIAN_POINT('Ctrl Pts',(-0.443253972640013,2.52858554058766,0.0785221577189908));
#9409=CARTESIAN_POINT('Ctrl Pts',(0.399586947667411,2.53215135127315,0.0392610788594954));
#9410=CARTESIAN_POINT('Ctrl Pts',(1.07765127757232,2.20530172674001,-6.18615037552163E-17));
#9411=CARTESIAN_POINT('',(-1.0750884603512,2.20207516956613,0.));
#9412=CARTESIAN_POINT('Origin',(0.,0.,0.));
#9413=CARTESIAN_POINT('Ctrl Pts',(-1.0750884603512,2.20207516956613,-4.75314232417645E-15));
#9414=CARTESIAN_POINT('Ctrl Pts',(-1.8073457627734,1.84457539538852,0.042339106641334));
#9415=CARTESIAN_POINT('Ctrl Pts',(-2.34095039172362,1.09624395863826,0.0846782132826726));
#9416=CARTESIAN_POINT('Ctrl Pts',(-2.43687977559142,0.292153052631133,0.127017319924011));
#9417=CARTESIAN_POINT('Ctrl Pts',(-2.44832567486989,0.196212235023275,0.132069047878662));
#9418=CARTESIAN_POINT('Ctrl Pts',(-2.45354070668951,0.0994776099830367,
0.137120775833312));
#9419=CARTESIAN_POINT('Ctrl Pts',(-2.45278840085115,0.00262419282126472,
0.142172503787962));
#9420=CARTESIAN_POINT('Origin',(0.,0.,0.));
#9421=CARTESIAN_POINT('',(-2.44709082993613,0.00122547174869078,1.05782749621206));
#9422=CARTESIAN_POINT('',(-2.4469182083441,0.00108108736496512,0.942172503787958));
#9423=CARTESIAN_POINT('',(-2.4505,-3.00099698131059E-16,0.));
#9424=CARTESIAN_POINT('Ctrl Pts',(-2.44709082993613,0.00122547174869078,
1.05782749621206));
#9425=CARTESIAN_POINT('Ctrl Pts',(-2.44858147013302,0.331094139137146,1.04074322659327));
#9426=CARTESIAN_POINT('Ctrl Pts',(-2.38654629113948,0.660424866872034,1.02365895697448));
#9427=CARTESIAN_POINT('Ctrl Pts',(-2.25832126611665,0.961571221090581,1.00657468735569));
#9428=CARTESIAN_POINT('Ctrl Pts',(-1.9406653489959,1.70761062579985,0.964251284937728));
#9429=CARTESIAN_POINT('Ctrl Pts',(-1.21679094422775,2.28067767489988,0.921927882519764));
#9430=CARTESIAN_POINT('Ctrl Pts',(-0.417767228755014,2.41869275133695,0.879604480101802));
#9431=CARTESIAN_POINT('Ctrl Pts',(0.381256486717722,2.55670782777402,0.83728107768384));
#9432=CARTESIAN_POINT('Ctrl Pts',(1.25542951289504,2.25967093154815,0.794957675265879));
#9433=CARTESIAN_POINT('Ctrl Pts',(1.80493193792011,1.66339843739796,0.752634272847918));
#9434=CARTESIAN_POINT('Ctrl Pts',(2.35443436294518,1.06712594324778,0.710310870429956));
#9435=CARTESIAN_POINT('Ctrl Pts',(2.57926618681799,0.171617851173292,0.667987468011993));
#9436=CARTESIAN_POINT('Ctrl Pts',(2.37661022655832,-0.613484110704425,0.625664065594031));
#9437=CARTESIAN_POINT('Ctrl Pts',(2.17395426629865,-1.39858607258214,0.583340663176068));
#9438=CARTESIAN_POINT('Ctrl Pts',(1.5438105219065,-2.07328190426309,0.541017260758106));
#9439=CARTESIAN_POINT('Ctrl Pts',(0.774359256385592,-2.32912561010772,0.498693858340144));
#9440=CARTESIAN_POINT('Ctrl Pts',(0.00490799086468277,-2.58496931595236,
0.456370455922182));
#9441=CARTESIAN_POINT('Ctrl Pts',(-0.903850795784982,-2.42196089596069,
0.41404705350422));
#9442=CARTESIAN_POINT('Ctrl Pts',(-1.53624073821425,-1.91439855300023,0.371723651086258));
#9443=CARTESIAN_POINT('Ctrl Pts',(-2.1035138362237,-1.45909962522464,0.33375826612819));
#9444=CARTESIAN_POINT('Ctrl Pts',(-2.44840292762362,-0.726550625723455,
0.295792881170123));
#9445=CARTESIAN_POINT('Ctrl Pts',(-2.45343712965594,0.00158941762237803,
0.257827496212055));
#9446=CARTESIAN_POINT('Ctrl Pts',(-2.45278840085115,0.00262419282126472,
0.142172503787962));
#9447=CARTESIAN_POINT('Ctrl Pts',(-2.44723554588049,-0.712261896697142,
0.179459882474651));
#9448=CARTESIAN_POINT('Ctrl Pts',(-2.11657712126492,-1.43361988081142,0.216747261161339));
#9449=CARTESIAN_POINT('Ctrl Pts',(-1.56678617588997,-1.89000633907613,0.254034639848028));
#9450=CARTESIAN_POINT('Ctrl Pts',(-0.942509053535351,-2.40822444951227,
0.296373746489366));
#9451=CARTESIAN_POINT('Ctrl Pts',(-0.0357006700407422,-2.58481029512054,
0.338712853130705));
#9452=CARTESIAN_POINT('Ctrl Pts',(0.738006177904425,-2.34071471461417,0.381051959772044));
#9453=CARTESIAN_POINT('Ctrl Pts',(1.51171302584959,-2.09661913410779,0.423391066413383));
#9454=CARTESIAN_POINT('Ctrl Pts',(2.15231833824532,-1.43184212748677,0.465730173054722));
#9455=CARTESIAN_POINT('Ctrl Pts',(2.3669503643466,-0.649736793975562,0.508069279696061));
#9456=CARTESIAN_POINT('Ctrl Pts',(2.58158239044788,0.132368539535648,0.550408386337399));
#9457=CARTESIAN_POINT('Ctrl Pts',(2.37024113025471,1.03180219993705,0.592747492978738));
#9458=CARTESIAN_POINT('Ctrl Pts',(1.82948647714086,1.63645052880757,0.635086599620077));
#9459=CARTESIAN_POINT('Ctrl Pts',(1.28873182402701,2.24109885767809,0.677425706261415));
#9460=CARTESIAN_POINT('Ctrl Pts',(0.418563777992485,2.55096185501775,0.719764812902754));
#9461=CARTESIAN_POINT('Ctrl Pts',(-0.382678773049915,2.42446863484039,0.762103919544093));
#9462=CARTESIAN_POINT('Ctrl Pts',(-1.18392132409231,2.29797541466303,0.804443026185432));
#9463=CARTESIAN_POINT('Ctrl Pts',(-1.91623838014258,1.73512597696867,0.846782132826771));
#9464=CARTESIAN_POINT('Ctrl Pts',(-2.24451388823343,0.993392607903086,0.88912123946811));
#9465=CARTESIAN_POINT('Ctrl Pts',(-2.381624565422,0.683593180229046,0.906804994241392));
#9466=CARTESIAN_POINT('Ctrl Pts',(-2.44825106878348,0.342587837773907,0.924488749014675));
#9467=CARTESIAN_POINT('Ctrl Pts',(-2.4469182083441,0.00108108736496512,
0.942172503787958));
#9468=CARTESIAN_POINT('Origin',(0.,0.,0.));
#9469=CARTESIAN_POINT('',(-2.44901144034399,-0.00211142026644101,1.85782749621206));
#9470=CARTESIAN_POINT('',(-2.44927322928455,-0.00216311090478056,1.74217250378796));
#9471=CARTESIAN_POINT('',(-2.4505,-3.00099698131059E-16,0.));
#9472=CARTESIAN_POINT('Ctrl Pts',(-2.44901144034399,-0.00211142026644101,
1.85782749621206));
#9473=CARTESIAN_POINT('Ctrl Pts',(-2.44428079907938,0.572343309026032,1.82801697443437));
#9474=CARTESIAN_POINT('Ctrl Pts',(-2.24249780427236,1.14979088066879,1.79820645265669));
#9475=CARTESIAN_POINT('Ctrl Pts',(-1.87352390546256,1.58572983322239,1.76839593087901));
#9476=CARTESIAN_POINT('Ctrl Pts',(-1.34967427553953,2.2046529052903,1.72607252846104));
#9477=CARTESIAN_POINT('Ctrl Pts',(-0.488820969467413,2.5383396176156,1.68374912604308));
#9478=CARTESIAN_POINT('Ctrl Pts',(0.315314577443851,2.43417478721053,1.64142572362512));
#9479=CARTESIAN_POINT('Ctrl Pts',(1.11945012435512,2.33000995680546,1.59910232120716));
#9480=CARTESIAN_POINT('Ctrl Pts',(1.86686791210553,1.78799358367002,1.5567789187892));
#9481=CARTESIAN_POINT('Ctrl Pts',(2.21572738312456,1.05602253293468,1.51445551637123));
#9482=CARTESIAN_POINT('Ctrl Pts',(2.56458685414359,0.324051482199336,1.47213211395327));
#9483=CARTESIAN_POINT('Ctrl Pts',(2.51488800843124,-0.597874246135909,1.42980871153531));
#9484=CARTESIAN_POINT('Ctrl Pts',(2.08936146294263,-1.28809947042103,1.38748530911735));
#9485=CARTESIAN_POINT('Ctrl Pts',(1.66383491745404,-1.97832469470614,1.34516190669938));
#9486=CARTESIAN_POINT('Ctrl Pts',(0.862480672189199,-2.43684941494112,1.30283850428142));
#9487=CARTESIAN_POINT('Ctrl Pts',(0.0518071380387072,-2.45396470323855,
1.26051510186346));
#9488=CARTESIAN_POINT('Ctrl Pts',(-0.758866396111789,-2.47107999153598,
1.2181916994455));
#9489=CARTESIAN_POINT('Ctrl Pts',(-1.57885921914794,-2.04678584789584,1.17586829702754));
#9490=CARTESIAN_POINT('Ctrl Pts',(-2.03313691592934,-1.37513289591652,1.13354489460957));
#9491=CARTESIAN_POINT('Ctrl Pts',(-2.30404082397389,-0.974599453861103,
1.1083057618104));
#9492=CARTESIAN_POINT('Ctrl Pts',(-2.44488865994441,-0.486099962014506,
1.08306662901123));
#9493=CARTESIAN_POINT('Ctrl Pts',(-2.44709082993613,0.00122547174869078,
1.05782749621206));
#9494=CARTESIAN_POINT('Ctrl Pts',(-2.4469182083441,0.00108108736496512,
0.942172503787958));
#9495=CARTESIAN_POINT('Ctrl Pts',(-2.4450598845014,-0.475060388503602,0.966827855656014));
#9496=CARTESIAN_POINT('Ctrl Pts',(-2.31109549859399,-0.952176550222066,
0.99148320752407));
#9497=CARTESIAN_POINT('Ctrl Pts',(-2.05186792976456,-1.34705035287639,1.01613855939213));
#9498=CARTESIAN_POINT('Ctrl Pts',(-1.60671250307345,-2.02514264415345,1.05847766603346));
#9499=CARTESIAN_POINT('Ctrl Pts',(-0.792167689559793,-2.46070992627076,
1.1008167726748));
#9500=CARTESIAN_POINT('Ctrl Pts',(0.018959005881323,-2.45444035901399,1.14315587931614));
#9501=CARTESIAN_POINT('Ctrl Pts',(0.830085701322441,-2.44817079175722,1.18549498595748));
#9502=CARTESIAN_POINT('Ctrl Pts',(1.63779427869103,-2.00006437512636,1.22783409259882));
#9503=CARTESIAN_POINT('Ctrl Pts',(2.07242512020182,-1.31518860000204,1.27017319924016));
#9504=CARTESIAN_POINT('Ctrl Pts',(2.50705596171262,-0.630312824877714,1.3125123058815));
#9505=CARTESIAN_POINT('Ctrl Pts',(2.56860906736563,0.29133230874007,1.35485141252284));
#9506=CARTESIAN_POINT('Ctrl Pts',(2.22890980083579,1.02792517390474,1.39719051916417));
#9507=CARTESIAN_POINT('Ctrl Pts',(1.88921053430595,1.76451803906942,1.43952962580551));
#9508=CARTESIAN_POINT('Ctrl Pts',(1.14825889559327,2.31605863578098,1.48186873244685));
#9509=CARTESIAN_POINT('Ctrl Pts',(0.345170071483936,2.43012699230601,1.52420783908819));
#9510=CARTESIAN_POINT('Ctrl Pts',(-0.457918752625402,2.54419534883104,1.56654694572953));
#9511=CARTESIAN_POINT('Ctrl Pts',(-1.32314476213139,2.22079146516954,1.60888605237087));
#9512=CARTESIAN_POINT('Ctrl Pts',(-1.85451854586612,1.60792579269655,1.65122515901221));
#9513=CARTESIAN_POINT('Ctrl Pts',(-2.23499448995806,1.16909976763974,1.68154094060412));
#9514=CARTESIAN_POINT('Ctrl Pts',(-2.44430800748012,0.581869813096559,1.71185672219604));
#9515=CARTESIAN_POINT('Ctrl Pts',(-2.44927322928455,-0.00216311090478056,
1.74217250378796));
#9516=CARTESIAN_POINT('Origin',(0.,0.,0.));
#9517=CARTESIAN_POINT('',(-2.45450932558232,7.6261763116035E-5,2.65782749621206));
#9518=CARTESIAN_POINT('',(-2.45449494699467,0.000217524429918226,2.54217250378796));
#9519=CARTESIAN_POINT('',(-2.4505,-3.00099698131059E-16,0.));
#9520=CARTESIAN_POINT('Ctrl Pts',(-2.45450932558232,7.6261763116035E-5,
2.65782749621206));
#9521=CARTESIAN_POINT('Ctrl Pts',(-2.45451119120266,0.00416415927192646,
2.65761412469344));
#9522=CARTESIAN_POINT('Ctrl Pts',(-2.45450186106136,0.00825204801413194,
2.65740075317482));
#9523=CARTESIAN_POINT('Ctrl Pts',(-2.45448130952338,0.0123398803409236,
2.65718738165621));
#9524=CARTESIAN_POINT('Ctrl Pts',(-2.45040480007216,0.823183678550061,2.61486397923825));
#9525=CARTESIAN_POINT('Ctrl Pts',(-2.00482375815798,1.63180781893863,2.57254057682028));
#9526=CARTESIAN_POINT('Ctrl Pts',(-1.32152997796213,2.06837842113986,2.53021717440232));
#9527=CARTESIAN_POINT('Ctrl Pts',(-0.638236197766273,2.50494902334109,2.48789377198436));
#9528=CARTESIAN_POINT('Ctrl Pts',(0.282770320711254,2.56946608735497,2.4455703695664));
#9529=CARTESIAN_POINT('Ctrl Pts',(1.02025628473274,2.23242197451411,2.40324696714844));
#9530=CARTESIAN_POINT('Ctrl Pts',(1.75774224875421,1.89537786167325,2.36092356473047));
#9531=CARTESIAN_POINT('Ctrl Pts',(2.31170765831966,1.15677257197763,2.31860016231251));
#9532=CARTESIAN_POINT('Ctrl Pts',(2.42878983651432,0.354416010264148,2.27627675989455));
#9533=CARTESIAN_POINT('Ctrl Pts',(2.54587201470898,-0.447940551449347,2.23395335747659));
#9534=CARTESIAN_POINT('Ctrl Pts',(2.22607096153286,-1.31404838518072,2.19162995505863));
#9535=CARTESIAN_POINT('Ctrl Pts',(1.61565150075097,-1.84778273272244,2.14930655264067));
#9536=CARTESIAN_POINT('Ctrl Pts',(1.00523203996909,-2.38151708026416,2.1069831502227));
#9537=CARTESIAN_POINT('Ctrl Pts',(0.104194171581416,-2.58287794161623,2.06465974780474));
#9538=CARTESIAN_POINT('Ctrl Pts',(-0.675361720300282,-2.35977058887531,
2.02233634538678));
#9539=CARTESIAN_POINT('Ctrl Pts',(-1.45491761218198,-2.13666323613438,1.98001294296881));
#9540=CARTESIAN_POINT('Ctrl Pts',(-2.11299152755771,-1.48908766930046,1.93768954055085));
#9541=CARTESIAN_POINT('Ctrl Pts',(-2.34860550835862,-0.713220169978244,
1.89536613813289));
#9542=CARTESIAN_POINT('Ctrl Pts',(-2.4182645964874,-0.483835553972742,1.88285325749261));
#9543=CARTESIAN_POINT('Ctrl Pts',(-2.45099711338713,-0.243237138041082,
1.87034037685233));
#9544=CARTESIAN_POINT('Ctrl Pts',(-2.44901144034399,-0.00211142026644101,
1.85782749621206));
#9545=CARTESIAN_POINT('Ctrl Pts',(-2.44927322928455,-0.00216311090478056,
1.74217250378796));
#9546=CARTESIAN_POINT('Ctrl Pts',(-2.45124245034903,-0.233792226701819,
1.75419582883738));
#9547=CARTESIAN_POINT('Ctrl Pts',(-2.42106894900518,-0.464918469377862,
1.7662191538868));
#9548=CARTESIAN_POINT('Ctrl Pts',(-2.35668248545627,-0.686084490105454,
1.77824247893622));
#9549=CARTESIAN_POINT('Ctrl Pts',(-2.12995108334824,-1.46490163915,1.82058158557756));
#9550=CARTESIAN_POINT('Ctrl Pts',(-1.47896672116872,-2.12020847595462,1.8629206922189));
#9551=CARTESIAN_POINT('Ctrl Pts',(-0.701667462640163,-2.35208966279054,
1.90525979886024));
#9552=CARTESIAN_POINT('Ctrl Pts',(0.0756317958883954,-2.58397084962646,
1.94759890550158));
#9553=CARTESIAN_POINT('Ctrl Pts',(0.979245950765992,-2.39242638649367,1.98993801214292));
#9554=CARTESIAN_POINT('Ctrl Pts',(1.59561556779576,-1.86512056429426,2.03227711878426));
#9555=CARTESIAN_POINT('Ctrl Pts',(2.21198518482554,-1.33781474209484,2.07461622542559));
#9556=CARTESIAN_POINT('Ctrl Pts',(2.54111026400748,-0.474747560828786,2.11695533206693));
#9557=CARTESIAN_POINT('Ctrl Pts',(2.43235915396947,0.329078447597896,2.15929443870827));
#9558=CARTESIAN_POINT('Ctrl Pts',(2.32360804393145,1.13290445602459,2.20163354534961));
#9559=CARTESIAN_POINT('Ctrl Pts',(1.77698074467345,1.8774892916119,2.24397265199095));
#9560=CARTESIAN_POINT('Ctrl Pts',(1.04265371162473,2.22205687499011,2.28631175863229));
#9561=CARTESIAN_POINT('Ctrl Pts',(0.308326678576009,2.56662445836832,2.32865086527363));
#9562=CARTESIAN_POINT('Ctrl Pts',(-0.613700088263441,2.51117478953743,2.37098997191497));
#9563=CARTESIAN_POINT('Ctrl Pts',(-1.30144008604655,2.08108561434068,2.4133290785563));
#9564=CARTESIAN_POINT('Ctrl Pts',(-1.98918008382967,1.65099643914393,2.45566818519764));
#9565=CARTESIAN_POINT('Ctrl Pts',(-2.44263331255644,0.84626775758132,2.49800729183898));
#9566=CARTESIAN_POINT('Ctrl Pts',(-2.45426657710675,0.0352019852067503,
2.54034639848032));
#9567=CARTESIAN_POINT('Ctrl Pts',(-2.45443382647206,0.0235414375533725,
2.54095510024953));
#9568=CARTESIAN_POINT('Ctrl Pts',(-2.45450975474792,0.0118795800677466,
2.54156380201875));
#9569=CARTESIAN_POINT('Ctrl Pts',(-2.45449494699467,0.000217524429918226,
2.54217250378796));
#9570=CARTESIAN_POINT('Origin',(0.,0.,0.));
#9571=CARTESIAN_POINT('',(-2.44879028350035,0.00206176536797276,3.45782749621206));
#9572=CARTESIAN_POINT('',(-2.44863779808279,0.00202668083941567,3.34217250378796));
#9573=CARTESIAN_POINT('',(-2.4505,-3.00099698131059E-16,0.));
#9574=CARTESIAN_POINT('Ctrl Pts',(-2.44879028350035,0.00206176536797276,
3.45782749621206));
#9575=CARTESIAN_POINT('Ctrl Pts',(-2.4507822485306,0.25146786442212,3.44488787253455));
#9576=CARTESIAN_POINT('Ctrl Pts',(-2.41573172748871,0.500327341519915,3.43194824885704));
#9577=CARTESIAN_POINT('Ctrl Pts',(-2.34131554709139,0.736798669794325,3.41900862517953));
#9578=CARTESIAN_POINT('Ctrl Pts',(-2.09791233631349,1.51025788594317,3.37668522276156));
#9579=CARTESIAN_POINT('Ctrl Pts',(-1.43336050190279,2.15118402855148,3.3343618203436));
#9580=CARTESIAN_POINT('Ctrl Pts',(-0.651600735693898,2.36644189707647,3.29203841792564));
#9581=CARTESIAN_POINT('Ctrl Pts',(0.130159030514992,2.58169976560146,3.24971501550768));
#9582=CARTESIAN_POINT('Ctrl Pts',(1.02912672852208,2.37128936004313,3.20739161308971));
#9583=CARTESIAN_POINT('Ctrl Pts',(1.63414878100557,1.8314443841374,3.16506821067175));
#9584=CARTESIAN_POINT('Ctrl Pts',(2.23917083348905,1.29159940823166,3.12274480825379));
#9585=CARTESIAN_POINT('Ctrl Pts',(2.55024724044895,0.422319861978524,3.08042140583583));
#9586=CARTESIAN_POINT('Ctrl Pts',(2.42510350427122,-0.378818907200365,3.03809800341787));
#9587=CARTESIAN_POINT('Ctrl Pts',(2.2999597680935,-1.17995767637926,2.99577460099991));
#9588=CARTESIAN_POINT('Ctrl Pts',(1.73859588877812,-1.91295566848391,2.95345119858194));
#9589=CARTESIAN_POINT('Ctrl Pts',(0.99775831871812,-2.24256752609274,2.91112779616398));
#9590=CARTESIAN_POINT('Ctrl Pts',(0.256920748658124,-2.57217938370157,2.86880439374602));
#9591=CARTESIAN_POINT('Ctrl Pts',(-0.663390512146504,-2.4984051068146,2.82648099132806));
#9592=CARTESIAN_POINT('Ctrl Pts',(-1.34226015405468,-2.05498624035627,2.7841575889101));
#9593=CARTESIAN_POINT('Ctrl Pts',(-2.01770730537467,-1.61380285005329,2.74204755801075));
#9594=CARTESIAN_POINT('Ctrl Pts',(-2.45414113525188,-0.806692568145523,
2.6999375271114));
#9595=CARTESIAN_POINT('Ctrl Pts',(-2.45450932558232,7.6261763116035E-5,
2.65782749621206));
#9596=CARTESIAN_POINT('Ctrl Pts',(-2.45449494699467,0.000217524429918226,
2.54217250378796));
#9597=CARTESIAN_POINT('Ctrl Pts',(-2.45347978066934,-0.799291082283641,
2.58390290866009));
#9598=CARTESIAN_POINT('Ctrl Pts',(-2.02600703470396,-1.59973100051144,2.62563331353221));
#9599=CARTESIAN_POINT('Ctrl Pts',(-1.3605912120938,-2.04290360643243,2.66736371840434));
#9600=CARTESIAN_POINT('Ctrl Pts',(-0.685469282156714,-2.49254056251051,
2.70970282504568));
#9601=CARTESIAN_POINT('Ctrl Pts',(0.234587878091294,-2.57441161148015,2.75204193168701));
#9602=CARTESIAN_POINT('Ctrl Pts',(0.978495183990076,-2.25104659733286,2.79438103832835));
#9603=CARTESIAN_POINT('Ctrl Pts',(1.72240248988886,-1.92768158318556,2.83672014496969));
#9604=CARTESIAN_POINT('Ctrl Pts',(2.29015994143841,-1.19908050592133,2.87905925161103));
#9605=CARTESIAN_POINT('Ctrl Pts',(2.42192042487556,-0.398704226023195,2.92139835825237));
#9606=CARTESIAN_POINT('Ctrl Pts',(2.55368090831271,0.401672053874929,2.96373746489371));
#9607=CARTESIAN_POINT('Ctrl Pts',(2.24944442363746,1.27382353640695,3.00607657153505));
#9608=CARTESIAN_POINT('Ctrl Pts',(1.6484517191997,1.81859025937093,3.04841567817639));
#9609=CARTESIAN_POINT('Ctrl Pts',(1.04745901476194,2.36335698233492,3.09075478481772));
#9610=CARTESIAN_POINT('Ctrl Pts',(0.149710090561681,2.58073894573087,3.13309389145906));
#9611=CARTESIAN_POINT('Ctrl Pts',(-0.633919837933851,2.37124634813164,3.1754329981004));
#9612=CARTESIAN_POINT('Ctrl Pts',(-1.41754976642938,2.16175375053241,3.21777210474174));
#9613=CARTESIAN_POINT('Ctrl Pts',(-2.08706069922018,1.525386591938,3.26011121138308));
#9614=CARTESIAN_POINT('Ctrl Pts',(-2.33603572860561,0.75339277828086,3.30245031802442));
#9615=CARTESIAN_POINT('Ctrl Pts',(-2.41389780579042,0.511966792496097,3.31569104661227));
#9616=CARTESIAN_POINT('Ctrl Pts',(-2.4506313265692,0.257276473065291,3.32893177520011));
#9617=CARTESIAN_POINT('Ctrl Pts',(-2.44863779808279,0.00202668083941567,
3.34217250378796));
#9618=CARTESIAN_POINT('Origin',(0.,0.,0.));
#9619=CARTESIAN_POINT('',(-2.44722122097757,-0.00133409068037049,4.25782749621205));
#9620=CARTESIAN_POINT('',(-2.44727990084847,-0.00138675037849539,4.14217250378796));
#9621=CARTESIAN_POINT('',(-2.4505,-3.00099698131059E-16,0.));
#9622=CARTESIAN_POINT('Ctrl Pts',(-2.44722122097757,-0.00133409068037049,
4.25782749621205));
#9623=CARTESIAN_POINT('Ctrl Pts',(-2.44476959024658,0.494163923095195,4.23216162037565));
#9624=CARTESIAN_POINT('Ctrl Pts',(-2.29877320492706,0.990990135522418,4.20649574453925));
#9625=CARTESIAN_POINT('Ctrl Pts',(-2.01920729690624,1.39550444749988,4.18082986870284));
#9626=CARTESIAN_POINT('Ctrl Pts',(-1.55819904988879,2.06255442930348,4.13850646628488));
#9627=CARTESIAN_POINT('Ctrl Pts',(-0.733982018406264,2.47858537266224,4.09618306386692));
#9628=CARTESIAN_POINT('Ctrl Pts',(0.0764783273015039,2.4533205734938,4.05385966144895));
#9629=CARTESIAN_POINT('Ctrl Pts',(0.886938673009272,2.42805577432537,4.01153625903099));
#9630=CARTESIAN_POINT('Ctrl Pts',(1.68364233294229,1.96149523262974,3.96921285661303));
#9631=CARTESIAN_POINT('Ctrl Pts',(2.10220740483942,1.26702596575867,3.92688945419507));
#9632=CARTESIAN_POINT('Ctrl Pts',(2.52077247673655,0.572556698887595,3.88456605177711));
#9633=CARTESIAN_POINT('Ctrl Pts',(2.5611989605978,-0.349821293158926,3.84224264935915));
#9634=CARTESIAN_POINT('Ctrl Pts',(2.20499732281998,-1.07824745639663,3.79991924694118));
#9635=CARTESIAN_POINT('Ctrl Pts',(1.84879568504216,-1.80667361963432,3.75759584452322));
#9636=CARTESIAN_POINT('Ctrl Pts',(1.09596592562527,-2.3411479540632,3.71527244210526));
#9637=CARTESIAN_POINT('Ctrl Pts',(0.290823696188848,-2.43722226081783,3.67294903968729));
#9638=CARTESIAN_POINT('Ctrl Pts',(-0.514318533247575,-2.53329656757247,
3.63062563726933));
#9639=CARTESIAN_POINT('Ctrl Pts',(-1.37177323270354,-2.19097084665287,3.58830223485137));
#9640=CARTESIAN_POINT('Ctrl Pts',(-1.88937328885896,-1.56681184134837,3.54597883243341));
#9641=CARTESIAN_POINT('Ctrl Pts',(-2.24872638093603,-1.13347829387951,3.51659505369296));
#9642=CARTESIAN_POINT('Ctrl Pts',(-2.44426685521786,-0.564298881106139,
3.48721127495251));
#9643=CARTESIAN_POINT('Ctrl Pts',(-2.44879028350035,0.00206176536797276,
3.45782749621206));
#9644=CARTESIAN_POINT('Ctrl Pts',(-2.44863779808279,0.00202668083941567,
3.34217250378796));
#9645=CARTESIAN_POINT('Ctrl Pts',(-2.44425673663492,-0.558920921325063,
3.37127088184145));
#9646=CARTESIAN_POINT('Ctrl Pts',(-2.25283838345664,-1.12257056969168,3.40036925989494));
#9647=CARTESIAN_POINT('Ctrl Pts',(-1.89987184308078,-1.55407547542566,3.42946763794843));
#9648=CARTESIAN_POINT('Ctrl Pts',(-1.38629380219047,-2.18192944675517,3.47180674458977));
#9649=CARTESIAN_POINT('Ctrl Pts',(-0.530698594429779,-2.5300169206943,3.51414585123111));
#9650=CARTESIAN_POINT('Ctrl Pts',(0.275331171558287,-2.43902774682149,3.55648495787245));
#9651=CARTESIAN_POINT('Ctrl Pts',(1.08136093754636,-2.34803857294868,3.59882406451379));
#9652=CARTESIAN_POINT('Ctrl Pts',(1.8378252617618,-1.81797275126393,3.64116317115513));
#9653=CARTESIAN_POINT('Ctrl Pts',(2.19851103921323,-1.09142696233993,3.68350227779647));
#9654=CARTESIAN_POINT('Ctrl Pts',(2.55919681666466,-0.364881173415942,3.72584138443781));
#9655=CARTESIAN_POINT('Ctrl Pts',(2.52410404735208,0.558144582747287,3.76818049107915));
#9656=CARTESIAN_POINT('Ctrl Pts',(2.10929373540885,1.25520657320205,3.81051959772049));
#9657=CARTESIAN_POINT('Ctrl Pts',(1.69448342346561,1.95226856365681,3.85285870436182));
#9658=CARTESIAN_POINT('Ctrl Pts',(0.899955568891718,2.42336678840311,3.89519781100316));
#9659=CARTESIAN_POINT('Ctrl Pts',(0.0893439171220223,2.45289242898376,3.9375369176445));
#9660=CARTESIAN_POINT('Ctrl Pts',(-0.721267734647671,2.48241806956442,3.97987602428584));
#9661=CARTESIAN_POINT('Ctrl Pts',(-1.54796318361316,2.07037112597943,4.02221513092718));
#9662=CARTESIAN_POINT('Ctrl Pts',(-2.0123864530499,1.40533425463558,4.06455423756852));
#9663=CARTESIAN_POINT('Ctrl Pts',(-2.29618813448365,0.998940788322545,4.090426992975));
#9664=CARTESIAN_POINT('Ctrl Pts',(-2.44470876469706,0.498074863705097,4.11629974838148));
#9665=CARTESIAN_POINT('Ctrl Pts',(-2.44727990084847,-0.00138675037849539,
4.14217250378796));
#9666=CARTESIAN_POINT('Origin',(0.,0.,0.));
#9667=CARTESIAN_POINT('',(-2.45364436265411,-0.00130297157212494,5.05782749621206));
#9668=CARTESIAN_POINT('',(-2.45368883860995,-0.00127745634613248,4.94217250378796));
#9669=CARTESIAN_POINT('',(-2.4505,-3.00099698131059E-16,0.));
#9670=CARTESIAN_POINT('Ctrl Pts',(-2.45364436265411,-0.00130297157212494,
5.05782749621206));
#9671=CARTESIAN_POINT('Ctrl Pts',(-2.44890065072277,0.734926114472917,5.01943536821676));
#9672=CARTESIAN_POINT('Ctrl Pts',(-2.09516161037558,1.47510769560909,4.98104324022146));
#9673=CARTESIAN_POINT('Ctrl Pts',(-1.51690197902683,1.92967332906283,4.94265111222616));
#9674=CARTESIAN_POINT('Ctrl Pts',(-0.879429758611428,2.43078554228515,4.9003277098082));
#9675=CARTESIAN_POINT('Ctrl Pts',(0.0308981140190441,2.58479406519437,4.85800430739023));
#9676=CARTESIAN_POINT('Ctrl Pts',(0.797732350424128,2.32126126663045,4.81568090497227));
#9677=CARTESIAN_POINT('Ctrl Pts',(1.56456658682921,2.05772846806654,4.77335750255431));
#9678=CARTESIAN_POINT('Ctrl Pts',(2.18790718700891,1.37665434802948,4.73103410013635));
#9679=CARTESIAN_POINT('Ctrl Pts',(2.38266190766968,0.589536262338264,4.68871069771839));
#9680=CARTESIAN_POINT('Ctrl Pts',(2.57741662833046,-0.197581823352954,4.64638729530042));
#9681=CARTESIAN_POINT('Ctrl Pts',(2.34358546947232,-1.09074387469833,4.60406389288246));
#9682=CARTESIAN_POINT('Ctrl Pts',(1.78811389495814,-1.68145159595198,4.5617404904645));
#9683=CARTESIAN_POINT('Ctrl Pts',(1.23264232044396,-2.27215931720563,4.51941708804654));
#9684=CARTESIAN_POINT('Ctrl Pts',(0.355530330273727,-2.56041270836756,4.47709368562858));
#9685=CARTESIAN_POINT('Ctrl Pts',(-0.442064466333378,-2.41437564982704,
4.43477028321061));
#9686=CARTESIAN_POINT('Ctrl Pts',(-1.23965926294048,-2.26833859128653,4.39244688079265));
#9687=CARTESIAN_POINT('Ctrl Pts',(-1.95773686598445,-1.68801108304359,4.35012347837469));
#9688=CARTESIAN_POINT('Ctrl Pts',(-2.26787593623026,-0.938812818797895,
4.30780007595673));
#9689=CARTESIAN_POINT('Ctrl Pts',(-2.38993960577132,-0.643945457277985,
4.29114254937517));
#9690=CARTESIAN_POINT('Ctrl Pts',(-2.44881236496696,-0.322919505812342,
4.27448502279361));
#9691=CARTESIAN_POINT('Ctrl Pts',(-2.44722122097757,-0.00133409068037049,
4.25782749621205));
#9692=CARTESIAN_POINT('Ctrl Pts',(-2.44727990084847,-0.00138675037849539,
4.14217250378796));
#9693=CARTESIAN_POINT('Ctrl Pts',(-2.4489162642847,-0.319262068898655,4.15863885502282));
#9694=CARTESIAN_POINT('Ctrl Pts',(-2.39143568339083,-0.636568570457953,
4.17510520625768));
#9695=CARTESIAN_POINT('Ctrl Pts',(-2.27208795289109,-0.928590296092531,
4.19157155749253));
#9696=CARTESIAN_POINT('Ctrl Pts',(-1.96521509338757,-1.67945117637405,4.23391066413387));
#9697=CARTESIAN_POINT('Ctrl Pts',(-1.24931828447256,-2.2631461378344,4.27624977077521));
#9698=CARTESIAN_POINT('Ctrl Pts',(-0.452043984954612,-2.41253390428878,
4.31858887741655));
#9699=CARTESIAN_POINT('Ctrl Pts',(0.345230314563356,-2.56192167074316,4.36092798405789));
#9700=CARTESIAN_POINT('Ctrl Pts',(1.22388210468428,-2.27700224219155,4.40326709069923));
#9701=CARTESIAN_POINT('Ctrl Pts',(1.78177640732824,-1.68817547605737,4.44560619734057));
#9702=CARTESIAN_POINT('Ctrl Pts',(2.33967070997219,-1.09934870992319,4.4879453039819));
#9703=CARTESIAN_POINT('Ctrl Pts',(2.5768075251392,-0.206614606206465,4.53028441062324));
#9704=CARTESIAN_POINT('Ctrl Pts',(2.38465579531495,0.581446765872876,4.57262351726458));
#9705=CARTESIAN_POINT('Ctrl Pts',(2.19250406549071,1.36950813795221,4.61496262390592));
#9706=CARTESIAN_POINT('Ctrl Pts',(1.57106379067523,2.05289677839415,4.65730173054726));
#9707=CARTESIAN_POINT('Ctrl Pts',(0.804751248283616,2.31884433113998,4.6996408371886));
#9708=CARTESIAN_POINT('Ctrl Pts',(0.0384387058919862,2.58479188388582,4.74197994382993));
#9709=CARTESIAN_POINT('Ctrl Pts',(-0.872746104075775,2.43329834893554,4.78431905047128));
#9710=CARTESIAN_POINT('Ctrl Pts',(-1.51177872699224,1.93369818852045,4.82665815711262));
#9711=CARTESIAN_POINT('Ctrl Pts',(-2.09293912294914,1.4793429386713,4.86516293933773));
#9712=CARTESIAN_POINT('Ctrl Pts',(-2.44900869472268,0.737076692851381,4.90366772156284));
#9713=CARTESIAN_POINT('Ctrl Pts',(-2.45368883860995,-0.00127745634613248,
4.94217250378796));
#9714=CARTESIAN_POINT('Origin',(0.,0.,0.));
#9715=CARTESIAN_POINT('',(-2.45111861015583,0.00218804967254627,5.85782749621206));
#9716=CARTESIAN_POINT('',(-2.45112004158473,0.00219228095941415,5.74217250378796));
#9717=CARTESIAN_POINT('',(-2.4505,-3.00099698131059E-16,0.));
#9718=CARTESIAN_POINT('Ctrl Pts',(-2.45111861015583,0.00218804967254627,
5.85782749621206));
#9719=CARTESIAN_POINT('Ctrl Pts',(-2.45267722565121,0.171297744836882,5.84903251847582));
#9720=CARTESIAN_POINT('Ctrl Pts',(-2.43666676456879,0.340114246849872,5.84023754073959));
#9721=CARTESIAN_POINT('Ctrl Pts',(-2.40199867071989,0.505008075907527,5.83144256300336));
#9722=CARTESIAN_POINT('Ctrl Pts',(-2.23516803953071,1.29851410773017,5.7891191605854));
#9723=CARTESIAN_POINT('Ctrl Pts',(-1.63627329148971,2.00118084351996,5.74679575816743));
#9724=CARTESIAN_POINT('Ctrl Pts',(-0.879226068428833,2.29163528762042,5.70447235574947));
#9725=CARTESIAN_POINT('Ctrl Pts',(-0.122178845367954,2.58208973172088,5.66214895333151));
#9726=CARTESIAN_POINT('Ctrl Pts',(0.793020852712802,2.460331884132,5.61982555091355));
#9727=CARTESIAN_POINT('Ctrl Pts',(1.44779555001256,1.98204914576702,5.57750214849559));
#9728=CARTESIAN_POINT('Ctrl Pts',(2.10257024731232,1.50376640740205,5.53517874607763));
#9729=CARTESIAN_POINT('Ctrl Pts',(2.49691994383109,0.668958778260969,5.49285534365967));
#9730=CARTESIAN_POINT('Ctrl Pts',(2.45048411180883,-0.140564535514672,5.4505319412417));
#9731=CARTESIAN_POINT('Ctrl Pts',(2.40404827978657,-0.950087849290307,5.40820853882374));
#9732=CARTESIAN_POINT('Ctrl Pts',(1.91682691922329,-1.73432684770051,5.36588513640578));
#9733=CARTESIAN_POINT('Ctrl Pts',(1.21165651890775,-2.13460048980139,5.32356173398782));
#9734=CARTESIAN_POINT('Ctrl Pts',(0.506486118592195,-2.53487413190227,5.28123833156986));
#9735=CARTESIAN_POINT('Ctrl Pts',(-0.416633321475635,-2.55118241769382,
5.23891492915189));
#9736=CARTESIAN_POINT('Ctrl Pts',(-1.13550213722612,-2.17606655854707,5.19659152673393));
#9737=CARTESIAN_POINT('Ctrl Pts',(-1.8543709529766,-1.80095069940033,5.15426812431597));
#9738=CARTESIAN_POINT('Ctrl Pts',(-2.36898914440973,-1.03441069531529,5.11194472189801));
#9739=CARTESIAN_POINT('Ctrl Pts',(-2.44398995602614,-0.227032741505079,
5.06962131948004));
#9740=CARTESIAN_POINT('Ctrl Pts',(-2.45095652193392,-0.152038196692948,
5.06569004505738));
#9741=CARTESIAN_POINT('Ctrl Pts',(-2.45413010893487,-0.0766913057520759,
5.06175877063472));
#9742=CARTESIAN_POINT('Ctrl Pts',(-2.45364436265411,-0.00130297157212494,
5.05782749621206));
#9743=CARTESIAN_POINT('Ctrl Pts',(-2.45368883860995,-0.00127745634613248,
4.94217250378796));
#9744=CARTESIAN_POINT('Ctrl Pts',(-2.45415488955067,-0.0748031115631014,
4.94600682820418));
#9745=CARTESIAN_POINT('Ctrl Pts',(-2.45113646785659,-0.14828997337155,4.94984115262041));
#9746=CARTESIAN_POINT('Ctrl Pts',(-2.4445088578359,-0.221449876124288,4.95367547703663));
#9747=CARTESIAN_POINT('Ctrl Pts',(-2.37132592989794,-1.02929099447407,4.99601458367797));
#9748=CARTESIAN_POINT('Ctrl Pts',(-1.85807963815686,-1.79726644529373,5.03835369031931));
#9749=CARTESIAN_POINT('Ctrl Pts',(-1.13966882262996,-2.1738947946943,5.08069279696065));
#9750=CARTESIAN_POINT('Ctrl Pts',(-0.421258007103072,-2.55052314409486,
5.12303190360199));
#9751=CARTESIAN_POINT('Ctrl Pts',(0.502317332209637,-2.53580439207634,5.16537101024333));
#9752=CARTESIAN_POINT('Ctrl Pts',(1.20836193308383,-2.13647491030144,5.20771011688466));
#9753=CARTESIAN_POINT('Ctrl Pts',(1.91440653395803,-1.73714542852654,5.250049223526));
#9754=CARTESIAN_POINT('Ctrl Pts',(2.40292039639372,-0.953205216995241,5.29238833016734));
#9755=CARTESIAN_POINT('Ctrl Pts',(2.45032403922356,-0.14344234547996,5.33472743680868));
#9756=CARTESIAN_POINT('Ctrl Pts',(2.4977276820534,0.666320526035315,5.37706654345001));
#9757=CARTESIAN_POINT('Ctrl Pts',(2.10402110527741,1.50190605753458,5.41940565009136));
#9758=CARTESIAN_POINT('Ctrl Pts',(1.44939307923848,1.98088952380724,5.4617447567327));
#9759=CARTESIAN_POINT('Ctrl Pts',(0.794765053199531,2.4598729900799,5.50408386337404));
#9760=CARTESIAN_POINT('Ctrl Pts',(-0.120784422102356,2.58225439112595,5.54642297001537));
#9761=CARTESIAN_POINT('Ctrl Pts',(-0.878233303668452,2.29202309499735,5.58876207665671));
#9762=CARTESIAN_POINT('Ctrl Pts',(-1.63568218523454,2.00179179886876,5.63110118329805));
#9763=CARTESIAN_POINT('Ctrl Pts',(-2.23503047306484,1.2989478055655,5.67344028993939));
#9764=CARTESIAN_POINT('Ctrl Pts',(-2.40197279010514,0.505163655925678,5.71577939658073));
#9765=CARTESIAN_POINT('Ctrl Pts',(-2.43666196850777,0.34022213319964,5.72457709898314));
#9766=CARTESIAN_POINT('Ctrl Pts',(-2.45268103865343,0.17135406301958,5.73337480138555));
#9767=CARTESIAN_POINT('Ctrl Pts',(-2.45112004158473,0.00219228095941415,
5.74217250378796));
#9768=CARTESIAN_POINT('Origin',(0.,0.,0.));
#9769=CARTESIAN_POINT('',(-2.44649108011119,-0.000113800941714537,6.65782749621206));
#9770=CARTESIAN_POINT('',(-2.44648217412756,-8.24998363560429E-5,6.54217250378796));
#9771=CARTESIAN_POINT('',(-2.4505,-3.00099698131059E-16,0.));
#9772=CARTESIAN_POINT('Ctrl Pts',(-2.44649108011119,-0.000113800941714537,
6.65782749621206));
#9773=CARTESIAN_POINT('Ctrl Pts',(-2.44631871903483,0.415678882547852,6.63630626631693));
#9774=CARTESIAN_POINT('Ctrl Pts',(-2.34588140389044,0.831549710158929,6.6147850364218));
#9775=CARTESIAN_POINT('Ctrl Pts',(-2.14564944517726,1.19198122018866,6.59326380652668));
#9776=CARTESIAN_POINT('Ctrl Pts',(-1.75187558527936,1.90080166945843,6.55094040410871));
#9777=CARTESIAN_POINT('Ctrl Pts',(-0.972148917036941,2.39521221106142,6.50861700169075));
#9778=CARTESIAN_POINT('Ctrl Pts',(-0.163086713480121,2.4490882986855,6.46629359927279));
#9779=CARTESIAN_POINT('Ctrl Pts',(0.645975490076699,2.50296438630957,6.42397019685483));
#9780=CARTESIAN_POINT('Ctrl Pts',(1.48437322894793,2.11630601995472,6.38164679443687));
#9781=CARTESIAN_POINT('Ctrl Pts',(1.96865531757284,1.4659560059784,6.33932339201891));
#9782=CARTESIAN_POINT('Ctrl Pts',(2.45293740619775,0.815605992002093,6.29699998960095));
#9783=CARTESIAN_POINT('Ctrl Pts',(2.58310384457635,-0.0984356695956784,
6.25467658718298));
#9784=CARTESIAN_POINT('Ctrl Pts',(2.29962146270785,-0.85812114478397,6.21235318476502));
#9785=CARTESIAN_POINT('Ctrl Pts',(2.01613908083936,-1.61780661997226,6.17002978234706));
#9786=CARTESIAN_POINT('Ctrl Pts',(1.31900787872379,-2.22313590875106,6.12770637992909));
#9787=CARTESIAN_POINT('Ctrl Pts',(0.527069109800669,-2.39725445548984,6.08538297751113));
#9788=CARTESIAN_POINT('Ctrl Pts',(-0.264869659122454,-2.57137300222862,
6.04305957509317));
#9789=CARTESIAN_POINT('Ctrl Pts',(-1.15161599485312,-2.31428080692735,6.00073617267521));
#9790=CARTESIAN_POINT('Ctrl Pts',(-1.72760590554977,-1.74356204534898,5.95841277025725));
#9791=CARTESIAN_POINT('Ctrl Pts',(-2.18390273507956,-1.29144099839104,5.92488434557552));
#9792=CARTESIAN_POINT('Ctrl Pts',(-2.4451768188504,-0.642495978794029,5.89135592089379));
#9793=CARTESIAN_POINT('Ctrl Pts',(-2.45111861015583,0.00218804967254627,
5.85782749621206));
#9794=CARTESIAN_POINT('Ctrl Pts',(-2.45112004158473,0.00219228095941415,
5.74217250378796));
#9795=CARTESIAN_POINT('Ctrl Pts',(-2.44516871119164,-0.642740163254894,
5.77571390802689));
#9796=CARTESIAN_POINT('Ctrl Pts',(-2.18368586072072,-1.29194179724376,5.80925531226582));
#9797=CARTESIAN_POINT('Ctrl Pts',(-1.727077308387,-1.74409505891404,5.84279671650475));
#9798=CARTESIAN_POINT('Ctrl Pts',(-1.15070316337826,-2.31484531813751,5.88513582314608));
#9799=CARTESIAN_POINT('Ctrl Pts',(-0.263418527110475,-2.57162153060804,
5.92747492978742));
#9800=CARTESIAN_POINT('Ctrl Pts',(0.528690603930214,-2.39690422190574,5.96981403642876));
#9801=CARTESIAN_POINT('Ctrl Pts',(1.3207997349709,-2.22218691320345,6.0121531430701));
#9802=CARTESIAN_POINT('Ctrl Pts',(2.0177333607845,-1.61597608332832,6.05449224971144));
#9803=CARTESIAN_POINT('Ctrl Pts',(2.30052395465526,-0.855717907800806,6.09683135635278));
#9804=CARTESIAN_POINT('Ctrl Pts',(2.58331454852602,-0.0954597322732809,
6.13917046299412));
#9805=CARTESIAN_POINT('Ctrl Pts',(2.45196211045394,0.818845788906634,6.18150956963546));
#9806=CARTESIAN_POINT('Ctrl Pts',(1.96658307154252,1.46874593663984,6.22384867627679));
#9807=CARTESIAN_POINT('Ctrl Pts',(1.48120403263111,2.11864608437304,6.26618778291813));
#9808=CARTESIAN_POINT('Ctrl Pts',(0.641798392880346,2.50414085865953,6.30852688955947));
#9809=CARTESIAN_POINT('Ctrl Pts',(-0.167460763063443,2.44879980735622,6.35086599620081));
#9810=CARTESIAN_POINT('Ctrl Pts',(-0.976719919007238,2.39345875605291,6.39320510284215));
#9811=CARTESIAN_POINT('Ctrl Pts',(-1.75583259114405,1.89728187915982,6.43554420948349));
#9812=CARTESIAN_POINT('Ctrl Pts',(-2.14822014291542,1.18735581071813,6.47788331612483));
#9813=CARTESIAN_POINT('Ctrl Pts',(-2.34682515967691,0.828030245761283,6.49931304534587));
#9814=CARTESIAN_POINT('Ctrl Pts',(-2.44635784802019,0.413945812065253,6.52074277456692));
#9815=CARTESIAN_POINT('Ctrl Pts',(-2.44648217412756,-8.24998363560429E-5,
6.54217250378796));
#9816=CARTESIAN_POINT('Origin',(0.,0.,0.));
#9817=CARTESIAN_POINT('',(-2.45153584345453,-0.0021256739944922,7.45782749621206));
#9818=CARTESIAN_POINT('',(-2.45142289816278,-0.00214958505015697,7.34217250378796));
#9819=CARTESIAN_POINT('',(-2.4505,-3.00099698131059E-16,0.));
#9820=CARTESIAN_POINT('Ctrl Pts',(-2.45153584345453,-0.00212567399449221,
7.45782749621206));
#9821=CARTESIAN_POINT('Ctrl Pts',(-2.44552947185313,0.656095934058606,7.42358001415804));
#9822=CARTESIAN_POINT('Ctrl Pts',(-2.17165895316412,1.31872531414478,7.38933253210402));
#9823=CARTESIAN_POINT('Ctrl Pts',(-1.69781926623356,1.77258018438606,7.35508505005));
#9824=CARTESIAN_POINT('Ctrl Pts',(-1.11224314358814,2.33345885810207,7.31276164763203));
#9825=CARTESIAN_POINT('Ctrl Pts',(-0.221268524773137,2.57549127213791,7.27043824521407));
#9826=CARTESIAN_POINT('Ctrl Pts',(0.567606742770822,2.38798102095328,7.2281148427961));
#9827=CARTESIAN_POINT('Ctrl Pts',(1.35648201031479,2.20047076976864,7.18579144037814));
#9828=CARTESIAN_POINT('Ctrl Pts',(2.04325792658772,1.58341785336352,7.14346803796019));
#9829=CARTESIAN_POINT('Ctrl Pts',(2.31382935139211,0.81903876801305,7.10114463554222));
#9830=CARTESIAN_POINT('Ctrl Pts',(2.5844007761965,0.0546596826625877,7.05882123312426));
#9831=CARTESIAN_POINT('Ctrl Pts',(2.43876770953236,-0.857045571633228,7.0164978307063));
#9832=CARTESIAN_POINT('Ctrl Pts',(1.94353716795057,-1.49909774453391,6.97417442828833));
#9833=CARTESIAN_POINT('Ctrl Pts',(1.44830662636876,-2.1411499174346,6.93185102587037));
#9834=CARTESIAN_POINT('Ctrl Pts',(0.603478609869307,-2.51354900894016,6.88952762345241));
#9835=CARTESIAN_POINT('Ctrl Pts',(-0.204554731972394,-2.44597386177769,
6.84720422103445));
#9836=CARTESIAN_POINT('Ctrl Pts',(-1.0125880738141,-2.37839871461522,6.80488081861649));
#9837=CARTESIAN_POINT('Ctrl Pts',(-1.78382674099803,-1.87084932878471,6.76255741619853));
#9838=CARTESIAN_POINT('Ctrl Pts',(-2.1655355488133,-1.15545945740118,6.72023401378057));
#9839=CARTESIAN_POINT('Ctrl Pts',(-2.35314741411761,-0.803841613007534,
6.69943184125773));
#9840=CARTESIAN_POINT('Ctrl Pts',(-2.44665768233904,-0.402014211737506,
6.6786296687349));
#9841=CARTESIAN_POINT('Ctrl Pts',(-2.44649108011119,-0.000113800941714537,
6.65782749621206));
#9842=CARTESIAN_POINT('Ctrl Pts',(-2.44648217412756,-8.24998363560429E-5,
6.54217250378796));
#9843=CARTESIAN_POINT('Ctrl Pts',(-2.44660348137673,-0.404057470632325,
6.56308188120826));
#9844=CARTESIAN_POINT('Ctrl Pts',(-2.35208543716669,-0.807979012017471,
6.58399125862855));
#9845=CARTESIAN_POINT('Ctrl Pts',(-2.16261589659925,-1.16092897605749,6.60490063604884));
#9846=CARTESIAN_POINT('Ctrl Pts',(-1.77896166710579,-1.87561243440111,6.64723974269018));
#9847=CARTESIAN_POINT('Ctrl Pts',(-1.00599077671297,-2.38130409109805,6.68957884933152));
#9848=CARTESIAN_POINT('Ctrl Pts',(-0.19747093585954,-2.44656265670112,6.73191795597286));
#9849=CARTESIAN_POINT('Ctrl Pts',(0.611048904993884,-2.51182122230418,6.7742570626142));
#9850=CARTESIAN_POINT('Ctrl Pts',(1.45511769630792,-2.13664669681336,6.81659616925554));
#9851=CARTESIAN_POINT('Ctrl Pts',(1.94842815605251,-1.49274623575995,6.85893527589687));
#9852=CARTESIAN_POINT('Ctrl Pts',(2.44173861579709,-0.848845774706545,6.90127438253821));
#9853=CARTESIAN_POINT('Ctrl Pts',(2.58429074397226,0.0637806219094324,6.94361348917955));
#9854=CARTESIAN_POINT('Ctrl Pts',(2.3108423165441,0.827448724539928,6.98595259582089));
#9855=CARTESIAN_POINT('Ctrl Pts',(2.03739388911593,1.59111682717045,7.02829170246223));
#9856=CARTESIAN_POINT('Ctrl Pts',(1.34794490608442,2.20582663581546,7.07063080910357));
#9857=CARTESIAN_POINT('Ctrl Pts',(0.558037377145987,2.39024222399774,7.11296991574491));
#9858=CARTESIAN_POINT('Ctrl Pts',(-0.231870151792425,2.57465781218002,7.15530902238624));
#9859=CARTESIAN_POINT('Ctrl Pts',(-1.12223622663775,2.32877917989957,7.19764812902759));
#9860=CARTESIAN_POINT('Ctrl Pts',(-1.70556456044661,1.76513827611953,7.23998723566892));
#9861=CARTESIAN_POINT('Ctrl Pts',(-2.17485144374213,1.31168990458975,7.2740489917086));
#9862=CARTESIAN_POINT('Ctrl Pts',(-2.44541792823371,0.652580023487596,7.30811074774828));
#9863=CARTESIAN_POINT('Ctrl Pts',(-2.45142289816278,-0.00214958505015697,
7.34217250378796));
#9864=CARTESIAN_POINT('Origin',(0.,0.,0.));
#9865=CARTESIAN_POINT('',(-2.45333810822071,0.00149720406526131,8.25782749621206));
#9866=CARTESIAN_POINT('',(-2.45347385627323,0.00142195494216932,8.14217250378797));
#9867=CARTESIAN_POINT('',(-2.4505,-3.00099698131059E-16,0.));
#9868=CARTESIAN_POINT('Ctrl Pts',(-2.45333810822071,0.00149720406526131,
8.25782749621206));
#9869=CARTESIAN_POINT('Ctrl Pts',(-2.45397968238504,0.0907038896081416,
8.2531771644171));
#9870=CARTESIAN_POINT('Ctrl Pts',(-2.44953543463151,0.179845985026688,8.24852683262215));
#9871=CARTESIAN_POINT('Ctrl Pts',(-2.4397929040988,0.268405208558051,8.24387650082719));
#9872=CARTESIAN_POINT('Ctrl Pts',(-2.35112459859154,1.0743966561804,8.20155309840923));
#9873=CARTESIAN_POINT('Ctrl Pts',(-1.82359386603104,1.83210820223256,8.15922969599128));
#9874=CARTESIAN_POINT('Ctrl Pts',(-1.09847316630295,2.19499145187045,8.11690629357332));
#9875=CARTESIAN_POINT('Ctrl Pts',(-0.373352466574871,2.55787470150833,8.07458289115535));
#9876=CARTESIAN_POINT('Ctrl Pts',(0.549358200320791,2.52592965473193,8.03225948873738));
#9877=CARTESIAN_POINT('Ctrl Pts',(1.24764612759045,2.11376675893546,7.98993608631942));
#9878=CARTESIAN_POINT('Ctrl Pts',(1.94593405486012,1.70160386313898,7.94761268390145));
#9879=CARTESIAN_POINT('Ctrl Pts',(2.41979924250378,0.909223118322442,7.9052892814835));
#9880=CARTESIAN_POINT('Ctrl Pts',(2.45251380639982,0.0990292900622,7.86296587906554));
#9881=CARTESIAN_POINT('Ctrl Pts',(2.48522837029586,-0.711164538198042,7.82064247664758));
#9882=CARTESIAN_POINT('Ctrl Pts',(2.07679231044428,-1.53917144990198,7.77831907422961));
#9883=CARTESIAN_POINT('Ctrl Pts',(1.41400872054937,-2.00629262797885,7.73599567181165));
#9884=CARTESIAN_POINT('Ctrl Pts',(0.751225130654471,-2.47341380605572,7.69367226939369));
#9885=CARTESIAN_POINT('Ctrl Pts',(-0.165905989283751,-2.57964925050551,
7.65134886697573));
#9886=CARTESIAN_POINT('Ctrl Pts',(-0.917923804687642,-2.27641091625825,
7.60902546455777));
#9887=CARTESIAN_POINT('Ctrl Pts',(-1.66994162009153,-1.97317258201099,7.5667020621398));
#9888=CARTESIAN_POINT('Ctrl Pts',(-2.2568461309611,-1.26046046906668,7.52437865972183));
#9889=CARTESIAN_POINT('Ctrl Pts',(-2.41020957315796,-0.46424194589642,7.48205525730387));
#9890=CARTESIAN_POINT('Ctrl Pts',(-2.43947354711001,-0.312311878414712,
7.47397933693994));
#9891=CARTESIAN_POINT('Ctrl Pts',(-2.45295220973374,-0.157341326931424,
7.465903416576));
#9892=CARTESIAN_POINT('Ctrl Pts',(-2.45153584345453,-0.00212567399449221,
7.45782749621206));
#9893=CARTESIAN_POINT('Ctrl Pts',(-2.45142289816278,-0.00214958505015697,
7.34217250378796));
#9894=CARTESIAN_POINT('Ctrl Pts',(-2.45288216648111,-0.161255490008206,
7.35044985438962));
#9895=CARTESIAN_POINT('Ctrl Pts',(-2.43871804379984,-0.320102722758881,
7.35872720499128));
#9896=CARTESIAN_POINT('Ctrl Pts',(-2.40798566431321,-0.475677037637661,
7.36700455559294));
#9897=CARTESIAN_POINT('Ctrl Pts',(-2.25078784159854,-1.27144827233516,7.40934366223428));
#9898=CARTESIAN_POINT('Ctrl Pts',(-1.6601016033968,-1.98158756645051,7.45168276887562));
#9899=CARTESIAN_POINT('Ctrl Pts',(-0.9062679427176,-2.28108351878577,7.49402187551696));
#9900=CARTESIAN_POINT('Ctrl Pts',(-0.152434282038396,-2.58057947112103,
7.53636098215829));
#9901=CARTESIAN_POINT('Ctrl Pts',(0.76454680111826,-2.46943208167621,7.57870008879963));
#9902=CARTESIAN_POINT('Ctrl Pts',(1.42499805585471,-1.99851048145462,7.62103919544097));
#9903=CARTESIAN_POINT('Ctrl Pts',(2.08544931059115,-1.52758888123302,7.66337830208231));
#9904=CARTESIAN_POINT('Ctrl Pts',(2.48937073690738,-0.696893070234654,7.70571740872365));
#9905=CARTESIAN_POINT('Ctrl Pts',(2.45189850621544,0.113390118141594,7.74805651536499));
#9906=CARTESIAN_POINT('Ctrl Pts',(2.4144262755235,0.923673306517865,7.79039562200633));
#9907=CARTESIAN_POINT('Ctrl Pts',(1.93556038782336,1.71354387227202,7.83273472864767));
#9908=CARTESIAN_POINT('Ctrl Pts',(1.23446470918613,2.1214995841262,7.87507383528901));
#9909=CARTESIAN_POINT('Ctrl Pts',(0.533369030548933,2.52945529598037,7.91741294193035));
#9910=CARTESIAN_POINT('Ctrl Pts',(-0.389956439025329,2.5554961539346,7.95975204857168));
#9911=CARTESIAN_POINT('Ctrl Pts',(-1.11293079588184,2.18770396700547,8.00209115521302));
#9912=CARTESIAN_POINT('Ctrl Pts',(-1.83590515273836,1.81991178007634,8.04443026185436));
#9913=CARTESIAN_POINT('Ctrl Pts',(-2.35852839687711,1.05828654826383,8.08676936849571));
#9914=CARTESIAN_POINT('Ctrl Pts',(-2.4416101127223,0.251403383282412,8.12910847513704));
#9915=CARTESIAN_POINT('Ctrl Pts',(-2.45015526165805,0.168413561173331,8.13346315135402));
#9916=CARTESIAN_POINT('Ctrl Pts',(-2.45405067483897,0.0849449733128952,
8.13781782757099));
#9917=CARTESIAN_POINT('Ctrl Pts',(-2.45347385627323,0.00142195494216932,
8.14217250378797));
#9918=CARTESIAN_POINT('Origin',(0.,0.,0.));
#9919=CARTESIAN_POINT('',(-2.44700919659994,0.0011436434892946,9.05782749621206));
#9920=CARTESIAN_POINT('',(-2.44711631602456,0.0012525846534501,8.94217250378797));
#9921=CARTESIAN_POINT('',(-2.4505,-3.00099698131059E-16,0.));
#9922=CARTESIAN_POINT('Ctrl Pts',(-2.44700919659994,0.0011436434892946,
9.05782749621206));
#9923=CARTESIAN_POINT('Ctrl Pts',(-2.44842479019009,0.336683737405834,9.04045091225821));
#9924=CARTESIAN_POINT('Ctrl Pts',(-2.38417117353217,0.67170491204158,9.02307432830436));
#9925=CARTESIAN_POINT('Ctrl Pts',(-2.25164548110497,0.977099482290081,9.00569774435051));
#9926=CARTESIAN_POINT('Ctrl Pts',(-1.92885831958852,1.7209359766906,8.96337434193255));
#9927=CARTESIAN_POINT('Ctrl Pts',(-1.20105210951221,2.28901482807564,8.92105093951459));
#9928=CARTESIAN_POINT('Ctrl Pts',(-0.401097684339819,2.42151841175928,8.87872753709663));
#9929=CARTESIAN_POINT('Ctrl Pts',(0.398856740832569,2.55402199544293,8.83640413467867));
#9930=CARTESIAN_POINT('Ctrl Pts',(1.27095938110103,2.25095031142518,8.7940807322607));
#9931=CARTESIAN_POINT('Ctrl Pts',(1.81634371305176,1.65091680194046,8.75175732984274));
#9932=CARTESIAN_POINT('Ctrl Pts',(2.36172804500248,1.05088329245573,8.70943392742478));
#9933=CARTESIAN_POINT('Ctrl Pts',(2.58039406863547,0.153887957504024,8.66711052500682));
#9934=CARTESIAN_POINT('Ctrl Pts',(2.37233227519797,-0.6298177092826,8.62478712258885));
#9935=CARTESIAN_POINT('Ctrl Pts',(2.16427048176047,-1.41352337606922,8.58246372017089));
#9936=CARTESIAN_POINT('Ctrl Pts',(1.5294808712525,-2.08393937469077,8.54014031775292));
#9937=CARTESIAN_POINT('Ctrl Pts',(0.758292028122076,-2.33444296802438,8.49781691533496));
#9938=CARTESIAN_POINT('Ctrl Pts',(-0.0128968150083492,-2.58494656135799,
8.455493512917));
#9939=CARTESIAN_POINT('Ctrl Pts',(-0.920484890761226,-2.41553774940367,
8.41317011049905));
#9940=CARTESIAN_POINT('Ctrl Pts',(-1.54937598941065,-1.90369766883025,8.37084670808108));
#9941=CARTESIAN_POINT('Ctrl Pts',(-2.10916696603463,-1.44809659704721,8.33317363745808));
#9942=CARTESIAN_POINT('Ctrl Pts',(-2.44814061482272,-0.72118021180151,8.29550056683506));
#9943=CARTESIAN_POINT('Ctrl Pts',(-2.45333810822071,0.00149720406526131,
8.25782749621206));
#9944=CARTESIAN_POINT('Ctrl Pts',(-2.45347385627323,0.00142195494216932,
8.14217250378797));
#9945=CARTESIAN_POINT('Ctrl Pts',(-2.44844245472095,-0.727122286250471,
8.18015693421233));
#9946=CARTESIAN_POINT('Ctrl Pts',(-2.1031409456273,-1.45980787714039,8.21814136463669));
#9947=CARTESIAN_POINT('Ctrl Pts',(-1.53537261678876,-1.91501815429747,8.25612579506105));
#9948=CARTESIAN_POINT('Ctrl Pts',(-0.902513217458377,-2.42241542874561,
8.29846490170239));
#9949=CARTESIAN_POINT('Ctrl Pts',(0.00674576875401803,-2.58506887949157,
8.34080400834373));
#9950=CARTESIAN_POINT('Ctrl Pts',(0.77626128426866,-2.32853645499039,8.38314311498507));
#9951=CARTESIAN_POINT('Ctrl Pts',(1.5457767997833,-2.07200403048922,8.42548222162641));
#9952=CARTESIAN_POINT('Ctrl Pts',(2.17554884460018,-1.39628573074092,8.46782132826775));
#9953=CARTESIAN_POINT('Ctrl Pts',(2.37734791724352,-0.610639405911168,8.51016043490908));
#9954=CARTESIAN_POINT('Ctrl Pts',(2.57914698988687,0.175006918918576,8.55249954155042));
#9955=CARTESIAN_POINT('Ctrl Pts',(2.35297309035668,1.07058126882979,8.59483864819176));
#9956=CARTESIAN_POINT('Ctrl Pts',(1.80233984845749,1.66620367132469,8.6371777548331));
#9957=CARTESIAN_POINT('Ctrl Pts',(1.2517066065583,2.2618260738196,8.67951686147444));
#9958=CARTESIAN_POINT('Ctrl Pts',(0.376614022290118,2.5574965288982,8.72185596811578));
#9959=CARTESIAN_POINT('Ctrl Pts',(-0.422431877786136,2.41789472729971,8.76419507475712));
#9960=CARTESIAN_POINT('Ctrl Pts',(-1.2214777778624,2.27829292570122,8.80653418139846));
#9961=CARTESIAN_POINT('Ctrl Pts',(-1.94447699374672,1.70341886742563,8.8488732880398));
#9962=CARTESIAN_POINT('Ctrl Pts',(-2.26053248852424,0.956376741666199,8.89121239468114));
#9963=CARTESIAN_POINT('Ctrl Pts',(-2.38733584500595,0.656658968854799,8.90819909771675));
#9964=CARTESIAN_POINT('Ctrl Pts',(-2.4486349994353,0.32922794899108,8.92518580075236));
#9965=CARTESIAN_POINT('Ctrl Pts',(-2.44711631602456,0.0012525846534501,
8.94217250378797));
#9966=CARTESIAN_POINT('Origin',(0.,0.,0.));
#9967=CARTESIAN_POINT('',(-2.44916657089282,-0.00214086048378637,9.85782749621207));
#9968=CARTESIAN_POINT('',(-2.44890296710392,-0.00209289085269487,9.74217250378797));
#9969=CARTESIAN_POINT('',(-2.4505,-3.00099698131059E-16,0.));
#9970=CARTESIAN_POINT('Ctrl Pts',(-2.44916657089282,-0.00214086048378637,
9.85782749621207));
#9971=CARTESIAN_POINT('Ctrl Pts',(-2.4443000397846,0.577853720703854,9.82772466009932));
#9972=CARTESIAN_POINT('Ctrl Pts',(-2.23817293760382,1.16095889116584,9.79762182398657));
#9973=CARTESIAN_POINT('Ctrl Pts',(-1.86255786053494,1.59859594239178,9.76751898787382));
#9974=CARTESIAN_POINT('Ctrl Pts',(-1.33445785024021,2.21389640652993,9.72519558545586));
#9975=CARTESIAN_POINT('Ctrl Pts',(-0.471326673231223,2.54164636014034,9.68287218303791));
#9976=CARTESIAN_POINT('Ctrl Pts',(0.332072352589864,2.43194546063792,9.64054878061995));
#9977=CARTESIAN_POINT('Ctrl Pts',(1.13547137841094,2.3222445611355,9.59822537820198));
#9978=CARTESIAN_POINT('Ctrl Pts',(1.87913825304411,1.77509280852021,9.55590197578401));
#9979=CARTESIAN_POINT('Ctrl Pts',(2.22294807929644,1.04073656975442,9.51357857336605));
#9980=CARTESIAN_POINT('Ctrl Pts',(2.56675790554877,0.306380330988639,9.47125517094809));
#9981=CARTESIAN_POINT('Ctrl Pts',(2.51071068342031,-0.615180393927636,9.42893176853014));
#9982=CARTESIAN_POINT('Ctrl Pts',(2.08044027709761,-1.30245883785323,9.38660836611217));
#9983=CARTESIAN_POINT('Ctrl Pts',(1.65016987077491,-1.98973728177882,9.34428496369421));
#9984=CARTESIAN_POINT('Ctrl Pts',(0.845676280257953,-2.44273344471371,9.30196156127624));
#9985=CARTESIAN_POINT('Ctrl Pts',(0.0349042252868802,-2.45426413939679,
9.25963815885828));
#9986=CARTESIAN_POINT('Ctrl Pts',(-0.775867829684193,-2.46579483407987,
9.21731475644032));
#9987=CARTESIAN_POINT('Ctrl Pts',(-1.5929183491094,-2.03586006051114,9.17499135402236));
#9988=CARTESIAN_POINT('Ctrl Pts',(-2.0425595523437,-1.36109560501879,9.1326679516044));
#9989=CARTESIAN_POINT('Ctrl Pts',(-2.30759300500181,-0.963367033696284,
9.10772113314029));
#9990=CARTESIAN_POINT('Ctrl Pts',(-2.44497688942113,-0.480576919804305,
9.08277431467618));
#9991=CARTESIAN_POINT('Ctrl Pts',(-2.44700919659994,0.0011436434892946,
9.05782749621206));
#9992=CARTESIAN_POINT('Ctrl Pts',(-2.44711631602456,0.0012525846534501,
8.94217250378797));
#9993=CARTESIAN_POINT('Ctrl Pts',(-2.44484970344542,-0.488245806646622,
8.9675249073937));
#9994=CARTESIAN_POINT('Ctrl Pts',(-2.30265559068752,-0.978956731903437,
8.99287731099942));
#9995=CARTESIAN_POINT('Ctrl Pts',(-2.02946487371307,-1.38055638423009,9.01822971460515));
#9996=CARTESIAN_POINT('Ctrl Pts',(-1.57322999045366,-2.0512371911237,9.06056882124649));
#9997=CARTESIAN_POINT('Ctrl Pts',(-0.751648450264089,-2.4733886116677,9.10290792788784));
#9998=CARTESIAN_POINT('Ctrl Pts',(0.0592642668109431,-2.45380344574561,
9.14524703452917));
#9999=CARTESIAN_POINT('Ctrl Pts',(0.870176983885975,-2.43421827982352,9.18758614117051));
#10000=CARTESIAN_POINT('Ctrl Pts',(1.67042087784649,-1.97289652743534,9.22992524781184));
#10001=CARTESIAN_POINT('Ctrl Pts',(2.09374612780316,-1.28097258205744,9.27226435445318));
#10002=CARTESIAN_POINT('Ctrl Pts',(2.51707137775985,-0.589048636679533,
9.31460346109452));
#10003=CARTESIAN_POINT('Ctrl Pts',(2.56347798371271,0.333477501688088,9.35694256773587));
#10004=CARTESIAN_POINT('Ctrl Pts',(2.21172690685546,1.06439076149939,9.39928167437721));
#10005=CARTESIAN_POINT('Ctrl Pts',(1.85997582999822,1.79530402131068,9.44162078101855));
#10006=CARTESIAN_POINT('Ctrl Pts',(1.11006707033088,2.33460440256564,9.48395988765988));
#10007=CARTESIAN_POINT('Ctrl Pts',(0.305213429580908,2.43546881853928,9.52629899430122));
#10008=CARTESIAN_POINT('Ctrl Pts',(-0.499640211169086,2.53633323451293,
9.56863810094255));
#10009=CARTESIAN_POINT('Ctrl Pts',(-1.35943873300173,2.19876168520523,9.6109772075839));
#10010=CARTESIAN_POINT('Ctrl Pts',(-1.88067578491744,1.57725146875786,9.65331631422524));
#10011=CARTESIAN_POINT('Ctrl Pts',(-2.24531218505443,1.14246801055816,9.68293504407948));
#10012=CARTESIAN_POINT('Ctrl Pts',(-2.44426212764736,0.568729602967145,
9.71255377393372));
#10013=CARTESIAN_POINT('Ctrl Pts',(-2.44890296710392,-0.00209289085269486,
9.74217250378797));
#10014=CARTESIAN_POINT('Origin',(0.,0.,0.));
#10015=CARTESIAN_POINT('',(-2.45449565980291,0.000180539251598464,10.6578274962121));
#10016=CARTESIAN_POINT('',(-2.45451849884274,-3.1633834378794E-5,10.542172503788));
#10017=CARTESIAN_POINT('',(-2.4505,-3.00099698131059E-16,0.));
#10018=CARTESIAN_POINT('Ctrl Pts',(-2.45449565980291,0.000180539251598464,
10.6578274962121));
#10019=CARTESIAN_POINT('Ctrl Pts',(-2.45450594062414,0.00986891292668717,
10.6573218103584));
#10020=CARTESIAN_POINT('Ctrl Pts',(-2.45445353368688,0.0195571722527011,
10.6568161245047));
#10021=CARTESIAN_POINT('Ctrl Pts',(-2.45433810212205,0.0292446806083813,
10.656310438651));
#10022=CARTESIAN_POINT('Ctrl Pts',(-2.44467705162092,0.840041169343448,
10.6139870362331));
#10023=CARTESIAN_POINT('Ctrl Pts',(-1.99353722868095,1.6455772150759,10.5716636338151));
#10024=CARTESIAN_POINT('Ctrl Pts',(-1.30725280137001,2.07743131876416,10.5293402313971));
#10025=CARTESIAN_POINT('Ctrl Pts',(-0.620968374059076,2.50928542245243,
10.4870168289792));
#10026=CARTESIAN_POINT('Ctrl Pts',(0.300460657622818,2.56745758409652,10.4446934265612));
#10027=CARTESIAN_POINT('Ctrl Pts',(1.03560775800279,2.22534207312862,10.4023700241433));
#10028=CARTESIAN_POINT('Ctrl Pts',(1.77075485838276,1.88322656216073,10.3600466217253));
#10029=CARTESIAN_POINT('Ctrl Pts',(2.31962002746079,1.14082337858087,10.3177232193073));
#10030=CARTESIAN_POINT('Ctrl Pts',(2.43117324686004,0.337679455436603,10.2753998168894));
#10031=CARTESIAN_POINT('Ctrl Pts',(2.54272646625929,-0.46546446770764,10.2330764144714));
#10032=CARTESIAN_POINT('Ctrl Pts',(2.21696773597977,-1.3293491304163,10.1907530120535));
#10033=CARTESIAN_POINT('Ctrl Pts',(1.60288668891411,-1.85886659913344,10.1484296096355));
#10034=CARTESIAN_POINT('Ctrl Pts',(0.988805641848436,-2.3883840678506,10.1061062072175));
#10035=CARTESIAN_POINT('Ctrl Pts',(0.086402277996615,-2.58353434257624,
10.0637828047996));
#10036=CARTESIAN_POINT('Ctrl Pts',(-0.691598482618519,-2.3550631222351,
10.0214594023816));
#10037=CARTESIAN_POINT('Ctrl Pts',(-1.46959924323365,-2.12659190189395,
9.97913599996364));
#10038=CARTESIAN_POINT('Ctrl Pts',(-2.12319740061209,-1.47449918648602,
9.93681259754568));
#10039=CARTESIAN_POINT('Ctrl Pts',(-2.35346205751109,-0.697027341449118,
9.89448919512772));
#10040=CARTESIAN_POINT('Ctrl Pts',(-2.41994925718359,-0.472538153673385,
9.8822686288225));
#10041=CARTESIAN_POINT('Ctrl Pts',(-2.45114219092616,-0.237595825907136,
9.87004806251728));
#10042=CARTESIAN_POINT('Ctrl Pts',(-2.44916657089282,-0.00214086048378637,
9.85782749621207));
#10043=CARTESIAN_POINT('Ctrl Pts',(-2.44890296710392,-0.00209289085269486,
9.74217250378797));
#10044=CARTESIAN_POINT('Ctrl Pts',(-2.45089607169639,-0.247244429614459,
9.75489288057506));
#10045=CARTESIAN_POINT('Ctrl Pts',(-2.41704981698823,-0.491858142409003,
9.76761325736216));
#10046=CARTESIAN_POINT('Ctrl Pts',(-2.3450968955658,-0.724695904556749,
9.78033363414925));
#10047=CARTESIAN_POINT('Ctrl Pts',(-2.10560537229968,-1.49968417783698,
9.82267274079059));
#10048=CARTESIAN_POINT('Ctrl Pts',(-1.44394674376867,-2.14421184081045,
9.86501184743193));
#10049=CARTESIAN_POINT('Ctrl Pts',(-0.6629441317963,-2.36329614771203,9.90735095407327));
#10050=CARTESIAN_POINT('Ctrl Pts',(0.118058480176069,-2.58238045461361,
9.94969006071461));
#10051=CARTESIAN_POINT('Ctrl Pts',(1.01840507558981,-2.37602140544331,9.99202916735595));
#10052=CARTESIAN_POINT('Ctrl Pts',(1.62603155524061,-1.83866391301822,10.0343682739973));
#10053=CARTESIAN_POINT('Ctrl Pts',(2.23365803489143,-1.30130642059312,10.0767073806386));
#10054=CARTESIAN_POINT('Ctrl Pts',(2.5485643987793,-0.432950484913232,10.11904648728));
#10055=CARTESIAN_POINT('Ctrl Pts',(2.42662658642559,0.368981047922729,10.1613855939213));
#10056=CARTESIAN_POINT('Ctrl Pts',(2.30468877407188,1.17091258075867,10.2037247005626));
#10057=CARTESIAN_POINT('Ctrl Pts',(1.74590678547659,1.90641971075067,10.246063807204));
#10058=CARTESIAN_POINT('Ctrl Pts',(1.00601990810412,2.23888086958012,10.2884029138453));
#10059=CARTESIAN_POINT('Ctrl Pts',(0.266133030731654,2.57134202840957,10.3307420204867));
#10060=CARTESIAN_POINT('Ctrl Pts',(-0.654858735418012,2.50075721607648,
10.373081127128));
#10061=CARTESIAN_POINT('Ctrl Pts',(-1.33544255914608,2.05943117750874,10.4154202337693));
#10062=CARTESIAN_POINT('Ctrl Pts',(-2.01460619326385,1.61902606393638,10.4576709904422));
#10063=CARTESIAN_POINT('Ctrl Pts',(-2.45436416747304,0.809425377921695,
10.4999217471151));
#10064=CARTESIAN_POINT('Ctrl Pts',(-2.45451849884274,-3.1633834378794E-5,
10.542172503788));
#10065=CARTESIAN_POINT('Origin',(0.,0.,0.));
#10066=CARTESIAN_POINT('',(-2.44864274206392,0.00202326491164903,11.4578274962121));
#10067=CARTESIAN_POINT('',(-2.44899529462048,0.00211273287450485,11.342172503788));
#10068=CARTESIAN_POINT('',(-2.4505,-3.00099698131059E-16,0.));
#10069=CARTESIAN_POINT('Ctrl Pts',(-2.44864274206392,0.00202326491164903,
11.4578274962121));
#10070=CARTESIAN_POINT('Ctrl Pts',(-2.45063313417738,0.25710244065764,11.4445955581995));
#10071=CARTESIAN_POINT('Ctrl Pts',(-2.41394631700749,0.511623348699365,
11.4313636201869));
#10072=CARTESIAN_POINT('Ctrl Pts',(-2.33618535765509,0.752906863795201,
11.4181316821743));
#10073=CARTESIAN_POINT('Ctrl Pts',(-2.08746076629505,1.52467130952633,11.3758082797564));
#10074=CARTESIAN_POINT('Ctrl Pts',(-1.41851035397114,2.16100518939464,11.3334848773384));
#10075=CARTESIAN_POINT('Ctrl Pts',(-0.63528655446768,2.37087362897826,11.2911614749205));
#10076=CARTESIAN_POINT('Ctrl Pts',(0.147937245035775,2.58074206856189,11.2488380725025));
#10077=CARTESIAN_POINT('Ctrl Pts',(1.04543443171877,2.36414506786083,11.2065146700845));
#10078=CARTESIAN_POINT('Ctrl Pts',(1.64672398408625,1.82014584336175,11.1641912676666));
#10079=CARTESIAN_POINT('Ctrl Pts',(2.24801353645374,1.27614661886266,11.1218678652486));
#10080=CARTESIAN_POINT('Ctrl Pts',(2.55309545450571,0.404745170565546,11.0795444628307));
#10081=CARTESIAN_POINT('Ctrl Pts',(2.42243689154382,-0.395512676610367,
11.0372210604127));
#10082=CARTESIAN_POINT('Ctrl Pts',(2.29177832858192,-1.19577052378629,10.9948976579947));
#10083=CARTESIAN_POINT('Ctrl Pts',(1.72537928460614,-1.92488476984101,10.9525742555768));
#10084=CARTESIAN_POINT('Ctrl Pts',(0.982289104388552,-2.24938633548608,
10.9102508531588));
#10085=CARTESIAN_POINT('Ctrl Pts',(0.239198924170983,-2.57388790113114,
10.8679274507408));
#10086=CARTESIAN_POINT('Ctrl Pts',(-0.680582392288389,-2.49377678636659,
10.8256040483229));
#10087=CARTESIAN_POINT('Ctrl Pts',(-1.35638191148693,-2.04569276311548,
10.7832806459049));
#10088=CARTESIAN_POINT('Ctrl Pts',(-2.02410688475446,-1.60296250961991,
10.7414629293406));
#10089=CARTESIAN_POINT('Ctrl Pts',(-2.45364548678456,-0.800999998758872,
10.6996452127763));
#10090=CARTESIAN_POINT('Ctrl Pts',(-2.45449565980291,0.000180539251598464,
10.6578274962121));
#10091=CARTESIAN_POINT('Ctrl Pts',(-2.45451849884274,-3.1633834378794E-5,
10.542172503788));
#10092=CARTESIAN_POINT('Ctrl Pts',(-2.45467347565279,-0.812873934143394,
10.5845999603978));
#10093=CARTESIAN_POINT('Ctrl Pts',(-2.01069613156042,-1.6255695989997,10.6270274170076));
#10094=CARTESIAN_POINT('Ctrl Pts',(-1.32685678597742,-2.06497328631131,
10.6694548736174));
#10095=CARTESIAN_POINT('Ctrl Pts',(-0.64444145185873,-2.50346196940119,
10.7117939802587));
#10096=CARTESIAN_POINT('Ctrl Pts',(0.276836203683142,-2.57021172930212,
10.7541330869));
#10097=CARTESIAN_POINT('Ctrl Pts',(1.01533250566608,-2.23467302006614,10.7964721935414));
#10098=CARTESIAN_POINT('Ctrl Pts',(1.753828807649,-1.89913431083016,10.8388113001827));
#10099=CARTESIAN_POINT('Ctrl Pts',(2.30954375607297,-1.1613071324573,10.8811504068241));
#10100=CARTESIAN_POINT('Ctrl Pts',(2.42814176417273,-0.358874876180815,
10.9234895134654));
#10101=CARTESIAN_POINT('Ctrl Pts',(2.54673977227249,0.44355738009568,10.9658286201067));
#10102=CARTESIAN_POINT('Ctrl Pts',(2.22822084004799,1.31059471427581,11.0081677267481));
#10103=CARTESIAN_POINT('Ctrl Pts',(1.61836240205076,1.84541776823085,11.0505068333894));
#10104=CARTESIAN_POINT('Ctrl Pts',(1.00850396405353,2.3802408221859,11.0928459400307));
#10105=CARTESIAN_POINT('Ctrl Pts',(0.107306020283557,2.58284959591588,11.1351850466721));
#10106=CARTESIAN_POINT('Ctrl Pts',(-0.67277769111436,2.36051557546492,11.1775241533134));
#10107=CARTESIAN_POINT('Ctrl Pts',(-1.45286140251225,2.13818155501397,11.2198632599548));
#10108=CARTESIAN_POINT('Ctrl Pts',(-2.11183088153809,1.49090474038213,11.2622023665961));
#10109=CARTESIAN_POINT('Ctrl Pts',(-2.34809375680837,0.714926089124754,
11.3045414732374));
#10110=CARTESIAN_POINT('Ctrl Pts',(-2.41809063190044,0.485029281748485,
11.3170851500876));
#10111=CARTESIAN_POINT('Ctrl Pts',(-2.45098481963534,0.243835787818979,
11.3296288269378));
#10112=CARTESIAN_POINT('Ctrl Pts',(-2.44899529462048,0.00211273287450485,
11.342172503788));
#10113=CARTESIAN_POINT('Origin',(0.,0.,0.));
#10114=CARTESIAN_POINT('',(-2.44731685610913,-0.00140773067336952,12.2578274962121));
#10115=CARTESIAN_POINT('',(-2.4470647235883,-0.0012054690616184,12.142172503788));
#10116=CARTESIAN_POINT('',(-2.4505,-3.00099698131059E-16,0.));
#10117=CARTESIAN_POINT('Ctrl Pts',(-2.44731685610913,-0.00140773067336952,
12.2578274962121));
#10118=CARTESIAN_POINT('Ctrl Pts',(-2.4446942722333,0.499684558237575,12.2318693060406));
#10119=CARTESIAN_POINT('Ctrl Pts',(-2.29510898968982,1.00221422879886,12.2059111158691));
#10120=CARTESIAN_POINT('Ctrl Pts',(-2.00954795106829,1.40937851666229,12.1799529256977));
#10121=CARTESIAN_POINT('Ctrl Pts',(-1.54395637196988,2.0732375103609,12.1376295232797));
#10122=CARTESIAN_POINT('Ctrl Pts',(-0.716893501761423,2.48358184081904,
12.0953061208618));
#10123=CARTESIAN_POINT('Ctrl Pts',(0.0933736111014519,2.4527356440558,12.0529827184438));
#10124=CARTESIAN_POINT('Ctrl Pts',(0.903640723964315,2.42188944729257,12.0106593160258));
#10125=CARTESIAN_POINT('Ctrl Pts',(1.6971120794816,1.94985272330796,11.9683359136078));
#10126=CARTESIAN_POINT('Ctrl Pts',(2.11088410829111,1.25251708660442,11.9260125111899));
#10127=CARTESIAN_POINT('Ctrl Pts',(2.52465613710063,0.55518144990085,11.8836891087719));
#10128=CARTESIAN_POINT('Ctrl Pts',(2.55872883920235,-0.367453099521673,
11.841365706354));
#10129=CARTESIAN_POINT('Ctrl Pts',(2.19751865871293,-1.09340866810195,11.799042303936));
#10130=CARTESIAN_POINT('Ctrl Pts',(1.83630847822352,-1.81936423668222,11.7567189015181));
#10131=CARTESIAN_POINT('Ctrl Pts',(1.07981541514298,-2.34864082442025,11.7143954991001));
#10132=CARTESIAN_POINT('Ctrl Pts',(0.274030576624401,-2.43916748378353,
11.6720720966821));
#10133=CARTESIAN_POINT('Ctrl Pts',(-0.531754261894183,-2.5296941431468,
11.6297486942642));
#10134=CARTESIAN_POINT('Ctrl Pts',(-1.38683087585082,-2.18147087413532,
11.5874252918462));
#10135=CARTESIAN_POINT('Ctrl Pts',(-1.90011979763105,-1.5537617338326,11.5451018894282));
#10136=CARTESIAN_POINT('Ctrl Pts',(-2.25293468359385,-1.12229882988837,
11.5160104250228));
#10137=CARTESIAN_POINT('Ctrl Pts',(-2.44426670725582,-0.558788519025065,
11.4869189606174));
#10138=CARTESIAN_POINT('Ctrl Pts',(-2.44864274206392,0.00202326491164903,
11.4578274962121));
#10139=CARTESIAN_POINT('Ctrl Pts',(-2.44899529462048,0.00211273287450485,
11.342172503788));
#10140=CARTESIAN_POINT('Ctrl Pts',(-2.44426950699009,-0.572060406192228,
11.3719679335791));
#10141=CARTESIAN_POINT('Ctrl Pts',(-2.24272232871244,-1.14922144210772,
11.4017633633703));
#10142=CARTESIAN_POINT('Ctrl Pts',(-1.87409278465252,-1.58506777084989,
11.4315587931615));
#10143=CARTESIAN_POINT('Ctrl Pts',(-1.35027266571165,-2.20440249168428,
11.4738978998028));
#10144=CARTESIAN_POINT('Ctrl Pts',(-0.489076156315162,-2.53839144547012,
11.5162370064441));
#10145=CARTESIAN_POINT('Ctrl Pts',(0.315350571729276,-2.43417699039813,
11.5585761130855));
#10146=CARTESIAN_POINT('Ctrl Pts',(1.1197772997737,-2.32996253532614,11.6009152197268));
#10147=CARTESIAN_POINT('Ctrl Pts',(1.8674342464661,-1.78754467139634,11.6432543263682));
#10148=CARTESIAN_POINT('Ctrl Pts',(2.21613920350807,-1.05517327219197,11.6855934330095));
#10149=CARTESIAN_POINT('Ctrl Pts',(2.56484416055002,-0.322801872987598,
11.7279325396508));
#10150=CARTESIAN_POINT('Ctrl Pts',(2.51459712794155,0.599523061491336,11.7702716462922));
#10151=CARTESIAN_POINT('Ctrl Pts',(2.08839480310448,1.28967854523516,11.8126107529335));
#10152=CARTESIAN_POINT('Ctrl Pts',(1.66219247826739,1.97983402897899,11.8549498595748));
#10153=CARTESIAN_POINT('Ctrl Pts',(0.860034861201667,2.4378200619877,11.8972889662162));
#10154=CARTESIAN_POINT('Ctrl Pts',(0.0490476317064056,2.45402891863516,
11.9396280728575));
#10155=CARTESIAN_POINT('Ctrl Pts',(-0.761939597788844,2.47023777528262,
11.9819671794989));
#10156=CARTESIAN_POINT('Ctrl Pts',(-1.58175643971363,2.04466945556887,12.0243062861402));
#10157=CARTESIAN_POINT('Ctrl Pts',(-2.03519506832506,1.37209498123819,12.0666453927815));
#10158=CARTESIAN_POINT('Ctrl Pts',(-2.30481900353504,0.972168364826713,
12.0918210964503));
#10159=CARTESIAN_POINT('Ctrl Pts',(-2.44490126731575,0.484906887990491,
12.1169968001192));
#10160=CARTESIAN_POINT('Ctrl Pts',(-2.4470647235883,-0.0012054690616184,
12.142172503788));
#10161=CARTESIAN_POINT('Origin',(0.,0.,0.));
#10162=CARTESIAN_POINT('',(-2.45375856134309,-0.00121882424236025,13.0578274962121));
#10163=CARTESIAN_POINT('',(-2.45339670897876,-0.00146880086599289,12.942172503788));
#10164=CARTESIAN_POINT('',(-2.4505,-3.00099698131059E-16,0.));
#10165=CARTESIAN_POINT('Ctrl Pts',(-2.45375856134309,-0.00121882424236025,
13.0578274962121));
#10166=CARTESIAN_POINT('Ctrl Pts',(-2.44923208495134,0.740524702851974,
13.0191430538817));
#10167=CARTESIAN_POINT('Ctrl Pts',(-2.08937875229641,1.48607239035232,12.9804586115513));
#10168=CARTESIAN_POINT('Ctrl Pts',(-1.50357549119931,1.94007513079693,12.941774169221));
#10169=CARTESIAN_POINT('Ctrl Pts',(-0.862667010590097,2.4367849067477,12.899450766803));
#10170=CARTESIAN_POINT('Ctrl Pts',(0.0486999946819842,2.58451994835246,
12.8571273643851));
#10171=CARTESIAN_POINT('Ctrl Pts',(0.813700976493747,2.31571187580085,12.8148039619671));
#10172=CARTESIAN_POINT('Ctrl Pts',(1.57870195830553,2.04690380324923,12.7724805595491));
#10173=CARTESIAN_POINT('Ctrl Pts',(2.197336916657,1.3615526165412,12.7301571571312));
#10174=CARTESIAN_POINT('Ctrl Pts',(2.38666578955733,0.573111838848801,12.6878337547132));
#10175=CARTESIAN_POINT('Ctrl Pts',(2.57599466245766,-0.2153289388436,12.6455103522952));
#10176=CARTESIAN_POINT('Ctrl Pts',(2.33601744990688,-1.10685930752036,12.6031869498773));
#10177=CARTESIAN_POINT('Ctrl Pts',(1.77649058658243,-1.69372724092635,12.5608635474593));
#10178=CARTESIAN_POINT('Ctrl Pts',(1.216963723258,-2.28059517433232,12.5185401450414));
#10179=CARTESIAN_POINT('Ctrl Pts',(0.337887209159924,-2.56280067246752,
12.4762167426234));
#10180=CARTESIAN_POINT('Ctrl Pts',(-0.458682848089992,-2.41127369158709,
12.4338933402054));
#10181=CARTESIAN_POINT('Ctrl Pts',(-1.25525290533992,-2.25974671070665,
12.3915699377875));
#10182=CARTESIAN_POINT('Ctrl Pts',(-1.9693165057417,-1.67448725081058,12.3492465353695));
#10183=CARTESIAN_POINT('Ctrl Pts',(-2.27428816194839,-0.923170692393001,
12.3069231329516));
#10184=CARTESIAN_POINT('Ctrl Pts',(-2.39221171246308,-0.632658724064287,
12.2905579207051));
#10185=CARTESIAN_POINT('Ctrl Pts',(-2.44897025110618,-0.317318878906041,
12.2741927084586));
#10186=CARTESIAN_POINT('Ctrl Pts',(-2.44731685610913,-0.00140773067336952,
12.2578274962121));
#10187=CARTESIAN_POINT('Ctrl Pts',(-2.4470647235883,-0.0012054690616184,
12.142172503788));
#10188=CARTESIAN_POINT('Ctrl Pts',(-2.44853964847253,-0.332610000341817,
12.1593359067605));
#10189=CARTESIAN_POINT('Ctrl Pts',(-2.38591324110648,-0.663480448487108,
12.176499309733));
#10190=CARTESIAN_POINT('Ctrl Pts',(-2.25653113483059,-0.965779913444993,
12.1936627127056));
#10191=CARTESIAN_POINT('Ctrl Pts',(-1.93736815742667,-1.71149970484984,
12.2360018193469));
#10192=CARTESIAN_POINT('Ctrl Pts',(-1.21198178732078,-2.2833586587119,12.2783409259882));
#10193=CARTESIAN_POINT('Ctrl Pts',(-0.412361596856918,-2.41963251695609,
12.3206800326296));
#10194=CARTESIAN_POINT('Ctrl Pts',(0.387258593606936,-2.55590637520028,
12.3630191392709));
#10195=CARTESIAN_POINT('Ctrl Pts',(1.26111260442874,-2.25659513782664,12.4053582459123));
#10196=CARTESIAN_POINT('Ctrl Pts',(1.80926127035868,-1.65868540092863,12.4476973525536));
#10197=CARTESIAN_POINT('Ctrl Pts',(2.3574099362886,-1.06077566403063,12.4900364591949));
#10198=CARTESIAN_POINT('Ctrl Pts',(2.57985325732663,-0.164267427608244,
12.5323755658363));
#10199=CARTESIAN_POINT('Ctrl Pts',(2.37478498777309,0.620531921436152,12.5747146724776));
#10200=CARTESIAN_POINT('Ctrl Pts',(2.16971671821954,1.40533127048057,12.6170537791189));
#10201=CARTESIAN_POINT('Ctrl Pts',(1.53713685807443,2.078421732147,12.6593928857603));
#10202=CARTESIAN_POINT('Ctrl Pts',(0.766559969366697,2.33174814614233,12.7017319924016));
#10203=CARTESIAN_POINT('Ctrl Pts',(-0.00401691934101722,2.58507456013765,
12.744071099043));
#10204=CARTESIAN_POINT('Ctrl Pts',(-0.912590836611347,2.41863692646186,
12.7864102056843));
#10205=CARTESIAN_POINT('Ctrl Pts',(-1.54333226224883,1.90860921405498,12.8287493123256));
#10206=CARTESIAN_POINT('Ctrl Pts',(-2.10656809123738,1.45316761829443,12.8665570428131));
#10207=CARTESIAN_POINT('Ctrl Pts',(-2.44825947251039,0.723746281051334,
12.9043647733005));
#10208=CARTESIAN_POINT('Ctrl Pts',(-2.45339670897876,-0.00146880086599289,
12.942172503788));
#10209=CARTESIAN_POINT('Origin',(0.,0.,0.));
#10210=CARTESIAN_POINT('',(-2.45094795586712,0.0022061736527193,13.8578274962121));
#10211=CARTESIAN_POINT('',(-2.45152510826581,0.00213207818356079,13.742172503788));
#10212=CARTESIAN_POINT('',(-2.4505,-3.00099698131059E-16,0.));
#10213=CARTESIAN_POINT('Ctrl Pts',(-2.45094795586712,0.0022061736527193,
13.8578274962121));
#10214=CARTESIAN_POINT('Ctrl Pts',(-2.45256019575125,0.176967728202779,
13.8487402041408));
#10215=CARTESIAN_POINT('Ctrl Pts',(-2.43545641918873,0.351416146632857,
13.8396529120695));
#10216=CARTESIAN_POINT('Ctrl Pts',(-2.39846348572391,0.52153971902537,13.8305656199982));
#10217=CARTESIAN_POINT('Ctrl Pts',(-2.22617158651246,1.31387789399109,13.7882422175802));
#10218=CARTESIAN_POINT('Ctrl Pts',(-1.62245146862923,2.01240311191786,13.7459188151623));
#10219=CARTESIAN_POINT('Ctrl Pts',(-0.863421714241279,2.29763654964152,
13.7035954127443));
#10220=CARTESIAN_POINT('Ctrl Pts',(-0.104391959853312,2.58286998736519,
13.6612720103263));
#10221=CARTESIAN_POINT('Ctrl Pts',(0.809947431039378,2.45481164488573,13.6189486079084));
#10222=CARTESIAN_POINT('Ctrl Pts',(1.46141245436887,1.97203052945118,13.5766252054904));
#10223=CARTESIAN_POINT('Ctrl Pts',(2.11287747769833,1.48924941401666,13.5343018030724));
#10224=CARTESIAN_POINT('Ctrl Pts',(2.50146813346461,0.651745525627052,13.4919784006545));
#10225=CARTESIAN_POINT('Ctrl Pts',(2.44945785974733,-0.157438763314421,
13.4496549982365));
#10226=CARTESIAN_POINT('Ctrl Pts',(2.39744758603005,-0.966623052255928,
13.4073315958186));
#10227=CARTESIAN_POINT('Ctrl Pts',(1.90483638282921,-1.74748774174929,13.3650081934006));
#10228=CARTESIAN_POINT('Ctrl Pts',(1.19692584762066,-2.14289507119913,13.3226847909826));
#10229=CARTESIAN_POINT('Ctrl Pts',(0.489015312412128,-2.53830240064897,
13.2803613885647));
#10230=CARTESIAN_POINT('Ctrl Pts',(-0.434194554804115,-2.54825237005527,
13.2380379861467));
#10231=CARTESIAN_POINT('Ctrl Pts',(-1.1504627320257,-2.16819424247273,13.1957145837288));
#10232=CARTESIAN_POINT('Ctrl Pts',(-1.86673090924731,-1.78813611489019,
13.1533911813108));
#10233=CARTESIAN_POINT('Ctrl Pts',(-2.37605739647428,-1.0180698903188,13.1110677788928));
#10234=CARTESIAN_POINT('Ctrl Pts',(-2.44549566211458,-0.210194522884695,
13.0687443764749));
#10235=CARTESIAN_POINT('Ctrl Pts',(-2.45146595426458,-0.140733514319843,
13.0651054163873));
#10236=CARTESIAN_POINT('Ctrl Pts',(-2.4541843569843,-0.0709930003124499,
13.0614664562997));
#10237=CARTESIAN_POINT('Ctrl Pts',(-2.45375856134309,-0.00121882424236025,
13.0578274962121));
#10238=CARTESIAN_POINT('Ctrl Pts',(-2.45339670897876,-0.00146880086599289,
12.942172503788));
#10239=CARTESIAN_POINT('Ctrl Pts',(-2.45401242302797,-0.0883881236149842,
12.9467038799419));
#10240=CARTESIAN_POINT('Ctrl Pts',(-2.44979361045224,-0.17524702442689,
12.9512352560958));
#10241=CARTESIAN_POINT('Ctrl Pts',(-2.44054226314134,-0.261566560352387,
12.9557666322497));
#10242=CARTESIAN_POINT('Ctrl Pts',(-2.35410190439172,-1.06809683121483,
12.998105738891));
#10243=CARTESIAN_POINT('Ctrl Pts',(-1.82831225288784,-1.82753958180174,
13.0404448455323));
#10244=CARTESIAN_POINT('Ctrl Pts',(-1.10381290256112,-2.19231856257553,
13.0827839521737));
#10245=CARTESIAN_POINT('Ctrl Pts',(-0.379313552234399,-2.55709754334934,
13.125123058815));
#10246=CARTESIAN_POINT('Ctrl Pts',(0.543895496915153,-2.52721275431003,
13.1674621654564));
#10247=CARTESIAN_POINT('Ctrl Pts',(1.24328662368826,-2.11634164893845,13.2098012720977));
#10248=CARTESIAN_POINT('Ctrl Pts',(1.94267775046136,-1.70547054356687,13.252140378739));
#10249=CARTESIAN_POINT('Ctrl Pts',(2.41825095485799,-0.913613121863004,
13.2944794853804));
#10250=CARTESIAN_POINT('Ctrl Pts',(2.45234934221823,-0.103180944924282,
13.3368185920217));
#10251=CARTESIAN_POINT('Ctrl Pts',(2.48644772957847,0.707251232014451,13.379157698663));
#10252=CARTESIAN_POINT('Ctrl Pts',(2.07907129990229,1.53625816418806,13.4214968053044));
#10253=CARTESIAN_POINT('Ctrl Pts',(1.41666514265488,2.00442597200802,13.4638359119457));
#10254=CARTESIAN_POINT('Ctrl Pts',(0.75425898540748,2.47259377982796,13.5061750185871));
#10255=CARTESIAN_POINT('Ctrl Pts',(-0.163176899411125,2.57992246329428,
13.5485141252284));
#10256=CARTESIAN_POINT('Ctrl Pts',(-0.915757110577525,2.27729060905725,
13.5908532318697));
#10257=CARTESIAN_POINT('Ctrl Pts',(-1.66833732174391,1.97465875482023,13.6331923385111));
#10258=CARTESIAN_POINT('Ctrl Pts',(-2.25606185925809,1.26206636287986,13.6755314451524));
#10259=CARTESIAN_POINT('Ctrl Pts',(-2.40994521979868,0.465647550453306,
13.7178705517938));
#10260=CARTESIAN_POINT('Ctrl Pts',(-2.43938739384867,0.313270443469298,
13.7259712024585));
#10261=CARTESIAN_POINT('Ctrl Pts',(-2.45294822593746,0.157824757199172,
13.7340718531232));
#10262=CARTESIAN_POINT('Ctrl Pts',(-2.45152510826581,0.00213207818356079,
13.742172503788));
#10263=CARTESIAN_POINT('Origin',(0.,0.,0.));
#10264=CARTESIAN_POINT('',(-2.44650205703081,-0.000206129442867353,14.6578274962121));
#10265=CARTESIAN_POINT('',(-2.44648675330186,0.00013847494270713,14.542172503788));
#10266=CARTESIAN_POINT('',(-2.4505,-3.00099698131059E-16,0.));
#10267=CARTESIAN_POINT('Ctrl Pts',(-2.44650205703081,-0.000206129442867353,
14.6578274962121));
#10268=CARTESIAN_POINT('Ctrl Pts',(-2.44618553699062,0.42122938413429,14.6360139519819));
#10269=CARTESIAN_POINT('Ctrl Pts',(-2.34285183903272,0.842810353195403,
14.6142004077517));
#10270=CARTESIAN_POINT('Ctrl Pts',(-2.13738885427315,1.20673097934083,14.5923868635215));
#10271=CARTESIAN_POINT('Ctrl Pts',(-1.73874237600212,1.91282252255884,14.5500634611035));
#10272=CARTESIAN_POINT('Ctrl Pts',(-0.955628979015579,2.40185101689915,
14.5077400586856));
#10273=CARTESIAN_POINT('Ctrl Pts',(-0.146214897047949,2.45015345942927,
14.4654166562676));
#10274=CARTESIAN_POINT('Ctrl Pts',(0.663199184919693,2.49845590195939,14.4230932538497));
#10275=CARTESIAN_POINT('Ctrl Pts',(1.49891395186842,2.1060322926793,14.3807698514317));
#10276=CARTESIAN_POINT('Ctrl Pts',(1.97870530738246,1.45236224042366,14.3384464490137));
#10277=CARTESIAN_POINT('Ctrl Pts',(2.4584966628965,0.798692188168016,14.2961230465958));
#10278=CARTESIAN_POINT('Ctrl Pts',(2.58236460697585,-0.116224307063184,
14.2537996441778));
#10279=CARTESIAN_POINT('Ctrl Pts',(2.29365666096027,-0.873939295663354,
14.2114762417598));
#10280=CARTESIAN_POINT('Ctrl Pts',(2.00494871494468,-1.63165428426354,14.1691528393419));
#10281=CARTESIAN_POINT('Ctrl Pts',(1.30366487883415,-2.23216776623269,14.1268294369239));
#10282=CARTESIAN_POINT('Ctrl Pts',(0.510545662655815,-2.40082775250856,
14.0845060345059));
#10283=CARTESIAN_POINT('Ctrl Pts',(-0.282573553522497,-2.56948773878442,
14.042182632088));
#10284=CARTESIAN_POINT('Ctrl Pts',(-1.16752814976861,-2.30629422936704,
13.99985922967));
#10285=CARTESIAN_POINT('Ctrl Pts',(-1.73957360762182,-1.73162190865603,
13.9575358272521));
#10286=CARTESIAN_POINT('Ctrl Pts',(-2.18879472110326,-1.28033794817224,
13.9242997169054));
#10287=CARTESIAN_POINT('Ctrl Pts',(-2.44505130565783,-0.636971511603942,
13.8910636065587));
#10288=CARTESIAN_POINT('Ctrl Pts',(-2.45094795586712,0.0022061736527193,
13.8578274962121));
#10289=CARTESIAN_POINT('Ctrl Pts',(-2.45152510826581,0.00213207818356079,
13.742172503788));
#10290=CARTESIAN_POINT('Ctrl Pts',(-2.44551011591929,-0.655923324644509,
13.7764109597646));
#10291=CARTESIAN_POINT('Ctrl Pts',(-2.1718157894574,-1.3183911056973,13.8106494157412));
#10292=CARTESIAN_POINT('Ctrl Pts',(-1.69820083327538,-1.77222389486669,
13.8448878717178));
#10293=CARTESIAN_POINT('Ctrl Pts',(-1.11253090264449,-2.33343129484734,
13.8872269783591));
#10294=CARTESIAN_POINT('Ctrl Pts',(-0.221148857815718,-2.57560086189586,
13.9295660850005));
#10295=CARTESIAN_POINT('Ctrl Pts',(0.567984032494793,-2.38789818512109,
13.9719051916418));
#10296=CARTESIAN_POINT('Ctrl Pts',(1.35711692280528,-2.20019550834633,14.0142442982831));
#10297=CARTESIAN_POINT('Ctrl Pts',(2.04400065859751,-1.58262058774832,14.0565834049245));
#10298=CARTESIAN_POINT('Ctrl Pts',(2.31426727392473,-0.817820633461076,
14.0989225115658));
#10299=CARTESIAN_POINT('Ctrl Pts',(2.58453388925195,-0.0530206791738243,
14.1412616182071));
#10300=CARTESIAN_POINT('Ctrl Pts',(2.43818338411416,0.859004308802644,14.1836007248485));
#10301=CARTESIAN_POINT('Ctrl Pts',(1.94219639616232,1.50084534926412,14.2259398314898));
#10302=CARTESIAN_POINT('Ctrl Pts',(1.44620940821049,2.1426863897256,14.2682789381312));
#10303=CARTESIAN_POINT('Ctrl Pts',(0.600585937444576,2.51434348267211,14.3106180447725));
#10304=CARTESIAN_POINT('Ctrl Pts',(-0.207655199690527,2.44571930558581,
14.3529571514138));
#10305=CARTESIAN_POINT('Ctrl Pts',(-1.01589633682564,2.37709512849952,14.3952962580552));
#10306=CARTESIAN_POINT('Ctrl Pts',(-1.78675514032997,1.86818968138044,14.4376353646965));
#10307=CARTESIAN_POINT('Ctrl Pts',(-2.16743054437203,1.15191511796523,14.4799744713379));
#10308=CARTESIAN_POINT('Ctrl Pts',(-2.3538402493456,0.801168711371672,14.5007071488212));
#10309=CARTESIAN_POINT('Ctrl Pts',(-2.44668866635445,0.400697683916469,
14.5214398263046));
#10310=CARTESIAN_POINT('Ctrl Pts',(-2.44648675330186,0.00013847494270713,
14.542172503788));
#10311=CARTESIAN_POINT('Origin',(0.,0.,0.));
#10312=CARTESIAN_POINT('',(-2.45170362471915,-0.00209312714770177,15.4578274962121));
#10313=CARTESIAN_POINT('',(-2.45101678589125,-0.00220376091521671,15.342172503788));
#10314=CARTESIAN_POINT('',(-2.4505,-3.00099698131059E-16,0.));
#10315=CARTESIAN_POINT('Ctrl Pts',(-2.45170362471915,-0.00209312714770177,
15.4578274962121));
#10316=CARTESIAN_POINT('Ctrl Pts',(-2.44569114235928,0.661629417064826,
15.423287699823));
#10317=CARTESIAN_POINT('Ctrl Pts',(-2.1665957765506,1.32980534203153,15.3887479034339));
#10318=CARTESIAN_POINT('Ctrl Pts',(-1.6855704568615,1.78423176908934,15.3542081070448));
#10319=CARTESIAN_POINT('Ctrl Pts',(-1.09614520521568,2.34106401920079,15.3118847046269));
#10320=CARTESIAN_POINT('Ctrl Pts',(-0.203524735473776,2.57695415849103,
15.2695613022089));
#10321=CARTESIAN_POINT('Ctrl Pts',(0.584040355411103,2.3840150238879,15.2272378997909));
#10322=CARTESIAN_POINT('Ctrl Pts',(1.37160544629598,2.19107588928478,15.184914497373));
#10323=CARTESIAN_POINT('Ctrl Pts',(2.05411515832385,1.56930748078828,15.142591094955));
#10324=CARTESIAN_POINT('Ctrl Pts',(2.31941555059053,0.803082981111423,15.100267692537));
#10325=CARTESIAN_POINT('Ctrl Pts',(2.5847159428572,0.0368584814345732,15.0579442901191));
#10326=CARTESIAN_POINT('Ctrl Pts',(2.43280701536272,-0.873822109422619,
15.0156208877011));
#10327=CARTESIAN_POINT('Ctrl Pts',(1.93316612431206,-1.51244818314025,14.9732974852832));
#10328=CARTESIAN_POINT('Ctrl Pts',(1.43352523326142,-2.15107425685787,14.9309740828652));
#10329=CARTESIAN_POINT('Ctrl Pts',(0.586152378654594,-2.51764581343592,
14.8886506804472));
#10330=CARTESIAN_POINT('Ctrl Pts',(-0.221396377932638,-2.44450698806738,
14.8463272780293));
#10331=CARTESIAN_POINT('Ctrl Pts',(-1.02894513451987,-2.37136816269885,
14.8040038756113));
#10332=CARTESIAN_POINT('Ctrl Pts',(-1.79666979308753,-1.85851895538374,
14.7616804731933));
#10333=CARTESIAN_POINT('Ctrl Pts',(-2.1734423425936,-1.14051705567834,14.7193570707754));
#10334=CARTESIAN_POINT('Ctrl Pts',(-2.35602576259141,-0.792574397475153,
14.6988472125876));
#10335=CARTESIAN_POINT('Ctrl Pts',(-2.44679966025702,-0.39645455782964,
14.6783373543998));
#10336=CARTESIAN_POINT('Ctrl Pts',(-2.44650205703081,-0.000206129442867353,
14.6578274962121));
#10337=CARTESIAN_POINT('Ctrl Pts',(-2.44648675330186,0.00013847494270713,
14.542172503788));
#10338=CARTESIAN_POINT('Ctrl Pts',(-2.44627633088679,-0.417301779901513,
14.5637789329459));
#10339=CARTESIAN_POINT('Ctrl Pts',(-2.34500734273702,-0.834837805473078,
14.5853853621039));
#10340=CARTESIAN_POINT('Ctrl Pts',(-2.14325810848994,-1.19628938140642,
14.6069917912619));
#10341=CARTESIAN_POINT('Ctrl Pts',(-1.74791826398601,-1.90457563765161,
14.6493308979032));
#10342=CARTESIAN_POINT('Ctrl Pts',(-0.96674657039832,-2.39750447043065,
14.6916700045446));
#10343=CARTESIAN_POINT('Ctrl Pts',(-0.157264022288075,-2.44947578697309,
14.7340091111859));
#10344=CARTESIAN_POINT('Ctrl Pts',(0.65221852582217,-2.50144710351553,14.7763482178272));
#10345=CARTESIAN_POINT('Ctrl Pts',(1.49001192845498,-2.11246090382136,14.8186873244686));
#10346=CARTESIAN_POINT('Ctrl Pts',(1.97268097795396,-1.4605455702895,14.8610264311099));
#10347=CARTESIAN_POINT('Ctrl Pts',(2.45535002745294,-0.808630236757634,
14.9033655377512));
#10348=CARTESIAN_POINT('Ctrl Pts',(2.5828947238181,0.106214230611921,14.9457046443926));
#10349=CARTESIAN_POINT('Ctrl Pts',(2.29694133555125,0.865288451737177,14.9880437510339));
#10350=CARTESIAN_POINT('Ctrl Pts',(2.01098794728439,1.62436267286245,15.0303828576753));
#10351=CARTESIAN_POINT('Ctrl Pts',(1.3115364743855,2.22766664774341,15.0727219643166));
#10352=CARTESIAN_POINT('Ctrl Pts',(0.518706793561342,2.39908458916875,15.1150610709579));
#10353=CARTESIAN_POINT('Ctrl Pts',(-0.27412288726279,2.57050253059408,15.1574001775993));
#10354=CARTESIAN_POINT('Ctrl Pts',(-1.16033077601218,2.31003443856381,15.1997392842406));
#10355=CARTESIAN_POINT('Ctrl Pts',(-1.73432367419482,1.73688946015601,15.242078390882));
#10356=CARTESIAN_POINT('Ctrl Pts',(-2.18665025447788,1.28523107046088,15.275443095184));
#10357=CARTESIAN_POINT('Ctrl Pts',(-2.44509151311632,0.639400522100025,
15.308807799486));
#10358=CARTESIAN_POINT('Ctrl Pts',(-2.45101678589125,-0.00220376091521671,
15.342172503788));
#10359=CARTESIAN_POINT('Origin',(0.,0.,0.));
#10360=CARTESIAN_POINT('',(-2.45320425869571,0.00157062206639257,16.2578274962121));
#10361=CARTESIAN_POINT('',(-2.45375743039664,0.00122626908859285,16.142172503788));
#10362=CARTESIAN_POINT('',(-2.4505,-3.00099698131059E-16,0.));
#10363=CARTESIAN_POINT('Ctrl Pts',(-2.45320425869571,0.00157062206639257,
16.2578274962121));
#10364=CARTESIAN_POINT('Ctrl Pts',(-2.45391173395103,0.0963983097870705,
16.2528848500821));
#10365=CARTESIAN_POINT('Ctrl Pts',(-2.44888938633013,0.191150369454898,
16.247942203952));
#10366=CARTESIAN_POINT('Ctrl Pts',(-2.4378864106789,0.285202769094392,16.242999557822));
#10367=CARTESIAN_POINT('Ctrl Pts',(-2.34366899069128,1.09056440203499,16.2006761554041));
#10368=CARTESIAN_POINT('Ctrl Pts',(-1.81093207781014,1.84462463999376,16.1583527529861));
#10369=CARTESIAN_POINT('Ctrl Pts',(-1.08332924046142,2.20250505734567,16.1160293505681));
#10370=CARTESIAN_POINT('Ctrl Pts',(-0.355726403112691,2.56038547469759,
16.0737059481502));
#10371=CARTESIAN_POINT('Ctrl Pts',(0.566742358703627,2.52208607144263,16.0313825457322));
#10372=CARTESIAN_POINT('Ctrl Pts',(1.26217497636144,2.1051235355482,15.9890591433142));
#10373=CARTESIAN_POINT('Ctrl Pts',(1.95760759401923,1.68816099965378,15.9467357408963));
#10374=CARTESIAN_POINT('Ctrl Pts',(2.42600406751854,0.892535331119909,15.9044123384783));
#10375=CARTESIAN_POINT('Ctrl Pts',(2.45313769424733,0.0821354000103284,
15.8620889360604));
#10376=CARTESIAN_POINT('Ctrl Pts',(2.48027132097612,-0.728264531099286,
15.8197655336424));
#10377=CARTESIAN_POINT('Ctrl Pts',(2.06614210093437,-1.55343872478459,15.7774421312244));
#10378=CARTESIAN_POINT('Ctrl Pts',(1.40015696240666,-2.01598394127932,15.7351187288065));
#10379=CARTESIAN_POINT('Ctrl Pts',(0.734171823878979,-2.47852915777403,
15.6927953263885));
#10380=CARTESIAN_POINT('Ctrl Pts',(-0.183669233134644,-2.57844539707816,
15.6504719239706));
#10381=CARTESIAN_POINT('Ctrl Pts',(-0.933580675884534,-2.27003477781442,
15.6081485215526));
#10382=CARTESIAN_POINT('Ctrl Pts',(-1.68349211863445,-1.96162415855066,
15.5658251191346));
#10383=CARTESIAN_POINT('Ctrl Pts',(-2.26547394712063,-1.24488668071899,
15.5235017167167));
#10384=CARTESIAN_POINT('Ctrl Pts',(-2.41334984458884,-0.447630761336837,
15.4811783142987));
#10385=CARTESIAN_POINT('Ctrl Pts',(-2.44054538325779,-0.301009137692811,
15.4733947082698));
#10386=CARTESIAN_POINT('Ctrl Pts',(-2.4530585485704,-0.151664211425061,
15.4656111022409));
#10387=CARTESIAN_POINT('Ctrl Pts',(-2.45170362471915,-0.00209312714770177,
15.4578274962121));
#10388=CARTESIAN_POINT('Ctrl Pts',(-2.45101678589125,-0.00220376091521671,
15.342172503788));
#10389=CARTESIAN_POINT('Ctrl Pts',(-2.45261055940026,-0.174781792067435,
15.3511469061273));
#10390=CARTESIAN_POINT('Ctrl Pts',(-2.43593488648265,-0.347054054347032,
15.3601213084666));
#10391=CARTESIAN_POINT('Ctrl Pts',(-2.39984878306786,-0.515159608355884,
15.369095710806));
#10392=CARTESIAN_POINT('Ctrl Pts',(-2.22960308614234,-1.30824183367466,
15.4114348174473));
#10393=CARTESIAN_POINT('Ctrl Pts',(-1.6273337846754,-2.00858441952683,15.4537739240886));
#10394=CARTESIAN_POINT('Ctrl Pts',(-0.868683124055122,-2.29565965109279,
15.49611303073));
#10395=CARTESIAN_POINT('Ctrl Pts',(-0.110032463434849,-2.58273488265876,
15.5384521373713));
#10396=CARTESIAN_POINT('Ctrl Pts',(0.804999556338751,-2.45654275993851,
15.5807912440127));
#10397=CARTESIAN_POINT('Ctrl Pts',(1.45762771755979,-1.97483797833521,15.623130350654));
#10398=CARTESIAN_POINT('Ctrl Pts',(2.1102558787808,-1.49313319673193,15.6654694572953));
#10399=CARTESIAN_POINT('Ctrl Pts',(2.50048018144927,-0.65591575624562,15.7078085639367));
#10400=CARTESIAN_POINT('Ctrl Pts',(2.44970559717748,0.153642737644857,15.750147670578));
#10401=CARTESIAN_POINT('Ctrl Pts',(2.39893101290568,0.963201231535358,15.7924867772194));
#10402=CARTESIAN_POINT('Ctrl Pts',(1.90715754169359,1.74510077883003,15.8348258838607));
#10403=CARTESIAN_POINT('Ctrl Pts',(1.19945649881003,2.14148726616248,15.877164990502));
#10404=CARTESIAN_POINT('Ctrl Pts',(0.4917554559265,2.53787375349492,15.9195040971434));
#10405=CARTESIAN_POINT('Ctrl Pts',(-0.431873158628486,2.54874718086516,
15.9618432037847));
#10406=CARTESIAN_POINT('Ctrl Pts',(-1.14870970000415,2.16913107690385,16.004182310426));
#10407=CARTESIAN_POINT('Ctrl Pts',(-1.86554624137983,1.78951497294252,16.0465214170674));
#10408=CARTESIAN_POINT('Ctrl Pts',(-2.37559070957618,1.01940933764961,16.0888605237087));
#10409=CARTESIAN_POINT('Ctrl Pts',(-2.44540965195168,0.211270532292635,
16.1311996303501));
#10410=CARTESIAN_POINT('Ctrl Pts',(-2.45144122637565,0.1414563932701,16.1348572548294));
#10411=CARTESIAN_POINT('Ctrl Pts',(-2.45418738704329,0.0713584117786554,
16.1385148793087));
#10412=CARTESIAN_POINT('Ctrl Pts',(-2.45375743039664,0.00122626908859285,
16.142172503788));
#10413=CARTESIAN_POINT('Origin',(0.,0.,0.));
#10414=CARTESIAN_POINT('',(-2.44693273525174,0.00106278712846283,17.0578274962121));
#10415=CARTESIAN_POINT('',(-2.44733932140245,0.00143065932062346,16.942172503788));
#10416=CARTESIAN_POINT('',(-2.4505,-3.00099698131059E-16,0.));
#10417=CARTESIAN_POINT('Ctrl Pts',(-2.44693273525174,0.00106278712846283,
17.0578274962121));
#10418=CARTESIAN_POINT('Ctrl Pts',(-2.44826793617737,0.342274107534463,
17.0401585979232));
#10419=CARTESIAN_POINT('Ctrl Pts',(-2.38175301659422,0.682987849082801,
17.0224896996342));
#10420=CARTESIAN_POINT('Ctrl Pts',(-2.24486236114766,0.992584379473367,
17.0048208013453));
#10421=CARTESIAN_POINT('Ctrl Pts',(-1.91695972664329,1.73418005389911,16.9624973989274));
#10422=CARTESIAN_POINT('Ctrl Pts',(-1.18525817028838,2.29723270973545,16.9201739965094));
#10423=CARTESIAN_POINT('Ctrl Pts',(-0.384410108534635,2.42422351265892,
16.8778505940914));
#10424=CARTESIAN_POINT('Ctrl Pts',(0.416437953219113,2.55121431558239,16.8355271916735));
#10425=CARTESIAN_POINT('Ctrl Pts',(1.28643252037168,2.24214326559299,16.7932037892555));
#10426=CARTESIAN_POINT('Ctrl Pts',(1.82767122184184,1.63836768636443,16.7508803868376));
#10427=CARTESIAN_POINT('Ctrl Pts',(2.36890992331201,1.03459210713585,16.7085569844196));
#10428=CARTESIAN_POINT('Ctrl Pts',(2.58139275909972,0.136111998668031,16.6662335820016));
#10429=CARTESIAN_POINT('Ctrl Pts',(2.36793817501351,-0.646142066565577,
16.6239101795837));
#10430=CARTESIAN_POINT('Ctrl Pts',(2.15448359092731,-1.42839613179916,16.5815867771657));
#10431=CARTESIAN_POINT('Ctrl Pts',(1.51509158696724,-2.09442415379859,16.5392633747478));
#10432=CARTESIAN_POINT('Ctrl Pts',(0.742195707010233,-2.33961028878049,
16.4969399723298));
#10433=CARTESIAN_POINT('Ctrl Pts',(-0.0307001729467758,-2.5847964237624,
16.4546165699118));
#10434=CARTESIAN_POINT('Ctrl Pts',(-0.937099928900703,-2.40914067172678,
16.4122931674939));
#10435=CARTESIAN_POINT('Ctrl Pts',(-1.56245084333064,-1.89298128174774,
16.3699697650759));
#10436=CARTESIAN_POINT('Ctrl Pts',(-2.11477151679402,-1.43710043899317,
16.332589008788));
#10437=CARTESIAN_POINT('Ctrl Pts',(-2.44785369152917,-0.715602040267163,
16.2952082525));
#10438=CARTESIAN_POINT('Ctrl Pts',(-2.45320425869571,0.00157062206639257,
16.2578274962121));
#10439=CARTESIAN_POINT('Ctrl Pts',(-2.45375743039664,0.00122626908859285,
16.142172503788));
#10440=CARTESIAN_POINT('Ctrl Pts',(-2.44921039161454,-0.740461468895879,
16.18085398595));
#10441=CARTESIAN_POINT('Ctrl Pts',(-2.08943753896976,-1.48596989055824,
16.219535468112));
#10442=CARTESIAN_POINT('Ctrl Pts',(-1.50371490001545,-1.93997554189356,
16.2582169502741));
#10443=CARTESIAN_POINT('Ctrl Pts',(-0.862607789149023,-2.4369108353018,
16.3005560569154));
#10444=CARTESIAN_POINT('Ctrl Pts',(0.0491998491384904,-2.58460944669724,
16.3428951635568));
#10445=CARTESIAN_POINT('Ctrl Pts',(0.814398508671991,-2.31547374693528,
16.3852342701981));
#10446=CARTESIAN_POINT('Ctrl Pts',(1.57959716820547,-2.04633804717332,16.4275733768394));
#10447=CARTESIAN_POINT('Ctrl Pts',(2.19818684898495,-1.36036803625397,16.4699124834808));
#10448=CARTESIAN_POINT('Ctrl Pts',(2.387055912797,-0.571513493151793,16.5122515901221));
#10449=CARTESIAN_POINT('Ctrl Pts',(2.57592497660905,0.217341049950412,16.5545906967634));
#10450=CARTESIAN_POINT('Ctrl Pts',(2.33507342345366,1.10908012523546,16.5969298034048));
#10451=CARTESIAN_POINT('Ctrl Pts',(1.77473244518347,1.69557906087766,16.6392689100461));
#10452=CARTESIAN_POINT('Ctrl Pts',(1.21439146691329,2.28207799651985,16.6816080166875));
#10453=CARTESIAN_POINT('Ctrl Pts',(0.334561063528342,2.5633367925192,16.7239471233288));
#10454=CARTESIAN_POINT('Ctrl Pts',(-0.462084367722453,2.41063096320864,
16.7662862299701));
#10455=CARTESIAN_POINT('Ctrl Pts',(-1.25872979897327,2.25792513389807,16.8086253366115));
#10456=CARTESIAN_POINT('Ctrl Pts',(-1.97219025808992,1.67125467927755,16.8509644432528));
#10457=CARTESIAN_POINT('Ctrl Pts',(-2.27593433716645,0.919122677655368,
16.8933035498942));
#10458=CARTESIAN_POINT('Ctrl Pts',(-2.39279757601285,0.629745574349115,
16.9095932011921));
#10459=CARTESIAN_POINT('Ctrl Pts',(-2.449011831938,0.315875736490138,16.92588285249));
#10460=CARTESIAN_POINT('Ctrl Pts',(-2.44733932140245,0.00143065932062346,
16.942172503788));
#10461=CARTESIAN_POINT('Origin',(0.,0.,0.));
#10462=CARTESIAN_POINT('',(-2.44932439460027,-0.00216647677020371,17.8578274962121));
#10463=CARTESIAN_POINT('',(-2.44855018848127,-0.00200161468709733,17.742172503788));
#10464=CARTESIAN_POINT('',(-2.4505,-3.00099698131059E-16,0.));
#10465=CARTESIAN_POINT('Ctrl Pts',(-2.44932439460027,-0.00216647677020371,
17.8578274962121));
#10466=CARTESIAN_POINT('Ctrl Pts',(-2.44432735118055,0.583364483646701,
17.8274323457643));
#10467=CARTESIAN_POINT('Ctrl Pts',(-2.23380041902901,1.17212217287416,17.7970371953165));
#10468=CARTESIAN_POINT('Ctrl Pts',(-1.85150344977178,1.61138628092558,17.7666420448687));
#10469=CARTESIAN_POINT('Ctrl Pts',(-1.31917812041283,2.22303489390921,17.7243186424507));
#10470=CARTESIAN_POINT('Ctrl Pts',(-0.453810057673014,2.54483230969522,
17.6819952400327));
#10471=CARTESIAN_POINT('Ctrl Pts',(0.348814354230171,2.42960064972722,17.6396718376148));
#10472=CARTESIAN_POINT('Ctrl Pts',(1.15143876613336,2.31436898975923,17.5973484351968));
#10473=CARTESIAN_POINT('Ctrl Pts',(1.89131952719991,1.76210825403724,17.5550250327788));
#10474=CARTESIAN_POINT('Ctrl Pts',(2.23006336434382,1.02540146376113,17.5127016303609));
#10475=CARTESIAN_POINT('Ctrl Pts',(2.56880720148773,0.288694673485041,17.4703782279429));
#10476=CARTESIAN_POINT('Ctrl Pts',(2.50641411470901,-0.632458171345165,
17.428054825525));
#10477=CARTESIAN_POINT('Ctrl Pts',(2.07142032492868,-1.31675685240075,17.385731423107));
#10478=CARTESIAN_POINT('Ctrl Pts',(1.63642653514833,-2.00105553345636,17.343408020689));
#10479=CARTESIAN_POINT('Ctrl Pts',(0.828832042366333,-2.44850005073733,
17.3010846182711));
#10480=CARTESIAN_POINT('Ctrl Pts',(0.0179998008846638,-2.45444632820522,
17.2587612158531));
#10481=CARTESIAN_POINT('Ctrl Pts',(-0.792832440596982,-2.4603926056731,
17.2164378134351));
#10482=CARTESIAN_POINT('Ctrl Pts',(-1.6069024307783,-2.02484064332792,17.1741144110172));
#10483=CARTESIAN_POINT('Ctrl Pts',(-2.05188556954207,-1.34699531564776,
17.1317910085992));
#10484=CARTESIAN_POINT('Ctrl Pts',(-2.31110004676363,-0.95213243895576,
17.1071365044702));
#10485=CARTESIAN_POINT('Ctrl Pts',(-2.44506964700506,-0.475050424361855,
17.0824820003411));
#10486=CARTESIAN_POINT('Ctrl Pts',(-2.44693273525174,0.00106278712846283,
17.0578274962121));
#10487=CARTESIAN_POINT('Ctrl Pts',(-2.44733932140245,0.00143065932062346,
16.942172503788));
#10488=CARTESIAN_POINT('Ctrl Pts',(-2.44466474060817,-0.501411473139033,
16.9682219591314));
#10489=CARTESIAN_POINT('Ctrl Pts',(-2.29395904503527,-1.00572463812667,
16.9942714144748));
#10490=CARTESIAN_POINT('Ctrl Pts',(-2.00651806831996,-1.41370040856583,
17.0203208698182));
#10491=CARTESIAN_POINT('Ctrl Pts',(-1.53933002136053,-2.07679794454109,
17.0626599764595));
#10492=CARTESIAN_POINT('Ctrl Pts',(-0.710926228405238,-2.48539946786777,
17.1049990831009));
#10493=CARTESIAN_POINT('Ctrl Pts',(0.0995554713400155,-2.45249919710485,
17.1473381897422));
#10494=CARTESIAN_POINT('Ctrl Pts',(0.910037171085223,-2.41959892634193,
17.1896772963835));
#10495=CARTESIAN_POINT('Ctrl Pts',(1.7025967776204,-1.94519686148946,17.2320164030249));
#10496=CARTESIAN_POINT('Ctrl Pts',(2.11450135898779,-1.24641389855554,17.2743555096662));
#10497=CARTESIAN_POINT('Ctrl Pts',(2.52640594035523,-0.547630935621566,
17.3166946163075));
#10498=CARTESIAN_POINT('Ctrl Pts',(2.55765549655481,0.375532925393901,17.3590337229489));
#10499=CARTESIAN_POINT('Ctrl Pts',(2.19394795737102,1.10057074466896,17.4013728295902));
#10500=CARTESIAN_POINT('Ctrl Pts',(1.83024041818725,1.82560856394398,17.4437119362316));
#10501=CARTESIAN_POINT('Ctrl Pts',(1.07157578362015,2.35252034147863,17.4860510428729));
#10502=CARTESIAN_POINT('Ctrl Pts',(0.265174180711339,2.44015291683897,17.5283901495142));
#10503=CARTESIAN_POINT('Ctrl Pts',(-0.541227422197499,2.52778549219932,
17.5707292561556));
#10504=CARTESIAN_POINT('Ctrl Pts',(-1.39536599344806,2.17613886538534,17.6130683627969));
#10505=CARTESIAN_POINT('Ctrl Pts',(-1.90632558716922,1.54615211391946,17.6554074694383));
#10506=CARTESIAN_POINT('Ctrl Pts',(-2.25536008677173,1.11581062849447,17.6843291475548));
#10507=CARTESIAN_POINT('Ctrl Pts',(-2.44426032078067,0.555590000217446,
17.7132508256714));
#10508=CARTESIAN_POINT('Ctrl Pts',(-2.44855018848127,-0.00200161468709733,
17.742172503788));
#10509=CARTESIAN_POINT('Origin',(0.,0.,0.));
#10510=CARTESIAN_POINT('',(-2.45447131381915,0.000284333535872242,18.6578274962121));
#10511=CARTESIAN_POINT('',(-2.45447923121619,-0.000280315077781223,18.542172503788));
#10512=CARTESIAN_POINT('',(-2.4505,-3.00099698131059E-16,0.));
#10513=CARTESIAN_POINT('Ctrl Pts',(-2.45447131381915,0.000284333535872242,
18.6578274962121));
#10514=CARTESIAN_POINT('Ctrl Pts',(-2.45449642498564,0.0155735304685792,
18.6570294960233));
#10515=CARTESIAN_POINT('Ctrl Pts',(-2.45436591171342,0.0308622871987328,
18.6562314958346));
#10516=CARTESIAN_POINT('Ctrl Pts',(-2.45407846744843,0.0461480928960939,
18.6554334956459));
#10517=CARTESIAN_POINT('Ctrl Pts',(-2.43883333408655,0.856858810692927,
18.6131100932279));
#10518=CARTESIAN_POINT('Ctrl Pts',(-1.98215613057064,1.65926855178873,18.5707866908099));
#10519=CARTESIAN_POINT('Ctrl Pts',(-1.29291361188798,2.08638566978081,18.528463288392));
#10520=CARTESIAN_POINT('Ctrl Pts',(-0.603671093205304,2.51350278777291,
18.486139885974));
#10521=CARTESIAN_POINT('Ctrl Pts',(0.318136740644127,2.56532728266126,18.443816483556));
#10522=CARTESIAN_POINT('Ctrl Pts',(1.0509101043071,2.2181566048269,18.4014930811381));
#10523=CARTESIAN_POINT('Ctrl Pts',(1.78368346797003,1.87098592699256,18.3591696787201));
#10524=CARTESIAN_POINT('Ctrl Pts',(2.32742236144652,1.12482007643556,18.3168462763022));
#10525=CARTESIAN_POINT('Ctrl Pts',(2.43344132952563,0.320926886733544,18.2745228738842));
#10526=CARTESIAN_POINT('Ctrl Pts',(2.53946029760475,-0.482966302968517,
18.2321994714662));
#10527=CARTESIAN_POINT('Ctrl Pts',(2.20775934028643,-1.3445868318156,18.1898760690483));
#10528=CARTESIAN_POINT('Ctrl Pts',(1.59004583873153,-1.86986229482401,18.1475526666303));
#10529=CARTESIAN_POINT('Ctrl Pts',(0.972332337176633,-2.39513775783242,
18.1052292642124));
#10530=CARTESIAN_POINT('Ctrl Pts',(0.0686062913851572,-2.58406815500216,
18.0629058617944));
#10531=CARTESIAN_POINT('Ctrl Pts',(-0.707802434290682,-2.35024392029511,
18.0205824593764));
#10532=CARTESIAN_POINT('Ctrl Pts',(-1.4842111599665,-2.11641968558808,17.9782590569585));
#10533=CARTESIAN_POINT('Ctrl Pts',(-2.13330256552669,-1.45984081900429,
17.9359356545405));
#10534=CARTESIAN_POINT('Ctrl Pts',(-2.35820697031774,-0.680801480621775,
17.8936122521225));
#10535=CARTESIAN_POINT('Ctrl Pts',(-2.42159309374546,-0.46124026880983,
17.8816840001524));
#10536=CARTESIAN_POINT('Ctrl Pts',(-2.45128543088856,-0.231951844806988,
17.8697557481822));
#10537=CARTESIAN_POINT('Ctrl Pts',(-2.44932439460027,-0.00216647677020371,
17.8578274962121));
#10538=CARTESIAN_POINT('Ctrl Pts',(-2.44855018848127,-0.00200161468709733,
17.742172503788));
#10539=CARTESIAN_POINT('Ctrl Pts',(-2.45054035630699,-0.260681128677846,
17.7555899323127));
#10540=CARTESIAN_POINT('Ctrl Pts',(-2.41279785980027,-0.518794814714601,
17.7690073608375));
#10541=CARTESIAN_POINT('Ctrl Pts',(-2.33287882030774,-0.763112058241259,
17.7824247893623));
#10542=CARTESIAN_POINT('Ctrl Pts',(-2.08069184353337,-1.53406260281827,
17.8247638960036));
#10543=CARTESIAN_POINT('Ctrl Pts',(-1.40853727379288,-2.16763681585453,
17.867103002645));
#10544=CARTESIAN_POINT('Ctrl Pts',(-0.624041939151175,-2.37386504710232,
17.9094421092863));
#10545=CARTESIAN_POINT('Ctrl Pts',(0.160453395490553,-2.58009327835011,
17.9517812159276));
#10546=CARTESIAN_POINT('Ctrl Pts',(1.0572894950335,-2.35897552780941,17.994120322569));
#10547=CARTESIAN_POINT('Ctrl Pts',(1.65600891856045,-1.81171136368957,18.0364594292103));
#10548=CARTESIAN_POINT('Ctrl Pts',(2.25472834208738,-1.26444719956974,18.0787985358516));
#10549=CARTESIAN_POINT('Ctrl Pts',(2.55533108959832,-0.39103662187079,18.121137642493));
#10550=CARTESIAN_POINT('Ctrl Pts',(2.420239476008,0.408784151412672,18.1634767491343));
#10551=CARTESIAN_POINT('Ctrl Pts',(2.28514786241768,1.20860492469616,18.2058158557757));
#10552=CARTESIAN_POINT('Ctrl Pts',(1.71436188772607,1.93483589356415,18.248154962417));
#10553=CARTESIAN_POINT('Ctrl Pts',(0.969114736684281,2.25510093583747,18.2904940690583));
#10554=CARTESIAN_POINT('Ctrl Pts',(0.223867585642514,2.57536597811077,18.3328331756997));
#10555=CARTESIAN_POINT('Ctrl Pts',(-0.695840741749422,2.48966509378942,
18.375172282341));
#10556=CARTESIAN_POINT('Ctrl Pts',(-1.36908480923408,2.03722124198579,18.4175113889823));
#10557=CARTESIAN_POINT('Ctrl Pts',(-2.02984001993379,1.59317034415132,18.4590650939176));
#10558=CARTESIAN_POINT('Ctrl Pts',(-2.45319011466729,0.795856637511719,
18.5006187988528));
#10559=CARTESIAN_POINT('Ctrl Pts',(-2.45447923121619,-0.000280315077781223,
18.542172503788));
#10560=CARTESIAN_POINT('Origin',(0.,0.,0.));
#10561=CARTESIAN_POINT('',(-2.44849865710204,0.00198121704041709,19.4578274962121));
#10562=CARTESIAN_POINT('',(-2.44936952853288,0.00217752272054485,19.342172503788));
#10563=CARTESIAN_POINT('',(-2.4505,-3.00099698131059E-16,0.));
#10564=CARTESIAN_POINT('Ctrl Pts',(-2.44849865710204,0.00198121704041709,
19.4578274962121));
#10565=CARTESIAN_POINT('Ctrl Pts',(-2.45048258357382,0.262734228461402,
19.4443032438644));
#10566=CARTESIAN_POINT('Ctrl Pts',(-2.412119819907,0.522918749126386,19.4307789915168));
#10567=CARTESIAN_POINT('Ctrl Pts',(-2.33094434568626,0.768979341845459,
19.4172547391692));
#10568=CARTESIAN_POINT('Ctrl Pts',(-2.07691017258718,1.53901240668088,19.3749313367512));
#10569=CARTESIAN_POINT('Ctrl Pts',(-1.40359291560209,2.17072383784431,19.3326079343333));
#10570=CARTESIAN_POINT('Ctrl Pts',(-0.618942236900824,2.37519289285147,
19.2902845319153));
#10571=CARTESIAN_POINT('Ctrl Pts',(0.165708441800439,2.57966194785863,19.2479611294973));
#10572=CARTESIAN_POINT('Ctrl Pts',(1.06169254221783,2.35688862670957,19.2056377270794));
#10573=CARTESIAN_POINT('Ctrl Pts',(1.6592210708706,1.80876095956626,19.1633143246614));
#10574=CARTESIAN_POINT('Ctrl Pts',(2.25674959952335,1.26063329242296,19.1209909222434));
#10575=CARTESIAN_POINT('Ctrl Pts',(2.55582255641143,0.387151279285426,19.0786675198255));
#10576=CARTESIAN_POINT('Ctrl Pts',(2.41965536475122,-0.41218768383175,19.0363441174075));
#10577=CARTESIAN_POINT('Ctrl Pts',(2.283488173091,-1.21152664694893,18.9940207149896));
#10578=CARTESIAN_POINT('Ctrl Pts',(1.71208083288248,-1.93672256004577,18.9516973125716));
#10579=CARTESIAN_POINT('Ctrl Pts',(0.966773292794929,-2.25609844005318,
18.9093739101536));
#10580=CARTESIAN_POINT('Ctrl Pts',(0.221465752707379,-2.57547432006059,
18.8670505077357));
#10581=CARTESIAN_POINT('Ctrl Pts',(-0.697741987259225,-2.48903016697857,
18.8247271053177));
#10582=CARTESIAN_POINT('Ctrl Pts',(-1.37043932563863,-2.03630224318865,
18.7824037028997));
#10583=CARTESIAN_POINT('Ctrl Pts',(-2.03045307592447,-1.59211042349219,
18.7408783006705));
#10584=CARTESIAN_POINT('Ctrl Pts',(-2.45316460825219,-0.795317047709615,
18.6993528984413));
#10585=CARTESIAN_POINT('Ctrl Pts',(-2.45447131381915,0.000284333535872242,
18.6578274962121));
#10586=CARTESIAN_POINT('Ctrl Pts',(-2.45447923121619,-0.000280315077781223,
18.542172503788));
#10587=CARTESIAN_POINT('Ctrl Pts',(-2.45450359665697,-0.0153280062970204,
18.5429579054941));
#10588=CARTESIAN_POINT('Ctrl Pts',(-2.45437718361159,-0.030375277128677,
18.5437433072002));
#10589=CARTESIAN_POINT('Ctrl Pts',(-2.45409874524395,-0.0454197343205972,
18.5445287089064));
#10590=CARTESIAN_POINT('Ctrl Pts',(-2.43908880619174,-0.856430039537394,
18.5868678155477));
#10591=CARTESIAN_POINT('Ctrl Pts',(-1.98228912050995,-1.65926383068508,
18.629206922189));
#10592=CARTESIAN_POINT('Ctrl Pts',(-1.29276445498518,-2.08648596151533,
18.6715460288304));
#10593=CARTESIAN_POINT('Ctrl Pts',(-0.603239789460381,-2.51370809234559,
18.7138851354717));
#10594=CARTESIAN_POINT('Ctrl Pts',(0.319009855907422,-2.56531856285839,
18.7562242421131));
#10595=CARTESIAN_POINT('Ctrl Pts',(1.0518959528828,-2.21769666726143,18.7985633487544));
#10596=CARTESIAN_POINT('Ctrl Pts',(1.78478204985816,-1.87007477166448,18.8409024553957));
#10597=CARTESIAN_POINT('Ctrl Pts',(2.32830459844111,-1.12322050995779,18.8832415620371));
#10598=CARTESIAN_POINT('Ctrl Pts',(2.4337081409891,-0.318948723397725,18.9255806686784));
#10599=CARTESIAN_POINT('Ctrl Pts',(2.5391116835371,0.485323063162368,18.9679197753197));
#10600=CARTESIAN_POINT('Ctrl Pts',(2.20639622005011,1.34701237457585,19.0102588819611));
#10601=CARTESIAN_POINT('Ctrl Pts',(1.58783655053459,1.87174749698245,19.0525979886024));
#10602=CARTESIAN_POINT('Ctrl Pts',(0.969276881019064,2.39648261938906,19.0949370952438));
#10603=CARTESIAN_POINT('Ctrl Pts',(0.0648730054750031,2.58426355278879,
19.1372762018851));
#10604=CARTESIAN_POINT('Ctrl Pts',(-0.711454070352378,2.3491480816357,19.1796153085265));
#10605=CARTESIAN_POINT('Ctrl Pts',(-1.48778114617976,2.11403261048261,19.2219544151678));
#10606=CARTESIAN_POINT('Ctrl Pts',(-2.13603142229046,1.45602073477671,19.2642935218091));
#10607=CARTESIAN_POINT('Ctrl Pts',(-2.35951841434036,0.676266556959933,
19.3066326284505));
#10608=CARTESIAN_POINT('Ctrl Pts',(-2.42205082993341,0.458088703025711,
19.318479253563));
#10609=CARTESIAN_POINT('Ctrl Pts',(-2.45132855731013,0.230379652654894,
19.3303258786755));
#10610=CARTESIAN_POINT('Ctrl Pts',(-2.44936952853288,0.00217752272054485,
19.342172503788));
#10611=CARTESIAN_POINT('Origin',(0.,0.,0.));
#10612=CARTESIAN_POINT('',(-2.4474177661784,-0.00147899005716184,20.2578274962121));
#10613=CARTESIAN_POINT('',(-2.44688139258877,-0.00101268112437026,20.142172503788));
#10614=CARTESIAN_POINT('',(-2.4505,-3.00099698131059E-16,0.));
#10615=CARTESIAN_POINT('Ctrl Pts',(-2.4474177661784,-0.00147899005716184,
20.2578274962121));
#10616=CARTESIAN_POINT('Ctrl Pts',(-2.4446244023887,0.505203710649909,20.2315769917055));
#10617=CARTESIAN_POINT('Ctrl Pts',(-2.29139905917431,1.01343507544043,20.205326487199));
#10618=CARTESIAN_POINT('Ctrl Pts',(-1.99979327751963,1.42318572858794,20.1790759826925));
#10619=CARTESIAN_POINT('Ctrl Pts',(-1.52964045278787,2.08382224244525,20.1367525802745));
#10620=CARTESIAN_POINT('Ctrl Pts',(-0.699770977560138,2.48846049433743,
20.0944291778566));
#10621=CARTESIAN_POINT('Ctrl Pts',(0.110264465500261,2.45203436324133,20.0521057754386));
#10622=CARTESIAN_POINT('Ctrl Pts',(0.920299908560683,2.41560823214523,20.0097823730206));
#10623=CARTESIAN_POINT('Ctrl Pts',(1.71050131945374,1.93811771806081,19.9674589706027));
#10624=CARTESIAN_POINT('Ctrl Pts',(2.11946067691125,1.23794879130831,19.9251355681847));
#10625=CARTESIAN_POINT('Ctrl Pts',(2.52842003436875,0.537779864555827,19.8828121657668));
#10626=CARTESIAN_POINT('Ctrl Pts',(2.55613733839068,-0.385067474864773,
19.8404887633488));
#10627=CARTESIAN_POINT('Ctrl Pts',(2.18993575005719,-1.10851801135245,19.7981653609308));
#10628=CARTESIAN_POINT('Ctrl Pts',(1.8237341617237,-1.83196854784013,19.7558419585129));
#10629=CARTESIAN_POINT('Ctrl Pts',(1.06361368103481,-2.35602228139494,19.7135185560949));
#10630=CARTESIAN_POINT('Ctrl Pts',(0.257224457764118,-2.44099699901485,
19.6711951536769));
#10631=CARTESIAN_POINT('Ctrl Pts',(-0.549164765506549,-2.52597171663476,
19.628871751259));
#10632=CARTESIAN_POINT('Ctrl Pts',(-1.40182273135899,-2.17186741831979,
19.586548348841));
#10633=CARTESIAN_POINT('Ctrl Pts',(-1.91077616967869,-1.54063791990863,
19.5442249464231));
#10634=CARTESIAN_POINT('Ctrl Pts',(-2.25709583236163,-1.11111496062379,
19.5154257963527));
#10635=CARTESIAN_POINT('Ctrl Pts',(-2.44427399501199,-0.553277951021609,
19.4866266462824));
#10636=CARTESIAN_POINT('Ctrl Pts',(-2.44849865710204,0.00198121704041709,
19.4578274962121));
#10637=CARTESIAN_POINT('Ctrl Pts',(-2.44936952853288,0.00217752272054485,
19.342172503788));
#10638=CARTESIAN_POINT('Ctrl Pts',(-2.44432710942723,-0.585200668602821,
19.3726649853168));
#10639=CARTESIAN_POINT('Ctrl Pts',(-2.23233624155838,-1.1758455900017,19.4031574668456));
#10640=CARTESIAN_POINT('Ctrl Pts',(-1.84780821169541,-1.61563251281492,
19.4336499483745));
#10641=CARTESIAN_POINT('Ctrl Pts',(-1.31388730901146,-2.2262809248454,19.4759890550158));
#10642=CARTESIAN_POINT('Ctrl Pts',(-0.447321795654437,-2.54608126897873,
19.5183281616572));
#10643=CARTESIAN_POINT('Ctrl Pts',(0.355284909779008,-2.42866964335559,
19.5606672682985));
#10644=CARTESIAN_POINT('Ctrl Pts',(1.15789161521248,-2.31125801773245,19.6030063749398));
#10645=CARTESIAN_POINT('Ctrl Pts',(1.89653951272237,-1.75663442235281,19.6453454815812));
#10646=CARTESIAN_POINT('Ctrl Pts',(2.23316959029373,-1.01863496143666,19.6876845882225));
#10647=CARTESIAN_POINT('Ctrl Pts',(2.56979966786507,-0.280635500520529,
19.7300236948639));
#10648=CARTESIAN_POINT('Ctrl Pts',(2.50441192549792,0.640739825932114,19.7723628015052));
#10649=CARTESIAN_POINT('Ctrl Pts',(2.06693255083469,1.3238026416251,19.8147019081465));
#10650=CARTESIAN_POINT('Ctrl Pts',(1.62945317617146,2.00686545731811,19.8570410147879));
#10651=CARTESIAN_POINT('Ctrl Pts',(0.819882169212132,2.45161576225146,19.8993801214292));
#10652=CARTESIAN_POINT('Ctrl Pts',(0.00873811626980386,2.45450346282045,
19.9417192280705));
#10653=CARTESIAN_POINT('Ctrl Pts',(-0.802405936672501,2.45739116338945,
19.9840583347119));
#10654=CARTESIAN_POINT('Ctrl Pts',(-1.61512303559781,2.01841625959413,20.0263974413532));
#10655=CARTESIAN_POINT('Ctrl Pts',(-2.05745471364159,1.33848560133759,20.0687365479946));
#10656=CARTESIAN_POINT('Ctrl Pts',(-2.31319188062225,0.945378914846541,
20.0932151999257));
#10657=CARTESIAN_POINT('Ctrl Pts',(-2.44512196288412,0.471729021673493,
20.1176938518568));
#10658=CARTESIAN_POINT('Ctrl Pts',(-2.44688139258877,-0.00101268112437026,
20.142172503788));
#10659=CARTESIAN_POINT('Origin',(0.,0.,0.));
#10660=CARTESIAN_POINT('',(-2.45386624914882,-0.00113190329454754,21.0578274962121));
#10661=CARTESIAN_POINT('',(-2.45307396903907,-0.00164186243163431,20.9421725037879));
#10662=CARTESIAN_POINT('',(-2.4505,-3.00099698131059E-16,0.));
#10663=CARTESIAN_POINT('Ctrl Pts',(-2.45386624914882,-0.00113190329454754,
21.0578274962121));
#10664=CARTESIAN_POINT('Ctrl Pts',(-2.4495767373451,0.74612978248249,21.0188507395466));
#10665=CARTESIAN_POINT('Ctrl Pts',(-2.08354403586559,1.49702756493175,20.9798739828812));
#10666=CARTESIAN_POINT('Ctrl Pts',(-1.49017767759624,1.95038490049398,20.9408972262158));
#10667=CARTESIAN_POINT('Ctrl Pts',(-0.845863339748866,2.44266867661335,
20.8985738237978));
#10668=CARTESIAN_POINT('Ctrl Pts',(0.0664995651392659,2.58412322862684,
20.8562504213799));
#10669=CARTESIAN_POINT('Ctrl Pts',(0.829631002671575,2.31005263361174,20.8139270189619));
#10670=CARTESIAN_POINT('Ctrl Pts',(1.59276244020384,2.03598203859666,20.771603616544));
#10671=CARTESIAN_POINT('Ctrl Pts',(2.2066624103803,1.34638629655305,20.729280214126));
#10672=CARTESIAN_POINT('Ctrl Pts',(2.39055645427188,0.556660228447093,20.686956811708));
#10673=CARTESIAN_POINT('Ctrl Pts',(2.57445049816346,-0.233065839658858,
20.6446334092901));
#10674=CARTESIAN_POINT('Ctrl Pts',(2.32833861577016,-1.12292223382715,20.6023100068721));
#10675=CARTESIAN_POINT('Ctrl Pts',(1.76478300611921,-1.7059225399107,20.5599866044542));
#10676=CARTESIAN_POINT('Ctrl Pts',(1.20122739646826,-2.28892284599426,20.5176632020362));
#10677=CARTESIAN_POINT('Ctrl Pts',(0.320228059559642,-2.56506706399307,
20.4753397996182));
#10678=CARTESIAN_POINT('Ctrl Pts',(-0.47527947112366,-2.40805734881286,
20.4330163972002));
#10679=CARTESIAN_POINT('Ctrl Pts',(-1.27078700180694,-2.25104763363266,
20.3906929947823));
#10680=CARTESIAN_POINT('Ctrl Pts',(-1.98080272626491,-1.66088398527347,
20.3483695923644));
#10681=CARTESIAN_POINT('Ctrl Pts',(-2.28059250137602,-0.907484773182661,
20.3060461899464));
#10682=CARTESIAN_POINT('Ctrl Pts',(-2.39444181818354,-0.62137099379153,
20.289973292035));
#10683=CARTESIAN_POINT('Ctrl Pts',(-2.44912811239328,-0.311715287417987,
20.2739003941235));
#10684=CARTESIAN_POINT('Ctrl Pts',(-2.4474177661784,-0.00147899005716184,
20.2578274962121));
#10685=CARTESIAN_POINT('Ctrl Pts',(-2.44688139258877,-0.00101268112437026,
20.142172503788));
#10686=CARTESIAN_POINT('Ctrl Pts',(-2.44816513217721,-0.345941061829376,
20.1600329584982));
#10687=CARTESIAN_POINT('Ctrl Pts',(-2.38015048719084,-0.690385953171378,
20.1778934132084));
#10688=CARTESIAN_POINT('Ctrl Pts',(-2.24036564400662,-1.00270902301118,
20.1957538679186));
#10689=CARTESIAN_POINT('Ctrl Pts',(-1.9089986391656,-1.74308657638562,20.2380929745599));
#10690=CARTESIAN_POINT('Ctrl Pts',(-1.17431837232131,-2.30295527041674,
20.2804320812012));
#10691=CARTESIAN_POINT('Ctrl Pts',(-0.372567979063618,-2.42607846217914,
20.3227711878426));
#10692=CARTESIAN_POINT('Ctrl Pts',(0.429182414194054,-2.54920165394154,
20.3651102944839));
#10693=CARTESIAN_POINT('Ctrl Pts',(1.29800293386513,-2.23557934343526,20.4074494011253));
#10694=CARTESIAN_POINT('Ctrl Pts',(1.83625810641794,-1.62874791489994,20.4497885077666));
#10695=CARTESIAN_POINT('Ctrl Pts',(2.37451327897076,-1.02191648636461,20.492127614408));
#10696=CARTESIAN_POINT('Ctrl Pts',(2.58220310440529,-0.121875939800231,
20.5344667210493));
#10697=CARTESIAN_POINT('Ctrl Pts',(2.3642736098797,0.659449695804327,20.5768058276906));
#10698=CARTESIAN_POINT('Ctrl Pts',(2.14634411535412,1.44077533140884,20.619144934332));
#10699=CARTESIAN_POINT('Ctrl Pts',(1.50279530086847,2.10338605605354,20.6614840409733));
#10700=CARTESIAN_POINT('Ctrl Pts',(0.72816191990582,2.34402299947547,20.7038231476146));
#10701=CARTESIAN_POINT('Ctrl Pts',(-0.0464714610568923,2.58465994289741,
20.746162254256));
#10702=CARTESIAN_POINT('Ctrl Pts',(-0.95218940849662,2.40332310509649,20.7885013608973));
#10703=CARTESIAN_POINT('Ctrl Pts',(-1.57446950176282,1.88300541467923,20.8308404675387));
#10704=CARTESIAN_POINT('Ctrl Pts',(-2.11990464353851,1.42694140698852,20.8679511462884));
#10705=CARTESIAN_POINT('Ctrl Pts',(-2.44758271427281,0.710448255773275,
20.9050618250382));
#10706=CARTESIAN_POINT('Ctrl Pts',(-2.45307396903907,-0.00164186243163431,
20.9421725037879));
#10707=CARTESIAN_POINT('Origin',(0.,0.,0.));
#10708=CARTESIAN_POINT('',(-2.45077715073522,0.00222010580503924,21.857827496212));
#10709=CARTESIAN_POINT('',(-2.45192339561065,0.00204828064707867,21.7421725037879));
#10710=CARTESIAN_POINT('',(-2.4505,-3.00099698131059E-16,0.));
#10711=CARTESIAN_POINT('Ctrl Pts',(-2.45077715073522,0.00222010580503924,
21.857827496212));
#10712=CARTESIAN_POINT('Ctrl Pts',(-2.45244026375057,0.182635521438812,
21.8484478898057));
#10713=CARTESIAN_POINT('Ctrl Pts',(-2.43420592996322,0.362717763180709,
21.8390682833993));
#10714=CARTESIAN_POINT('Ctrl Pts',(-2.39481453108522,0.538046615944328,
21.829688676993));
#10715=CARTESIAN_POINT('Ctrl Pts',(-2.21706954325802,1.32917934257705,21.787365274575));
#10716=CARTESIAN_POINT('Ctrl Pts',(-1.6085526804466,2.02352991753004,21.7450418721571));
#10717=CARTESIAN_POINT('Ctrl Pts',(-0.847576397798938,2.30352882078366,
21.7027184697391));
#10718=CARTESIAN_POINT('Ctrl Pts',(-0.0866001151512351,2.5835277240373,
21.6603950673212));
#10719=CARTESIAN_POINT('Ctrl Pts',(0.826835587332673,2.44917495559155,21.6180716649032));
#10720=CARTESIAN_POINT('Ctrl Pts',(1.47496003114712,1.96191836357903,21.5757482624852));
#10721=CARTESIAN_POINT('Ctrl Pts',(2.12308447496153,1.47466177156653,21.5334248600673));
#10722=CARTESIAN_POINT('Ctrl Pts',(2.50589766010645,0.634501355987238,21.4911014576493));
#10723=CARTESIAN_POINT('Ctrl Pts',(2.44831541284178,-0.174305521802888,
21.4487780552313));
#10724=CARTESIAN_POINT('Ctrl Pts',(2.39073316557711,-0.983112399593038,
21.4064546528134));
#10725=CARTESIAN_POINT('Ctrl Pts',(1.89275548590292,-1.76056573959403,21.3641312503954));
#10726=CARTESIAN_POINT('Ctrl Pts',(1.18213839674829,-2.15108799968291,21.3218078479775));
#10727=CARTESIAN_POINT('Ctrl Pts',(0.471521307593673,-2.54161025977178,
21.2794844455595));
#10728=CARTESIAN_POINT('Ctrl Pts',(-0.451735191041368,-2.54520143994851,
21.2371610431415));
#10729=CARTESIAN_POINT('Ctrl Pts',(-1.16536875158895,-2.16021907269529,
21.1948376407236));
#10730=CARTESIAN_POINT('Ctrl Pts',(-1.87900231213655,-1.77523670544206,
21.1525142383056));
#10731=CARTESIAN_POINT('Ctrl Pts',(-2.38301293459671,-1.00168079075884,
21.1101908358877));
#10732=CARTESIAN_POINT('Ctrl Pts',(-2.44688536042345,-0.193346333304644,
21.0678674334697));
#10733=CARTESIAN_POINT('Ctrl Pts',(-2.45193595584786,-0.1294287623126,21.0645207877171));
#10734=CARTESIAN_POINT('Ctrl Pts',(-2.45423455779445,-0.0652937361585034,
21.0611741419646));
#10735=CARTESIAN_POINT('Ctrl Pts',(-2.45386624914882,-0.00113190329454754,
21.0578274962121));
#10736=CARTESIAN_POINT('Ctrl Pts',(-2.45307396903907,-0.00164186243163431,
20.9421725037879));
#10737=CARTESIAN_POINT('Ctrl Pts',(-2.45384761777164,-0.101966404066716,
20.9474009316795));
#10738=CARTESIAN_POINT('Ctrl Pts',(-2.44822609471337,-0.202203548728654,
20.9526293595711));
#10739=CARTESIAN_POINT('Ctrl Pts',(-2.43591736083732,-0.301612690077846,
20.9578577874627));
#10740=CARTESIAN_POINT('Ctrl Pts',(-2.33624288755297,-1.10661456138417,
21.000196894104));
#10741=CARTESIAN_POINT('Ctrl Pts',(-1.79805170189159,-1.85731976096327,
21.0425360007454));
#10742=CARTESIAN_POINT('Ctrl Pts',(-1.06765924194229,-2.2101509782728,21.0848751073867));
#10743=CARTESIAN_POINT('Ctrl Pts',(-0.337266781992992,-2.56298219558234,
21.127214214028));
#10744=CARTESIAN_POINT('Ctrl Pts',(0.585326952244219,-2.51793943062228,
21.1695533206693));
#10745=CARTESIAN_POINT('Ctrl Pts',(1.27787595235591,-2.09563752929443,21.2118924273107));
#10746=CARTESIAN_POINT('Ctrl Pts',(1.97042495246761,-1.67333562796657,21.254231533952));
#10747=CARTESIAN_POINT('Ctrl Pts',(2.43292921845375,-0.873774590270887,
21.2965706405934));
#10748=CARTESIAN_POINT('Ctrl Pts',(2.45371315274431,-0.0628917124923539,
21.3389097472348));
#10749=CARTESIAN_POINT('Ctrl Pts',(2.47449708703488,0.747991165286156,21.3812488538761));
#10750=CARTESIAN_POINT('Ctrl Pts',(2.05356068962983,1.57019588314754,21.4235879605174));
#10751=CARTESIAN_POINT('Ctrl Pts',(1.38355507737789,2.02742174979691,21.4659270671587));
#10752=CARTESIAN_POINT('Ctrl Pts',(0.713549465125928,2.48464761644628,21.5082661738001));
#10753=CARTESIAN_POINT('Ctrl Pts',(-0.20552536197295,2.57689463188366,21.5506052804414));
#10754=CARTESIAN_POINT('Ctrl Pts',(-0.953033902926841,2.261943850834,21.5929443870828));
#10755=CARTESIAN_POINT('Ctrl Pts',(-1.70054244388073,1.94699306978433,21.6352834937241));
#10756=CARTESIAN_POINT('Ctrl Pts',(-2.27648469868961,1.22484449224763,21.6776226003654));
#10757=CARTESIAN_POINT('Ctrl Pts',(-2.41726759477328,0.426005841826502,
21.7199617070068));
#10758=CARTESIAN_POINT('Ctrl Pts',(-2.44188549961531,0.286317467547558,
21.7273653059338));
#10759=CARTESIAN_POINT('Ctrl Pts',(-2.4531973065269,0.144284100337561,21.7347689048609));
#10760=CARTESIAN_POINT('Ctrl Pts',(-2.45192339561065,0.00204828064707867,
21.7421725037879));
#10761=CARTESIAN_POINT('Origin',(0.,0.,0.));
#10762=CARTESIAN_POINT('',(-2.44651884106482,-0.000297702156279583,22.6578274962121));
#10763=CARTESIAN_POINT('',(-2.44652741818257,0.000358158153537213,22.542172503788));
#10764=CARTESIAN_POINT('',(-2.4505,-3.00099698131059E-16,0.));
#10765=CARTESIAN_POINT('Ctrl Pts',(-2.44651884106482,-0.000297702156279583,
22.6578274962121));
#10766=CARTESIAN_POINT('Ctrl Pts',(-2.44605503950896,0.426777531908182,
22.6357216376468));
#10767=CARTESIAN_POINT('Ctrl Pts',(-2.3397784981325,0.854068794585224,22.6136157790816));
#10768=CARTESIAN_POINT('Ctrl Pts',(-2.12902721506848,1.22142322150288,22.5915099205163));
#10769=CARTESIAN_POINT('Ctrl Pts',(-1.72552733123021,1.9247521238646,22.5491865180984));
#10770=CARTESIAN_POINT('Ctrl Pts',(-0.939063686508212,2.40837590260392,
22.5068631156804));
#10771=CARTESIAN_POINT('Ctrl Pts',(-0.129335964024876,2.45110253453492,
22.4645397132624));
#10772=CARTESIAN_POINT('Ctrl Pts',(0.680391758458507,2.49382916646593,22.4222163108445));
#10773=CARTESIAN_POINT('Ctrl Pts',(1.51338355870323,2.09565865158857,22.3798929084265));
#10774=CARTESIAN_POINT('Ctrl Pts',(1.98866133778568,1.4386995033837,22.3375695060085));
#10775=CARTESIAN_POINT('Ctrl Pts',(2.46393911686811,0.781740355178845,22.2952461035906));
#10776=CARTESIAN_POINT('Ctrl Pts',(2.58150287478829,-0.134007426353506,
22.2529227011726));
#10777=CARTESIAN_POINT('Ctrl Pts',(2.28758310389872,-0.88971594965377,22.2105992987547));
#10778=CARTESIAN_POINT('Ctrl Pts',(1.99366333300913,-1.64542447295406,22.1682758963367));
#10779=CARTESIAN_POINT('Ctrl Pts',(1.28826003330977,-2.24109373802225,22.1259524939187));
#10780=CARTESIAN_POINT('Ctrl Pts',(0.493997970425276,-2.40428718126016,
22.0836290915008));
#10781=CARTESIAN_POINT('Ctrl Pts',(-0.300264092459193,-2.56748062449807,
22.0413056890828));
#10782=CARTESIAN_POINT('Ctrl Pts',(-1.18338491852879,-2.29819824590572,
21.9989822866649));
#10783=CARTESIAN_POINT('Ctrl Pts',(-1.75145877514209,-1.71959961745333,
21.9566588842469));
#10784=CARTESIAN_POINT('Ctrl Pts',(-2.19363752691133,-1.2692285674111,21.9237150882353));
#10785=CARTESIAN_POINT('Ctrl Pts',(-2.44493583356812,-0.631449196775602,
21.8907712922237));
#10786=CARTESIAN_POINT('Ctrl Pts',(-2.45077715073522,0.00222010580503924,
21.857827496212));
#10787=CARTESIAN_POINT('Ctrl Pts',(-2.45192339561065,0.00204828064707867,
21.7421725037879));
#10788=CARTESIAN_POINT('Ctrl Pts',(-2.44591216714184,-0.669122676207722,
21.7771080115022));
#10789=CARTESIAN_POINT('Ctrl Pts',(-2.15966337969236,-1.3448015037868,21.8120435192165));
#10790=CARTESIAN_POINT('Ctrl Pts',(-1.66886628902848,-1.7998746938669,21.8469790269308));
#10791=CARTESIAN_POINT('Ctrl Pts',(-1.07405854984159,-2.35138785583363,
21.8893181335722));
#10792=CARTESIAN_POINT('Ctrl Pts',(-0.178819534109371,-2.57888545646158,
21.9316572402135));
#10793=CARTESIAN_POINT('Ctrl Pts',(0.607124255160193,-2.37824804157426,
21.9739963468548));
#10794=CARTESIAN_POINT('Ctrl Pts',(1.39306804442971,-2.17761062668694,22.0163354534961));
#10795=CARTESIAN_POINT('Ctrl Pts',(2.06971660723662,-1.54883819628441,22.0586745601375));
#10796=CARTESIAN_POINT('Ctrl Pts',(2.32738634465144,-0.779702760243623,
22.1010136667788));
#10797=CARTESIAN_POINT('Ctrl Pts',(2.58505608206628,-0.0105673242027703,
22.1433527734202));
#10798=CARTESIAN_POINT('Ctrl Pts',(2.42374699408901,0.898931117476322,22.1856918800615));
#10799=CARTESIAN_POINT('Ctrl Pts',(1.9172858401876,1.53253992387863,22.2280309867028));
#10800=CARTESIAN_POINT('Ctrl Pts',(1.41082468628624,2.16614873028088,22.2703700933442));
#10801=CARTESIAN_POINT('Ctrl Pts',(0.559211466460781,2.52386790140634,22.3127091999855));
#10802=CARTESIAN_POINT('Ctrl Pts',(-0.247793631510701,2.44197910473602,
22.3550483066269));
#10803=CARTESIAN_POINT('Ctrl Pts',(-1.05479872948225,2.36009030806569,22.3973874132682));
#10804=CARTESIAN_POINT('Ctrl Pts',(-1.81719570559985,1.83859354359949,22.4397265199095));
#10805=CARTESIAN_POINT('Ctrl Pts',(-2.18605629215363,1.11616370017628,22.4820656265509));
#10806=CARTESIAN_POINT('Ctrl Pts',(-2.36060774707999,0.774296922188712,
22.5021012522966));
#10807=CARTESIAN_POINT('Ctrl Pts',(-2.44703253643979,0.387434147083485,
22.5221368780423));
#10808=CARTESIAN_POINT('Ctrl Pts',(-2.44652741818257,0.000358158153537213,
22.542172503788));
#10809=CARTESIAN_POINT('Origin',(0.,0.,0.));
#10810=CARTESIAN_POINT('',(-2.45183158050284,-0.00202607996204418,23.457827496212));
#10811=CARTESIAN_POINT('',(-2.45061074833635,-0.00223305219117096,23.342172503788));
#10812=CARTESIAN_POINT('',(-2.4505,-3.00099698131059E-16,0.));
#10813=CARTESIAN_POINT('Ctrl Pts',(-2.45183158050284,-0.00202607996204418,
23.457827496212));
#10814=CARTESIAN_POINT('Ctrl Pts',(-2.44582498250596,0.667196655845209,
23.4229953854879));
#10815=CARTESIAN_POINT('Ctrl Pts',(-2.16148734348512,1.34087475809766,23.3881632747638));
#10816=CARTESIAN_POINT('Ctrl Pts',(-1.67325809935663,1.79578569322896,23.3533311640396));
#10817=CARTESIAN_POINT('Ctrl Pts',(-1.08002609756608,2.3485336654773,23.3110077616217));
#10818=CARTESIAN_POINT('Ctrl Pts',(-0.185770244427078,2.57829563170229,
23.2686843592037));
#10819=CARTESIAN_POINT('Ctrl Pts',(0.600454879552817,2.37994277235467,23.2263609567858));
#10820=CARTESIAN_POINT('Ctrl Pts',(1.38668000353264,2.18158991300707,23.1840375543678));
#10821=CARTESIAN_POINT('Ctrl Pts',(2.06487439835336,1.55512222808694,23.1417141519498));
#10822=CARTESIAN_POINT('Ctrl Pts',(2.32488719844169,0.787085508260366,23.0993907495319));
#10823=CARTESIAN_POINT('Ctrl Pts',(2.58489999853004,0.0190487884337467,
23.0570673471139));
#10824=CARTESIAN_POINT('Ctrl Pts',(2.42673120388593,-0.890556966299377,
23.0147439446959));
#10825=CARTESIAN_POINT('Ctrl Pts',(1.92270575183184,-1.52572499032332,22.972420542278));
#10826=CARTESIAN_POINT('Ctrl Pts',(1.41868029977777,-2.16089301434725,22.93009713986));
#10827=CARTESIAN_POINT('Ctrl Pts',(0.568798190313761,-2.52162330766206,
22.8877737374421));
#10828=CARTESIAN_POINT('Ctrl Pts',(-0.238228768695827,-2.44292514296122,
22.8454503350241));
#10829=CARTESIAN_POINT('Ctrl Pts',(-1.04525572770542,-2.36422697826037,
22.8031269326061));
#10830=CARTESIAN_POINT('Ctrl Pts',(-1.80942753626056,-1.84610035554386,
22.7608035301882));
#10831=CARTESIAN_POINT('Ctrl Pts',(-2.18124537906091,-1.12552003119352,
22.7184801277702));
#10832=CARTESIAN_POINT('Ctrl Pts',(-2.35885972744917,-0.781304692287325,
22.6982625839175));
#10833=CARTESIAN_POINT('Ctrl Pts',(-2.44694302401464,-0.390891546210193,
22.6780450400648));
#10834=CARTESIAN_POINT('Ctrl Pts',(-2.44651884106482,-0.000297702156279583,
22.6578274962121));
#10835=CARTESIAN_POINT('Ctrl Pts',(-2.44652741818257,0.000358158153537213,
22.542172503788));
#10836=CARTESIAN_POINT('Ctrl Pts',(-2.44596512501825,-0.430531399968592,
22.5644759846836));
#10837=CARTESIAN_POINT('Ctrl Pts',(-2.33767976884795,-0.861685171488669,
22.5867794655792));
#10838=CARTESIAN_POINT('Ctrl Pts',(-2.12332222977882,-1.23132708371886,
22.6090829464749));
#10839=CARTESIAN_POINT('Ctrl Pts',(-1.71640338386024,-1.93302510181068,
22.6514220531162));
#10840=CARTESIAN_POINT('Ctrl Pts',(-0.927241495033076,-2.41305821561412,
22.6937611597576));
#10841=CARTESIAN_POINT('Ctrl Pts',(-0.117014635085855,-2.45172823427093,
22.7361002663989));
#10842=CARTESIAN_POINT('Ctrl Pts',(0.693212224861342,-2.49039825292774,
22.7784393730402));
#10843=CARTESIAN_POINT('Ctrl Pts',(1.5245040559286,-2.08770517643796,22.8207784796816));
#10844=CARTESIAN_POINT('Ctrl Pts',(1.99640159042075,-1.42795087439993,22.8631175863229));
#10845=CARTESIAN_POINT('Ctrl Pts',(2.4682991249129,-0.768196572361893,22.9054566929643));
#10846=CARTESIAN_POINT('Ctrl Pts',(2.58080236282996,0.148618955224388,22.9477957996056));
#10847=CARTESIAN_POINT('Ctrl Pts',(2.28242097573776,0.902894652953447,22.9901349062469));
#10848=CARTESIAN_POINT('Ctrl Pts',(1.98403958864555,1.65717035068253,23.0324740128883));
#10849=CARTESIAN_POINT('Ctrl Pts',(1.27477357654405,2.24890621855437,23.0748131195296));
#10850=CARTESIAN_POINT('Ctrl Pts',(0.479235925177236,2.40728006675578,23.117152226171));
#10851=CARTESIAN_POINT('Ctrl Pts',(-0.316301726189573,2.56565391495718,
23.1594913328123));
#10852=CARTESIAN_POINT('Ctrl Pts',(-1.19811101682169,2.29066574348813,23.2018304394536));
#10853=CARTESIAN_POINT('Ctrl Pts',(-1.76261427027663,1.70817168668717,23.244169546095));
#10854=CARTESIAN_POINT('Ctrl Pts',(-2.1981689528899,1.25873581101898,23.2768371986593));
#10855=CARTESIAN_POINT('Ctrl Pts',(-2.44482413436855,0.626234687516515,
23.3095048512236));
#10856=CARTESIAN_POINT('Ctrl Pts',(-2.45061074833635,-0.00223305219117096,
23.342172503788));
#10857=CARTESIAN_POINT('Origin',(0.,0.,-1.47904511860479));
#10858=CARTESIAN_POINT('',(-1.99583392989514,-0.00164926464131698,23.7209548813952));
#10859=CARTESIAN_POINT('',(-1.99764284170635,0.000851992992676968,23.8790451186048));
#10860=CARTESIAN_POINT('',(-1.99475,4.03981020633857E-13,-1.47904511860479));
#10861=CARTESIAN_POINT('',(-1.97959496748083,0.245420714742238,24.50525));
#10862=CARTESIAN_POINT('Ctrl Pts',(-1.99583392989514,-0.00164926464131691,
23.7209548813952));
#10863=CARTESIAN_POINT('Ctrl Pts',(-1.9968855024659,-0.118809805942343,
23.728446173089));
#10864=CARTESIAN_POINT('Ctrl Pts',(-1.93419140724538,-0.896774432952024,
23.7782608672008));
#10865=CARTESIAN_POINT('Ctrl Pts',(-0.911828861708041,-2.17415297545205,
23.8703989637307));
#10866=CARTESIAN_POINT('Ctrl Pts',(1.33175293478252,-1.94516872322012,23.9973691709844));
#10867=CARTESIAN_POINT('Ctrl Pts',(2.35590509889789,0.0621220732712832,
24.1243393782384));
#10868=CARTESIAN_POINT('Ctrl Pts',(1.22745053520999,2.01448000455152,24.2513095854922));
#10869=CARTESIAN_POINT('Ctrl Pts',(-1.02858118383587,2.12041610541359,24.3782797927461));
#10870=CARTESIAN_POINT('Ctrl Pts',(-1.89801534866759,0.903452385056865,
24.4629265975821));
#10871=CARTESIAN_POINT('Ctrl Pts',(-1.97959496748082,0.245420714742313,
24.50525));
#10872=CARTESIAN_POINT('',(-0.407652562758078,1.95265126189414,24.50525));
#10873=CARTESIAN_POINT('Origin',(0.,0.,24.50525));
#10874=CARTESIAN_POINT('Ctrl Pts',(-1.99764284170635,0.00085199299267695,
23.8790451186048));
#10875=CARTESIAN_POINT('Ctrl Pts',(-1.99436715728184,-0.613649439337014,
23.9184236525045));
#10876=CARTESIAN_POINT('Ctrl Pts',(-1.36122111898238,-1.89471011498649,
24.0001412930456));
#10877=CARTESIAN_POINT('Ctrl Pts',(0.817973374160278,-2.21053272043233,
24.1241980402279));
#10878=CARTESIAN_POINT('Ctrl Pts',(2.30301402245599,-0.512148340557086,
24.2512153601519));
#10879=CARTESIAN_POINT('Ctrl Pts',(1.674912756705,1.65836796725257,24.378232680076));
#10880=CARTESIAN_POINT('Ctrl Pts',(0.24166366648125,2.0882081993032,24.4629108933587));
#10881=CARTESIAN_POINT('Ctrl Pts',(-0.4076525627588,1.95265126189399,24.50525));
#10882=CARTESIAN_POINT('Origin',(0.,0.,-1.47904511860479));
#10883=CARTESIAN_POINT('',(-1.99150926676762,-0.00024233477887608,22.9209548813952));
#10884=CARTESIAN_POINT('',(-1.99484015108914,-0.0018177436674327,23.0790451186047));
#10885=CARTESIAN_POINT('',(-1.99475,4.03981020633857E-13,-1.47904511860479));
#10886=CARTESIAN_POINT('Ctrl Pts',(-1.99150926676762,-0.000242334778875961,
22.9209548813952));
#10887=CARTESIAN_POINT('Ctrl Pts',(-1.99185455913213,-0.318192577760585,
22.9411724252479));
#10888=CARTESIAN_POINT('Ctrl Pts',(-1.77005361978223,-1.30128478605611,
23.0037133715186));
#10889=CARTESIAN_POINT('Ctrl Pts',(-0.228807242491405,-2.34628640912002,
23.1085777202073));
#10890=CARTESIAN_POINT('Ctrl Pts',(1.84664960858395,-1.46536404316653,23.2355479274611));
#10891=CARTESIAN_POINT('Ctrl Pts',(2.23290613147693,0.755941093646845,23.3625181347151));
#10892=CARTESIAN_POINT('Ctrl Pts',(0.576719717599789,2.28580815893301,23.4894883419689));
#10893=CARTESIAN_POINT('Ctrl Pts',(-1.47825392840529,1.75782191898924,23.608967257529));
#10894=CARTESIAN_POINT('Ctrl Pts',(-1.99094445372519,0.543109785451063,
23.686122770671));
#10895=CARTESIAN_POINT('Ctrl Pts',(-1.99583392989514,-0.00164926464131691,
23.7209548813952));
#10896=CARTESIAN_POINT('Ctrl Pts',(-1.99484015108914,-0.00181774366743258,
23.0790451186047));
#10897=CARTESIAN_POINT('Ctrl Pts',(-1.9962346947758,-0.153275180353312,
23.0887165726818));
#10898=CARTESIAN_POINT('Ctrl Pts',(-1.91131516926029,-0.9662262501804,23.1407271334001));
#10899=CARTESIAN_POINT('Ctrl Pts',(-0.798085058971124,-2.21852563316919,
23.2350768007599));
#10900=CARTESIAN_POINT('Ctrl Pts',(1.43108576045911,-1.87368610656973,23.3620941206838));
#10901=CARTESIAN_POINT('Ctrl Pts',(2.35037186943588,0.186189415184726,23.4891114406079));
#10902=CARTESIAN_POINT('Ctrl Pts',(1.11815436836127,2.07570231768813,23.6161287605319));
#10903=CARTESIAN_POINT('Ctrl Pts',(-1.13736772283233,2.06510660675428,23.7431460804559));
#10904=CARTESIAN_POINT('Ctrl Pts',(-1.97555308243499,0.753708357097197,
23.8307848664802));
#10905=CARTESIAN_POINT('Ctrl Pts',(-1.99788911552757,0.0470516863299492,
23.8760845458631));
#10906=CARTESIAN_POINT('Ctrl Pts',(-1.99764284170635,0.00085199299267695,
23.8790451186048));
#10907=CARTESIAN_POINT('Origin',(0.,0.,-1.47904511860479));
#10908=CARTESIAN_POINT('',(-1.99497560556175,0.00180720508266196,22.1209548813952));
#10909=CARTESIAN_POINT('',(-1.99151624869198,0.000291547022211042,22.2790451186048));
#10910=CARTESIAN_POINT('',(-1.99475,4.03981020633857E-13,-1.47904511860479));
#10911=CARTESIAN_POINT('Ctrl Pts',(-1.99497560556175,0.00180720508266202,
22.1209548813952));
#10912=CARTESIAN_POINT('Ctrl Pts',(-1.99022067088762,-0.514010726491639,
22.1538986774068));
#10913=CARTESIAN_POINT('Ctrl Pts',(-1.52285647342705,-1.7001518019312,22.2291658758364));
#10914=CARTESIAN_POINT('Ctrl Pts',(0.474455608801953,-2.30917486244222,
22.3467564766839));
#10915=CARTESIAN_POINT('Ctrl Pts',(2.19708760073256,-0.854519159734979,
22.4737266839378));
#10916=CARTESIAN_POINT('Ctrl Pts',(1.90999071506285,1.3817851298529,22.6006968911917));
#10917=CARTESIAN_POINT('Ctrl Pts',(-0.124219111753841,2.35413848780229,
22.7276670984456));
#10918=CARTESIAN_POINT('Ctrl Pts',(-1.73898870880108,1.36116064380626,22.8344197618468));
#10919=CARTESIAN_POINT('Ctrl Pts',(-1.99113172416258,0.347404399826265,
22.89884902283));
#10920=CARTESIAN_POINT('Ctrl Pts',(-1.99150926676762,-0.000242334778875961,
22.9209548813952));
#10921=CARTESIAN_POINT('Ctrl Pts',(-1.99151624869198,0.000291547022210972,
22.2790451186048));
#10922=CARTESIAN_POINT('Ctrl Pts',(-1.99105853218949,-0.3504601142977,22.3013485995004));
#10923=CARTESIAN_POINT('Ctrl Pts',(-1.73558284268583,-1.36767343802751,
22.3659911870374));
#10924=CARTESIAN_POINT('Ctrl Pts',(-0.112399222395231,-2.35502710849036,
22.4729728812157));
#10925=CARTESIAN_POINT('Ctrl Pts',(1.91765919019992,-1.37162941700542,22.5999902011398));
#10926=CARTESIAN_POINT('Ctrl Pts',(2.19239801962464,0.867282364654784,22.7270075210638));
#10927=CARTESIAN_POINT('Ctrl Pts',(0.460333080665931,2.31233250434551,22.8540248409878));
#10928=CARTESIAN_POINT('Ctrl Pts',(-1.52912384593445,1.69192951214063,22.9713707068348));
#10929=CARTESIAN_POINT('Ctrl Pts',(-1.99012974577896,0.509766024453988,
23.0463774660404));
#10930=CARTESIAN_POINT('Ctrl Pts',(-1.99484015108914,-0.00181774366743258,
23.0790451186047));
#10931=CARTESIAN_POINT('Origin',(0.,0.,-1.47904511860479));
#10932=CARTESIAN_POINT('',(-1.99749018587619,-0.000921389143520827,21.3209548813952));
#10933=CARTESIAN_POINT('',(-1.99590866900402,0.00166733638921758,21.4790451186048));
#10934=CARTESIAN_POINT('',(-1.99475,4.03981020633857E-13,-1.47904511860479));
#10935=CARTESIAN_POINT('Ctrl Pts',(-1.99749018587619,-0.000921389143520883,
21.3209548813952));
#10936=CARTESIAN_POINT('Ctrl Pts',(-1.99778999557661,-0.0531502469707051,
21.3243015271478));
#10937=CARTESIAN_POINT('Ctrl Pts',(-1.97225597155269,-0.765594304990007,
21.3699715753183));
#10938=CARTESIAN_POINT('Ctrl Pts',(-1.1192673629799,-2.07476191756569,21.4579650259067));
#10939=CARTESIAN_POINT('Ctrl Pts',(1.13537360904899,-2.06599206652615,21.5849352331606));
#10940=CARTESIAN_POINT('Ctrl Pts',(2.3514613175128,-0.167410083297791,21.7119054404145));
#10941=CARTESIAN_POINT('Ctrl Pts',(1.41661136721561,1.88430587953843,21.8388756476684));
#10942=CARTESIAN_POINT('Ctrl Pts',(-0.814046703622753,2.21240241272419,
21.9658458549223));
#10943=CARTESIAN_POINT('Ctrl Pts',(-1.91451027631426,0.956714097230605,
22.0598722661646));
#10944=CARTESIAN_POINT('Ctrl Pts',(-1.99632940873961,0.14866851923707,22.1115752749889));
#10945=CARTESIAN_POINT('Ctrl Pts',(-1.99497560556175,0.00180720508266202,
22.1209548813952));
#10946=CARTESIAN_POINT('Ctrl Pts',(-1.99590866900402,0.00166733638921734,
21.4790451186048));
#10947=CARTESIAN_POINT('Ctrl Pts',(-1.99101542354886,-0.54467759982231,
21.5139806263191));
#10948=CARTESIAN_POINT('Ctrl Pts',(-1.47561210593682,-1.76126654148221,
21.5912552406747));
#10949=CARTESIAN_POINT('Ctrl Pts',(0.583178029368184,-2.28444505330724,
21.7108689616716));
#10950=CARTESIAN_POINT('Ctrl Pts',(2.23558944009154,-0.748949678226114,
21.8378862815957));
#10951=CARTESIAN_POINT('Ctrl Pts',(1.84166415556682,1.47209339446037,21.9649036015196));
#10952=CARTESIAN_POINT('Ctrl Pts',(-0.23802015814085,2.34566244151516,22.0919209214437));
#10953=CARTESIAN_POINT('Ctrl Pts',(-1.77291039590186,1.29576282507227,22.196634760472));
#10954=CARTESIAN_POINT('Ctrl Pts',(-1.99192742381681,0.315378194203477,
22.2590094928591));
#10955=CARTESIAN_POINT('Ctrl Pts',(-1.99151624869198,0.000291547022210972,
22.2790451186048));
#10956=CARTESIAN_POINT('Origin',(0.,0.,-1.47904511860479));
#10957=CARTESIAN_POINT('',(-1.99224100758391,-0.00120392385877232,20.5209548813952));
#10958=CARTESIAN_POINT('',(-1.99684525596436,-0.00133650482941783,20.6790451186048));
#10959=CARTESIAN_POINT('',(-1.99475,4.03981020633857E-13,-1.47904511860479));
#10960=CARTESIAN_POINT('Ctrl Pts',(-1.99224100758391,-0.00120392385877197,
20.5209548813952));
#10961=CARTESIAN_POINT('Ctrl Pts',(-1.99363325941504,-0.253741713763136,
20.5370277793067));
#10962=CARTESIAN_POINT('Ctrl Pts',(-1.83189848440572,-1.16954880445064,
20.5954240796361));
#10963=CARTESIAN_POINT('Ctrl Pts',(-0.456477659862079,-2.31279583952387,
20.6961437823834));
#10964=CARTESIAN_POINT('Ctrl Pts',(1.6949690987159,-1.63843712229916,20.8231139896373));
#10965=CARTESIAN_POINT('Ctrl Pts',(2.29598727142038,0.534639036362976,20.9500841968912));
#10966=CARTESIAN_POINT('Ctrl Pts',(0.796811227132131,2.21866814035183,21.0770544041451));
#10967=CARTESIAN_POINT('Ctrl Pts',(-1.3725009971516,1.88233367605118,21.2006779656464));
#10968=CARTESIAN_POINT('Ctrl Pts',(-1.99399844799794,0.607362735608021,
21.2819781247298));
#10969=CARTESIAN_POINT('Ctrl Pts',(-1.99749018587619,-0.000921389143520883,
21.3209548813952));
#10970=CARTESIAN_POINT('Ctrl Pts',(-1.99684525596436,-0.00133650482941808,
20.6790451186048));
#10971=CARTESIAN_POINT('Ctrl Pts',(-1.99747501960825,-0.0830024421592919,
20.6842735464963));
#10972=CARTESIAN_POINT('Ctrl Pts',(-1.95584301886423,-0.825340921944485,
20.7318410810293));
#10973=CARTESIAN_POINT('Ctrl Pts',(-1.02554856753737,-2.12297808204117,
20.8217477222035));
#10974=CARTESIAN_POINT('Ctrl Pts',(1.22747389894261,-2.0129812788532,20.9487650421275));
#10975=CARTESIAN_POINT('Ctrl Pts',(2.35693366377738,-0.0604111340540538,
21.0757823620516));
#10976=CARTESIAN_POINT('Ctrl Pts',(1.32898482224672,1.94745606972551,21.2027996819756));
#10977=CARTESIAN_POINT('Ctrl Pts',(-0.915444287757947,2.1727281375204,21.3298170018996));
#10978=CARTESIAN_POINT('Ctrl Pts',(-1.93507962172209,0.894252387772451,
21.4218988141093));
#10979=CARTESIAN_POINT('Ctrl Pts',(-1.9969456548437,0.117449789491568,21.4716415196777));
#10980=CARTESIAN_POINT('Ctrl Pts',(-1.99590866900402,0.00166733638921734,
21.4790451186048));
#10981=CARTESIAN_POINT('Origin',(0.,0.,-1.47904511860479));
#10982=CARTESIAN_POINT('',(-1.99312087176262,0.00161274543637441,19.7209548813952));
#10983=CARTESIAN_POINT('',(-1.99180439006996,-0.000824340204725049,19.8790451186048));
#10984=CARTESIAN_POINT('',(-1.99475,4.03981020633857E-13,-1.47904511860479));
#10985=CARTESIAN_POINT('Ctrl Pts',(-1.99312087176262,0.00161274543637444,
19.7209548813952));
#10986=CARTESIAN_POINT('Ctrl Pts',(-1.98968192268936,-0.450377960742678,
19.7497540314656));
#10987=CARTESIAN_POINT('Ctrl Pts',(-1.61339717903016,-1.57179914144911,
19.8208765839539));
#10988=CARTESIAN_POINT('Ctrl Pts',(0.247048790610012,-2.34443241412816,
19.9343225388601));
#10989=CARTESIAN_POINT('Ctrl Pts',(2.10330301895634,-1.0646656093841,20.061292746114));
#10990=CARTESIAN_POINT('Ctrl Pts',(2.0356159034317,1.18897617430391,20.1882629533679));
#10991=CARTESIAN_POINT('Ctrl Pts',(0.10590245999703,2.35503314590555,20.3152331606218));
#10992=CARTESIAN_POINT('Ctrl Pts',(-1.66414125646537,1.49197284957946,20.4261304699642));
#10993=CARTESIAN_POINT('Ctrl Pts',(-1.98996716044266,0.411244685500659,
20.4947043768887));
#10994=CARTESIAN_POINT('Ctrl Pts',(-1.99224100758391,-0.00120392385877197,
20.5209548813952));
#10995=CARTESIAN_POINT('Ctrl Pts',(-1.99180439006996,-0.000824340204724841,
19.8790451186048));
#10996=CARTESIAN_POINT('Ctrl Pts',(-1.99284937662136,-0.281602094708555,
19.896905573315));
#10997=CARTESIAN_POINT('Ctrl Pts',(-1.80623847218132,-1.22665110166896,
19.9571051346665));
#10998=CARTESIAN_POINT('Ctrl Pts',(-0.357873132381371,-2.33038894229026,
20.0596438026594));
#10999=CARTESIAN_POINT('Ctrl Pts',(1.76383231338145,-1.56450675022861,20.1866611225834));
#11000=CARTESIAN_POINT('Ctrl Pts',(2.27102180036648,0.633439644702114,20.3136784425075));
#11001=CARTESIAN_POINT('Ctrl Pts',(0.699441717491183,2.25156991564901,20.4406957624314));
#11002=CARTESIAN_POINT('Ctrl Pts',(-1.42132417394977,1.82696424060745,20.5624846544639));
#11003=CARTESIAN_POINT('Ctrl Pts',(-1.99237527822705,0.578317346747391,
20.641934439855));
#11004=CARTESIAN_POINT('Ctrl Pts',(-1.99684525596436,-0.00133650482941808,
20.6790451186048));
#11005=CARTESIAN_POINT('Origin',(0.,0.,-1.47904511860479));
#11006=CARTESIAN_POINT('',(-1.99798271913518,0.000231452487769965,18.9209548813952));
#11007=CARTESIAN_POINT('',(-1.99382977638889,0.0017725417048866,19.0790451186048));
#11008=CARTESIAN_POINT('',(-1.99475,4.03981020633857E-13,-1.47904511860479));
#11009=CARTESIAN_POINT('Ctrl Pts',(-1.99798271913518,0.000231452487770123,
18.9209548813952));
#11010=CARTESIAN_POINT('Ctrl Pts',(-1.99691903787442,-0.647402032613039,
18.9624802836245));
#11011=CARTESIAN_POINT('Ctrl Pts',(-1.30211730807037,-1.95707393283707,
19.0463290882716));
#11012=CARTESIAN_POINT('Ctrl Pts',(0.928528238935361,-2.16684834699098,
19.1725012953368));
#11013=CARTESIAN_POINT('Ctrl Pts',(2.32393504393153,-0.395881751214744,
19.2994715025907));
#11014=CARTESIAN_POINT('Ctrl Pts',(1.59358313931722,1.73720730698498,19.4264417098446));
#11015=CARTESIAN_POINT('Ctrl Pts',(-0.594457200581991,2.28123148453506,
19.5534119170984));
#11016=CARTESIAN_POINT('Ctrl Pts',(-1.86578167130184,1.08846508423875,19.651582974282));
#11017=CARTESIAN_POINT('Ctrl Pts',(-1.99473582272346,0.213870272280659,
19.7074306290476));
#11018=CARTESIAN_POINT('Ctrl Pts',(-1.99312087176262,0.00161274543637444,
19.7209548813952));
#11019=CARTESIAN_POINT('Ctrl Pts',(-1.99382977638889,0.00177254170488682,
19.0790451186048));
#11020=CARTESIAN_POINT('Ctrl Pts',(-1.98972515875545,-0.476363613015602,
19.1095376001336));
#11021=CARTESIAN_POINT('Ctrl Pts',(-1.57755368547404,-1.62474792733362,
19.1823691883038));
#11022=CARTESIAN_POINT('Ctrl Pts',(0.341271742863524,-2.33287792195687,
19.2975398831153));
#11023=CARTESIAN_POINT('Ctrl Pts',(2.14508879272012,-0.978457905368288,
19.4245572030393));
#11024=CARTESIAN_POINT('Ctrl Pts',(1.98540848369728,1.27158914516195,19.5515745229634));
#11025=CARTESIAN_POINT('Ctrl Pts',(0.00839346700838828,2.35769280249617,
19.6785918428874));
#11026=CARTESIAN_POINT('Ctrl Pts',(-1.69722751078314,1.43643151043362,19.7877487081012));
#11027=CARTESIAN_POINT('Ctrl Pts',(-1.9903721834168,0.383995701278938,19.8545664666736));
#11028=CARTESIAN_POINT('Ctrl Pts',(-1.99180439006996,-0.000824340204724841,
19.8790451186048));
#11029=CARTESIAN_POINT('Origin',(0.,0.,-1.47904511860479));
#11030=CARTESIAN_POINT('',(-1.99379303657575,-0.00176355010682069,18.1209548813952));
#11031=CARTESIAN_POINT('',(-1.99798916403529,-0.000228181391768167,18.2790451186048));
#11032=CARTESIAN_POINT('',(-1.99475,4.03981020633857E-13,-1.47904511860479));
#11033=CARTESIAN_POINT('Ctrl Pts',(-1.99379303657575,-0.00176355010682052,
18.1209548813952));
#11034=CARTESIAN_POINT('Ctrl Pts',(-1.99538935452561,-0.188812871833617,
18.1328831333654));
#11035=CARTESIAN_POINT('Ctrl Pts',(-1.88545983445616,-1.03770416276352,
18.1871347877535));
#11036=CARTESIAN_POINT('Ctrl Pts',(-0.679802134300005,-2.25726948049166,
18.2837098445596));
#11037=CARTESIAN_POINT('Ctrl Pts',(1.52714444375655,-1.79589150486922,18.4106800518135));
#11038=CARTESIAN_POINT('Ctrl Pts',(2.33717564303521,0.30823118427704,18.5376502590674));
#11039=CARTESIAN_POINT('Ctrl Pts',(1.00933664148997,2.13040747123729,18.6646204663213));
#11040=CARTESIAN_POINT('Ctrl Pts',(-1.24176661487133,2.00384932655849,18.7915906735751));
#11041=CARTESIAN_POINT('Ctrl Pts',(-1.99226228190403,0.685182598197949,
18.8770354785998));
#11042=CARTESIAN_POINT('Ctrl Pts',(-1.99800316006534,0.0126771270771923,
18.9201568812065));
#11043=CARTESIAN_POINT('Ctrl Pts',(-1.99798271913518,0.000231452487770123,
18.9209548813952));
#11044=CARTESIAN_POINT('Ctrl Pts',(-1.99798916403529,-0.000228181391767968,
18.2790451186048));
#11045=CARTESIAN_POINT('Ctrl Pts',(-1.99800899793164,-0.012477266092771,
18.2798305203109));
#11046=CARTESIAN_POINT('Ctrl Pts',(-1.99235887395581,-0.685026095535388,
18.3229550286584));
#11047=CARTESIAN_POINT('Ctrl Pts',(-1.24177516838345,-2.00419066768041,
18.4084186436472));
#11048=CARTESIAN_POINT('Ctrl Pts',(1.01040701496368,-2.13022615356754,18.5354359635712));
#11049=CARTESIAN_POINT('Ctrl Pts',(2.33771769089012,-0.306368730340369,
18.6624532834953));
#11050=CARTESIAN_POINT('Ctrl Pts',(1.52520901414179,1.79792192945402,18.7894706034193));
#11051=CARTESIAN_POINT('Ctrl Pts',(-0.683392859853091,2.25649285403983,
18.9164879233433));
#11052=CARTESIAN_POINT('Ctrl Pts',(-1.8864156933587,1.03535444444075,19.0130127617384));
#11053=CARTESIAN_POINT('Ctrl Pts',(-1.99542446018947,0.187533079834375,
19.0671984934923));
#11054=CARTESIAN_POINT('Ctrl Pts',(-1.99382977638889,0.00177254170488682,
19.0790451186048));
#11055=CARTESIAN_POINT('Origin',(0.,0.,-1.47904511860479));
#11056=CARTESIAN_POINT('',(-1.99184618389856,0.000865127372006838,17.3209548813952));
#11057=CARTESIAN_POINT('',(-1.99316281920955,-0.00162934947814997,17.4790451186048));
#11058=CARTESIAN_POINT('',(-1.99475,4.03981020633857E-13,-1.47904511860479));
#11059=CARTESIAN_POINT('Ctrl Pts',(-1.99184618389856,0.000865127372006828,
17.3209548813952));
#11060=CARTESIAN_POINT('Ctrl Pts',(-1.99032959737337,-0.386699381348846,
17.3456093855243));
#11061=CARTESIAN_POINT('Ctrl Pts',(-1.69406802365858,-1.44172282084515,
17.4125872920713));
#11062=CARTESIAN_POINT('Ctrl Pts',(0.0172877380261932,-2.35734969477841,
17.5218886010363));
#11063=CARTESIAN_POINT('Ctrl Pts',(1.98947600304585,-1.26466662906185,17.6488588082902));
#11064=CARTESIAN_POINT('Ctrl Pts',(2.14184320547626,0.984837109634436,17.775829015544));
#11065=CARTESIAN_POINT('Ctrl Pts',(0.335015437913597,2.33348689855279,17.902799222798));
#11066=CARTESIAN_POINT('Ctrl Pts',(-1.57972676945643,1.62146721495462,18.0178411780816));
#11067=CARTESIAN_POINT('Ctrl Pts',(-1.98972535554673,0.474868926241488,
18.0905597309474));
#11068=CARTESIAN_POINT('Ctrl Pts',(-1.99379303657575,-0.00176355010682052,
18.1209548813952));
#11069=CARTESIAN_POINT('Ctrl Pts',(-1.99316281920955,-0.00162934947815016,
17.4790451186048));
#11070=CARTESIAN_POINT('Ctrl Pts',(-1.99478285074208,-0.212199013029784,
17.4924625471296));
#11071=CARTESIAN_POINT('Ctrl Pts',(-1.86711225706861,-1.08531368698141,
17.5482190822957));
#11072=CARTESIAN_POINT('Ctrl Pts',(-0.599428442729515,-2.28023493159759,
17.6463147241031));
#11073=CARTESIAN_POINT('Ctrl Pts',(1.5906925238854,-1.74025374462637,17.7733320440271));
#11074=CARTESIAN_POINT('Ctrl Pts',(2.32478025773261,0.392660864471763,17.9003493639512));
#11075=CARTESIAN_POINT('Ctrl Pts',(0.930890860039063,2.16615512092895,18.0273666838751));
#11076=CARTESIAN_POINT('Ctrl Pts',(-1.3011974724079,1.95816315404478,18.1535986020931));
#11077=CARTESIAN_POINT('Ctrl Pts',(-1.99693980054367,0.64784126818084,18.2374914136696));
#11078=CARTESIAN_POINT('Ctrl Pts',(-1.99798916403529,-0.000228181391767968,
18.2790451186048));
#11079=CARTESIAN_POINT('Origin',(0.,0.,-1.47904511860479));
#11080=CARTESIAN_POINT('',(-1.99695131403112,0.00127851392262751,16.5209548813952));
#11081=CARTESIAN_POINT('',(-1.99217715215978,0.00116458179186874,16.6790451186048));
#11082=CARTESIAN_POINT('',(-1.99475,4.03981020633857E-13,-1.47904511860479));
#11083=CARTESIAN_POINT('Ctrl Pts',(-1.99695131403112,0.0012785139226276,
16.5209548813952));
#11084=CARTESIAN_POINT('Ctrl Pts',(-1.99259585846887,-0.58251261776068,
16.5583356376832));
#11085=CARTESIAN_POINT('Ctrl Pts',(-1.41447577495437,-1.83479432529662,
16.6380397963891));
#11086=CARTESIAN_POINT('Ctrl Pts',(0.712834826853045,-2.24705650996661,
16.760067357513));
#11087=CARTESIAN_POINT('Ctrl Pts',(2.27426375960074,-0.620581018985151,
16.8870375647669));
#11088=CARTESIAN_POINT('Ctrl Pts',(1.75536948901827,1.57355470396859,17.0140077720207));
#11089=CARTESIAN_POINT('Ctrl Pts',(-0.36920304249889,2.32832247825929,17.1409779792746));
#11090=CARTESIAN_POINT('Ctrl Pts',(-1.80909353809998,1.2203103924296,17.2432936823995));
#11091=CARTESIAN_POINT('Ctrl Pts',(-1.99293306088134,0.278617129567366,
17.3032859831063));
#11092=CARTESIAN_POINT('Ctrl Pts',(-1.99184618389856,0.000865127372006828,
17.3209548813952));
#11093=CARTESIAN_POINT('Ctrl Pts',(-1.99217715215978,0.00116458179186867,
16.6790451186048));
#11094=CARTESIAN_POINT('Ctrl Pts',(-1.98999999646129,-0.40815773762222,
16.7050945739482));
#11095=CARTESIAN_POINT('Ctrl Pts',(-1.66793149151012,-1.48590988532565,
16.7734831359329));
#11096=CARTESIAN_POINT('Ctrl Pts',(0.0956287989740662,-2.355767589139,16.884210804559));
#11097=CARTESIAN_POINT('Ctrl Pts',(2.03110108030785,-1.19725277314494,17.011228124483));
#11098=CARTESIAN_POINT('Ctrl Pts',(2.10741414159636,1.05716197294014,17.138245444407));
#11099=CARTESIAN_POINT('Ctrl Pts',(0.254715166118652,2.34390827153712,17.2652627643311));
#11100=CARTESIAN_POINT('Ctrl Pts',(-1.61079803731833,1.57588134084248,17.3788626557303));
#11101=CARTESIAN_POINT('Ctrl Pts',(-1.98967079162499,0.45226000935907,17.4501234404882));
#11102=CARTESIAN_POINT('Ctrl Pts',(-1.99316281920955,-0.00162934947815016,
17.4790451186048));
#11103=CARTESIAN_POINT('Origin',(0.,0.,-1.47904511860479));
#11104=CARTESIAN_POINT('',(-1.99572977164192,-0.00170384222700574,15.7209548813952));
#11105=CARTESIAN_POINT('',(-1.99740160550243,0.000998204556411052,15.8790451186048));
#11106=CARTESIAN_POINT('',(-1.99475,4.03981020633857E-13,-1.47904511860479));
#11107=CARTESIAN_POINT('Ctrl Pts',(-1.99572977164192,-0.00170384222700588,
15.7209548813952));
#11108=CARTESIAN_POINT('Ctrl Pts',(-1.99683270343229,-0.123457329418355,
15.7287384874241));
#11109=CARTESIAN_POINT('Ctrl Pts',(-1.93126068112857,-0.906060978578068,
15.7788454958709));
#11110=CARTESIAN_POINT('Ctrl Pts',(-0.896648704865739,-2.18023337040339,
15.8712759067358));
#11111=CARTESIAN_POINT('Ctrl Pts',(1.34476747364227,-1.93623265420035,15.9982461139896));
#11112=CARTESIAN_POINT('Ctrl Pts',(2.35609282970634,0.0788861658613507,
16.1252163212435));
#11113=CARTESIAN_POINT('Ctrl Pts',(1.21224398394502,2.02184593200051,16.2521865284974));
#11114=CARTESIAN_POINT('Ctrl Pts',(-1.04047329330418,2.11537509091856,16.3791567357513));
#11115=CARTESIAN_POINT('Ctrl Pts',(-1.95843139238505,0.816055134121286,
16.4687461867172));
#11116=CARTESIAN_POINT('Ctrl Pts',(-1.99752721130333,0.0784699157103159,
16.5160122352652));
#11117=CARTESIAN_POINT('Ctrl Pts',(-1.99695131403112,0.0012785139226276,
16.5209548813952));
#11118=CARTESIAN_POINT('Ctrl Pts',(-1.99740160550243,0.00099820455641106,
15.8790451186048));
#11119=CARTESIAN_POINT('Ctrl Pts',(-1.99370023614505,-0.602748628883622,
15.9177266007668));
#11120=CARTESIAN_POINT('Ctrl Pts',(-1.38028516085263,-1.87384538130254,
15.9987471895702));
#11121=CARTESIAN_POINT('Ctrl Pts',(0.782276957985213,-2.22414670429727,
16.1221068850149));
#11122=CARTESIAN_POINT('Ctrl Pts',(2.2929055224434,-0.548971826580871,16.249124204939));
#11123=CARTESIAN_POINT('Ctrl Pts',(1.704733350654,1.62870193847707,16.3761415248629));
#11124=CARTESIAN_POINT('Ctrl Pts',(-0.443858810723858,2.31555072442255,
16.503158844787));
#11125=CARTESIAN_POINT('Ctrl Pts',(-1.82884408866752,1.17669301721355,16.6041267093676));
#11126=CARTESIAN_POINT('Ctrl Pts',(-1.99353860508394,0.257128392313624,
16.6627554673068));
#11127=CARTESIAN_POINT('Ctrl Pts',(-1.99217715215978,0.00116458179186867,
16.6790451186048));
#11128=CARTESIAN_POINT('Origin',(0.,0.,-1.47904511860479));
#11129=CARTESIAN_POINT('',(-1.99149560426942,-0.000167792983348677,14.9209548813952));
#11130=CARTESIAN_POINT('',(-1.99517067278375,-0.00179390005510177,15.0790451186048));
#11131=CARTESIAN_POINT('',(-1.99475,4.03981020633857E-13,-1.47904511860479));
#11132=CARTESIAN_POINT('Ctrl Pts',(-1.99149560426942,-0.000167792983348583,
14.9209548813952));
#11133=CARTESIAN_POINT('Ctrl Pts',(-1.99173785851776,-0.322720966835465,
14.941464739583));
#11134=CARTESIAN_POINT('Ctrl Pts',(-1.76536638897614,-1.31056254377754,
15.0042980001888));
#11135=CARTESIAN_POINT('Ctrl Pts',(-0.21263805117564,-2.34780354982058,
15.1094546632124));
#11136=CARTESIAN_POINT('Ctrl Pts',(1.85669106744545,-1.45261651148066,15.2364248704663));
#11137=CARTESIAN_POINT('Ctrl Pts',(2.22766066522509,0.771313431729834,15.3633950777202));
#11138=CARTESIAN_POINT('Ctrl Pts',(0.560936019559882,2.28970461660849,15.4903652849741));
#11139=CARTESIAN_POINT('Ctrl Pts',(-1.48526110718087,1.74896222764933,15.6095518861991));
#11140=CARTESIAN_POINT('Ctrl Pts',(-1.99083550549725,0.538577955392992,
15.6864150850061));
#11141=CARTESIAN_POINT('Ctrl Pts',(-1.99572977164192,-0.00170384222700588,
15.7209548813952));
#11142=CARTESIAN_POINT('Ctrl Pts',(-1.99517067278375,-0.00179390005510177,
15.0790451186048));
#11143=CARTESIAN_POINT('Ctrl Pts',(-1.99646803238674,-0.14227544571559,
15.0880195209441));
#11144=CARTESIAN_POINT('Ctrl Pts',(-1.91885345210777,-0.944092523599761,
15.1393330299248));
#11145=CARTESIAN_POINT('Ctrl Pts',(-0.834420476588558,-2.20511411711067,
15.2329856455468));
#11146=CARTESIAN_POINT('Ctrl Pts',(1.40013588510504,-1.89694631038207,15.3600029654708));
#11147=CARTESIAN_POINT('Ctrl Pts',(2.35308417453332,0.147582752352149,15.4870202853949));
#11148=CARTESIAN_POINT('Ctrl Pts',(1.15214746973809,2.05702260785027,15.6140376053188));
#11149=CARTESIAN_POINT('Ctrl Pts',(-1.10340222895637,2.08357608989091,15.7410549252429));
#11150=CARTESIAN_POINT('Ctrl Pts',(-1.9696398684246,0.775661723098001,15.8293907630048));
#11151=CARTESIAN_POINT('Ctrl Pts',(-1.99775159775743,0.0580869993455256,
15.8753874941255));
#11152=CARTESIAN_POINT('Ctrl Pts',(-1.99740160550243,0.00099820455641106,
15.8790451186048));
#11153=CARTESIAN_POINT('Origin',(0.,0.,-1.47904511860479));
#11154=CARTESIAN_POINT('',(-1.99511464393632,0.00179586406614344,14.1209548813952));
#11155=CARTESIAN_POINT('',(-1.99148314676551,0.000112721033546509,14.2790451186048));
#11156=CARTESIAN_POINT('',(-1.99475,4.03981020633857E-13,-1.47904511860479));
#11157=CARTESIAN_POINT('Ctrl Pts',(-1.99511464393632,0.00179586406614349,
14.1209548813952));
#11158=CARTESIAN_POINT('Ctrl Pts',(-1.99031466719488,-0.518505987664431,
14.1541909917419));
#11159=CARTESIAN_POINT('Ctrl Pts',(-1.51608605094631,-1.70912036928094,
14.2297505045065));
#11160=CARTESIAN_POINT('Ctrl Pts',(0.490348739021751,-2.30585224233855,
14.3476334196891));
#11161=CARTESIAN_POINT('Ctrl Pts',(2.20292078401032,-0.839366706948347,
14.474603626943));
#11162=CARTESIAN_POINT('Ctrl Pts',(1.90042874387294,1.39490753773124,14.6015738341969));
#11163=CARTESIAN_POINT('Ctrl Pts',(-0.140430710978244,2.35322664968167,
14.7285440414508));
#11164=CARTESIAN_POINT('Ctrl Pts',(-1.74391877908516,1.35190122394337,14.8350043905169));
#11165=CARTESIAN_POINT('Ctrl Pts',(-1.99123795140256,0.342888110182512,
14.899141337165));
#11166=CARTESIAN_POINT('Ctrl Pts',(-1.99149560426942,-0.000167792983348583,
14.9209548813952));
#11167=CARTESIAN_POINT('Ctrl Pts',(-1.99148314676551,0.000112721033546474,
14.2790451186048));
#11168=CARTESIAN_POINT('Ctrl Pts',(-1.99131185922732,-0.339690971417257,
14.3006515477628));
#11169=CARTESIAN_POINT('Ctrl Pts',(-1.74734127274221,-1.34559130575002,
14.3645970835621));
#11170=CARTESIAN_POINT('Ctrl Pts',(-0.151061206087832,-2.35286342851562,
14.4708817260027));
#11171=CARTESIAN_POINT('Ctrl Pts',(1.89487438652815,-1.40293865172736,14.5978990459267));
#11172=CARTESIAN_POINT('Ctrl Pts',(2.2063452493004,0.831159697122361,14.7249163658507));
#11173=CARTESIAN_POINT('Ctrl Pts',(0.498247931734623,2.30445976310136,14.8519336857748));
#11174=CARTESIAN_POINT('Ctrl Pts',(-1.51300932258991,1.7133249444358,14.9699766033595));
#11175=CARTESIAN_POINT('Ctrl Pts',(-1.99034739677153,0.520483244831458,
15.0456804143028));
#11176=CARTESIAN_POINT('Ctrl Pts',(-1.99517067278375,-0.00179390005510177,
15.0790451186048));
#11177=CARTESIAN_POINT('Origin',(0.,0.,-1.47904511860479));
#11178=CARTESIAN_POINT('',(-1.99740252611268,-0.000992144320337381,13.3209548813952));
#11179=CARTESIAN_POINT('',(-1.9955844561164,0.00173554905423284,13.4790451186048));
#11180=CARTESIAN_POINT('',(-1.99475,4.03981020633857E-13,-1.47904511860479));
#11181=CARTESIAN_POINT('Ctrl Pts',(-1.99740252611268,-0.000992144320337198,
13.3209548813952));
#11182=CARTESIAN_POINT('Ctrl Pts',(-1.99774913123626,-0.0577895479995564,
13.3245938414828));
#11183=CARTESIAN_POINT('Ctrl Pts',(-1.96979972317684,-0.774830503751046,
13.3705562039884));
#11184=CARTESIAN_POINT('Ctrl Pts',(-1.10495101849633,-2.08242159422195,
13.4588419689119));
#11185=CARTESIAN_POINT('Ctrl Pts',(1.14957607715301,-2.05812324514239,13.5858121761658));
#11186=CARTESIAN_POINT('Ctrl Pts',(2.35255856756512,-0.151210566872388,
13.7127823834197));
#11187=CARTESIAN_POINT('Ctrl Pts',(1.40359972987109,1.894018016721,13.8397525906736));
#11188=CARTESIAN_POINT('Ctrl Pts',(-0.829265195633706,2.20674323034388,
13.9667227979275));
#11189=CARTESIAN_POINT('Ctrl Pts',(-1.91765995199167,0.947432563273637,
14.0604568948347));
#11190=CARTESIAN_POINT('Ctrl Pts',(-1.99642703549267,0.144054836087643,
14.1118675893239));
#11191=CARTESIAN_POINT('Ctrl Pts',(-1.99511464393632,0.00179586406614349,
14.1209548813952));
#11192=CARTESIAN_POINT('Ctrl Pts',(-1.9955844561164,0.00173554905423281,
13.4790451186048));
#11193=CARTESIAN_POINT('Ctrl Pts',(-1.9906881467987,-0.533933096035126,
13.5132835745814));
#11194=CARTESIAN_POINT('Ctrl Pts',(-1.4923926878599,-1.74004025674718,13.5898611371993));
#11195=CARTESIAN_POINT('Ctrl Pts',(0.545581575104675,-2.2937145738163,13.7087778064586));
#11196=CARTESIAN_POINT('Ctrl Pts',(2.22298781706136,-0.785564107140691,
13.8357951263826));
#11197=CARTESIAN_POINT('Ctrl Pts',(1.86559217928514,1.44164892460722,13.9628124463066));
#11198=CARTESIAN_POINT('Ctrl Pts',(-0.199464851904689,2.34925511047346,
14.0898297662307));
#11199=CARTESIAN_POINT('Ctrl Pts',(-1.76172155469051,1.31788471912336,14.1952406569967));
#11200=CARTESIAN_POINT('Ctrl Pts',(-1.99164750753333,0.326174945926526,
14.2583124411214));
#11201=CARTESIAN_POINT('Ctrl Pts',(-1.99148314676551,0.000112721033546474,
14.2790451186048));
#11202=CARTESIAN_POINT('Origin',(0.,0.,-1.47904511860479));
#11203=CARTESIAN_POINT('',(-1.9921588650168,-0.00114591747005889,12.5209548813952));
#11204=CARTESIAN_POINT('',(-1.99710797193854,-0.00119562967828307,12.6790451186048));
#11205=CARTESIAN_POINT('',(-1.99475,4.03981020633857E-13,-1.47904511860479));
#11206=CARTESIAN_POINT('Ctrl Pts',(-1.9921588650168,-0.00114591747005909,
12.5209548813952));
#11207=CARTESIAN_POINT('Ctrl Pts',(-1.99350475755727,-0.25830313556317,
12.5373200936417));
#11208=CARTESIAN_POINT('Ctrl Pts',(-1.82781441796359,-1.17884773168539,
12.5960087083062));
#11209=CARTESIAN_POINT('Ctrl Pts',(-0.440537590706227,-2.31588494544368,
12.6970207253886));
#11210=CARTESIAN_POINT('Ctrl Pts',(1.70621353334662,-1.62672426304606,12.8239909326425));
#11211=CARTESIAN_POINT('Ctrl Pts',(2.29225051935244,0.550439829487665,12.9509611398964));
#11212=CARTESIAN_POINT('Ctrl Pts',(0.781511384680127,2.22410350590373,13.0779313471503));
#11213=CARTESIAN_POINT('Ctrl Pts',(-1.3803090509661,1.87366660161095,13.2012625943166));
#11214=CARTESIAN_POINT('Ctrl Pts',(-1.99371789490167,0.602800102433931,
13.2822704390649));
#11215=CARTESIAN_POINT('Ctrl Pts',(-1.99740252611268,-0.000992144320337198,
13.3209548813952));
#11216=CARTESIAN_POINT('Ctrl Pts',(-1.99710797193854,-0.00119562967828295,
12.6790451186048));
#11217=CARTESIAN_POINT('Ctrl Pts',(-1.99760917397881,-0.0719494836075869,
12.6835764947587));
#11218=CARTESIAN_POINT('Ctrl Pts',(-1.96208750924084,-0.803286251661634,
12.7304469775539));
#11219=CARTESIAN_POINT('Ctrl Pts',(-1.06027625346291,-2.10584901347975,
12.8196565669905));
#11220=CARTESIAN_POINT('Ctrl Pts',(1.19424884442458,-2.03286878544129,12.9466738869145));
#11221=CARTESIAN_POINT('Ctrl Pts',(2.35562364483704,-0.0991112764303932,
13.0736912068385));
#11222=CARTESIAN_POINT('Ctrl Pts',(1.36078895832842,1.92536729278402,13.2007085267625));
#11223=CARTESIAN_POINT('Ctrl Pts',(-0.879637768350177,2.18746958783955,
13.3277258466866));
#11224=CARTESIAN_POINT('Ctrl Pts',(-1.92800865020163,0.916362008260045,
13.420504710634));
#11225=CARTESIAN_POINT('Ctrl Pts',(-1.99674289887317,0.12847212178069,13.4709444679401));
#11226=CARTESIAN_POINT('Ctrl Pts',(-1.9955844561164,0.00173554905423281,
13.4790451186048));
#11227=CARTESIAN_POINT('Origin',(0.,0.,-1.47904511860479));
#11228=CARTESIAN_POINT('',(-1.99323815944991,0.00164697314138954,11.7209548813952));
#11229=CARTESIAN_POINT('',(-1.99195362472057,-0.000981272968664654,11.8790451186048));
#11230=CARTESIAN_POINT('',(-1.99475,4.03981020633857E-13,-1.47904511860479));
#11231=CARTESIAN_POINT('Ctrl Pts',(-1.99323815944991,0.00164697314138934,
11.7209548813952));
#11232=CARTESIAN_POINT('Ctrl Pts',(-1.98967599032796,-0.454863659793869,
11.7500463458006));
#11233=CARTESIAN_POINT('Ctrl Pts',(-1.6073406180934,-1.58091626896194,11.821461212624));
#11234=CARTESIAN_POINT('Ctrl Pts',(0.263190068058092,-2.34267527357795,
11.9351994818653));
#11235=CARTESIAN_POINT('Ctrl Pts',(2.11058595164912,-1.05015398397536,12.0621696891192));
#11236=CARTESIAN_POINT('Ctrl Pts',(2.0273786194508,1.20296815533566,12.1891398963731));
#11237=CARTESIAN_POINT('Ctrl Pts',(0.0896797991062791,2.35570668441345,
12.316110103627));
#11238=CARTESIAN_POINT('Ctrl Pts',(-1.66972777748032,1.4827828112436,12.4267150986343));
#11239=CARTESIAN_POINT('Ctrl Pts',(-1.99002403572222,0.406751998589953,
12.4949966912238));
#11240=CARTESIAN_POINT('Ctrl Pts',(-1.9921588650168,-0.00114591747005909,
12.5209548813952));
#11241=CARTESIAN_POINT('Ctrl Pts',(-1.99195362472057,-0.000981272968664897,
11.8790451186048));
#11242=CARTESIAN_POINT('Ctrl Pts',(-1.99315423945754,-0.270750376731748,
11.8962085215773));
#11243=CARTESIAN_POINT('Ctrl Pts',(-1.81641900129272,-1.20448536032894,
11.9557110311912));
#11244=CARTESIAN_POINT('Ctrl Pts',(-0.396097208116597,-2.32419723839291,
12.0575526474464));
#11245=CARTESIAN_POINT('Ctrl Pts',(1.737900288011,-1.59326344028923,12.1845699673704));
#11246=CARTESIAN_POINT('Ctrl Pts',(2.28111858791796,0.596056867325744,12.3115872872944));
#11247=CARTESIAN_POINT('Ctrl Pts',(0.736325268973554,2.23977920775732,12.4386046072184));
#11248=CARTESIAN_POINT('Ctrl Pts',(-1.40330431850088,1.84782993570273,12.5610905509886));
#11249=CARTESIAN_POINT('Ctrl Pts',(-1.99292617130783,0.589142172669957,
12.6412373881174));
#11250=CARTESIAN_POINT('Ctrl Pts',(-1.99710797193854,-0.00119562967828295,
12.6790451186048));
#11251=CARTESIAN_POINT('Origin',(0.,0.,-1.47904511860479));
#11252=CARTESIAN_POINT('',(-1.99800253719316,0.00014696211896244,10.9209548813952));
#11253=CARTESIAN_POINT('',(-1.99352514341734,0.00171980163322982,11.0790451186048));
#11254=CARTESIAN_POINT('',(-1.99475,4.03981020633857E-13,-1.47904511860479));
#11255=CARTESIAN_POINT('Ctrl Pts',(-1.99800253719316,0.00014696211896245,
10.9209548813952));
#11256=CARTESIAN_POINT('Ctrl Pts',(-1.99731048143793,-0.652028054488447,
10.9627725979595));
#11257=CARTESIAN_POINT('Ctrl Pts',(-1.29377835363174,-1.96554537055817,
11.0469137169418));
#11258=CARTESIAN_POINT('Ctrl Pts',(0.943430253008483,-2.16040176982576,
11.173378238342));
#11259=CARTESIAN_POINT('Ctrl Pts',(2.32660653495589,-0.379866398696293,
11.3003484455959));
#11260=CARTESIAN_POINT('Ctrl Pts',(1.58158043085374,1.74814181063735,11.4273186528497));
#11261=CARTESIAN_POINT('Ctrl Pts',(-0.610154945358331,2.27708308851757,
11.5542888601037));
#11262=CARTESIAN_POINT('Ctrl Pts',(-1.86947320797437,1.07916638007941,11.6521676029521));
#11263=CARTESIAN_POINT('Ctrl Pts',(-1.99485837355653,0.209285898184941,
11.7077229433827));
#11264=CARTESIAN_POINT('Ctrl Pts',(-1.99323815944991,0.00164697314138934,
11.7209548813952));
#11265=CARTESIAN_POINT('Ctrl Pts',(-1.99352514341734,0.00171980163322982,
11.0790451186048));
#11266=CARTESIAN_POINT('Ctrl Pts',(-1.98967826936081,-0.465667208835488,
11.1088405483959));
#11267=CARTESIAN_POINT('Ctrl Pts',(-1.59248298847649,-1.60309637919185,
11.1809750848285));
#11268=CARTESIAN_POINT('Ctrl Pts',(0.302912497167387,-2.33816804791504,
11.2954487279023));
#11269=CARTESIAN_POINT('Ctrl Pts',(2.12873011938496,-1.01355507006492,11.4224660478263));
#11270=CARTESIAN_POINT('Ctrl Pts',(2.00602422063487,1.2388109732551,11.5494833677503));
#11271=CARTESIAN_POINT('Ctrl Pts',(0.0471130923241888,2.35723697530873,
11.6765006876744));
#11272=CARTESIAN_POINT('Ctrl Pts',(-1.68439473653372,1.45840831064242,11.7863546046258));
#11273=CARTESIAN_POINT('Ctrl Pts',(-1.99019253335153,0.394722715698714,
11.853869414936));
#11274=CARTESIAN_POINT('Ctrl Pts',(-1.99195362472057,-0.000981272968664897,
11.8790451186048));
#11275=CARTESIAN_POINT('Origin',(0.,0.,-1.47904511860479));
#11276=CARTESIAN_POINT('',(-1.99366456530849,-0.00174269800029035,10.1209548813952));
#11277=CARTESIAN_POINT('',(-1.99802112857236,-2.57504959200183E-5,10.2790451186048));
#11278=CARTESIAN_POINT('',(-1.99475,4.03981020633857E-13,-1.47904511860479));
#11279=CARTESIAN_POINT('Ctrl Pts',(-1.99366456530849,-0.00174269800029027,
10.1209548813952));
#11280=CARTESIAN_POINT('Ctrl Pts',(-1.99527275468271,-0.193407171486628,
10.1331754477005));
#11281=CARTESIAN_POINT('Ctrl Pts',(-1.88194262316761,-1.04699937041106,
10.1877194164236));
#11282=CARTESIAN_POINT('Ctrl Pts',(-0.664239202615746,-2.26189803728336,
10.2845867875648));
#11283=CARTESIAN_POINT('Ctrl Pts',(1.53947731651516,-1.78533079324062,10.4115569948187));
#11284=CARTESIAN_POINT('Ctrl Pts',(2.33499728455247,0.32432102998492,10.5385272020725));
#11285=CARTESIAN_POINT('Ctrl Pts',(0.994639648129273,2.13730868611139,10.6654974093264));
#11286=CARTESIAN_POINT('Ctrl Pts',(-1.25553855339793,1.9952492050592,10.7924676165803));
#11287=CARTESIAN_POINT('Ctrl Pts',(-1.99439780105699,0.675973613661738,
10.8776201072699));
#11288=CARTESIAN_POINT('Ctrl Pts',(-1.99801090596205,0.00803346829660538,
10.9204491955416));
#11289=CARTESIAN_POINT('Ctrl Pts',(-1.99800253719316,0.00014696211896245,
10.9209548813952));
#11290=CARTESIAN_POINT('Ctrl Pts',(-1.99802112857236,-2.57504959202544E-5,
10.2790451186048));
#11291=CARTESIAN_POINT('Ctrl Pts',(-1.99802139127224,-0.0014035926386325,
10.2791334685732));
#11292=CARTESIAN_POINT('Ctrl Pts',(-1.997396130801,-0.66307124280884,10.3215609251831));
#11293=CARTESIAN_POINT('Ctrl Pts',(-1.27452282778516,-1.98352649659275,
10.4063274884342));
#11294=CARTESIAN_POINT('Ctrl Pts',(0.975285705239301,-2.14653292413298,
10.5333448083582));
#11295=CARTESIAN_POINT('Ctrl Pts',(2.33237086341372,-0.344720113613569,
10.6603621282822));
#11296=CARTESIAN_POINT('Ctrl Pts',(1.5545308633467,1.77263069930924,10.7873794482062));
#11297=CARTESIAN_POINT('Ctrl Pts',(-0.646241956488163,2.2674119905534,10.9143967681303));
#11298=CARTESIAN_POINT('Ctrl Pts',(-1.87798874059562,1.0575211530769,11.0116186582631));
#11299=CARTESIAN_POINT('Ctrl Pts',(-1.99514465169048,0.19848660997858,11.0665014417546));
#11300=CARTESIAN_POINT('Ctrl Pts',(-1.99352514341734,0.00171980163322982,
11.0790451186048));
#11301=CARTESIAN_POINT('Origin',(0.,0.,-1.47904511860479));
#11302=CARTESIAN_POINT('',(-1.99190842477769,0.000930945868489363,9.32095488139522));
#11303=CARTESIAN_POINT('',(-1.99344998719875,-0.00170364987860938,9.47904511860478));
#11304=CARTESIAN_POINT('',(-1.99475,4.03981020633857E-13,-1.47904511860479));
#11305=CARTESIAN_POINT('Ctrl Pts',(-1.99190842477769,0.000930945868489394,
9.32095488139522));
#11306=CARTESIAN_POINT('Ctrl Pts',(-1.99025409107239,-0.391198045614882,
9.34590169985934));
#11307=CARTESIAN_POINT('Ctrl Pts',(-1.68869165330305,-1.45093925392043,
9.41317192074142));
#11308=CARTESIAN_POINT('Ctrl Pts',(0.0335234320998379,-2.35717471326548,
9.52276554404145));
#11309=CARTESIAN_POINT('Ctrl Pts',(1.99813913054961,-1.25093423661054,9.64973575129535));
#11310=CARTESIAN_POINT('Ctrl Pts',(2.13500939744307,0.999565566727712,9.77670595854921));
#11311=CARTESIAN_POINT('Ctrl Pts',(0.318935741240959,2.33573894995075,9.90367616580313));
#11312=CARTESIAN_POINT('Ctrl Pts',(-1.58600439547375,1.61239114596766,10.0184258067518));
#11313=CARTESIAN_POINT('Ctrl Pts',(-1.98970312359121,0.470383068506138,
10.0908520452825));
#11314=CARTESIAN_POINT('Ctrl Pts',(-1.99366456530849,-0.00174269800029027,
10.1209548813952));
#11315=CARTESIAN_POINT('Ctrl Pts',(-1.99344998719875,-0.0017036498786095,
9.47904511860478));
#11316=CARTESIAN_POINT('Ctrl Pts',(-1.99507240931094,-0.201261304212527,
9.49176549539188));
#11317=CARTESIAN_POINT('Ctrl Pts',(-1.87581742430337,-1.06314114597083,
9.54682497882032));
#11318=CARTESIAN_POINT('Ctrl Pts',(-0.636796252956758,-2.27008289131724,
9.64422356889009));
#11319=CARTESIAN_POINT('Ctrl Pts',(1.5618975293753,-1.76614323002478,9.77124088881411));
#11320=CARTESIAN_POINT('Ctrl Pts',(2.33091544739048,0.354427677174692,9.89825820873813));
#11321=CARTESIAN_POINT('Ctrl Pts',(0.966340415661779,2.15057480741536,10.0252755286621));
#11322=CARTESIAN_POINT('Ctrl Pts',(-1.28120553730588,1.97832287734288,10.1522044986177));
#11323=CARTESIAN_POINT('Ctrl Pts',(-1.99789550012917,0.65888646097121,10.2367943619319));
#11324=CARTESIAN_POINT('Ctrl Pts',(-1.99802112857236,-2.57504959202544E-5,
10.2790451186048));
#11325=CARTESIAN_POINT('Origin',(0.,0.,-1.47904511860479));
#11326=CARTESIAN_POINT('',(-1.99706026989319,0.00121875038140872,8.52095488139522));
#11327=CARTESIAN_POINT('',(-1.991995621869,0.00101962588792096,8.67904511860479));
#11328=CARTESIAN_POINT('',(-1.99475,4.03981020633857E-13,-1.47904511860479));
#11329=CARTESIAN_POINT('Ctrl Pts',(-1.99706026989319,0.00121875038140875,
8.52095488139522));
#11330=CARTESIAN_POINT('Ctrl Pts',(-1.99282941906458,-0.587053347272268,
8.55862795201823));
#11331=CARTESIAN_POINT('Ctrl Pts',(-1.40690779658877,-1.84354047944384,
8.63862442505921));
#11332=CARTESIAN_POINT('Ctrl Pts',(0.72829438578655,-2.24209360575996,8.76094430051814));
#11333=CARTESIAN_POINT('Ctrl Pts',(2.27848403144356,-0.604902444874099,
8.88791450777203));
#11334=CARTESIAN_POINT('Ctrl Pts',(1.74449009064557,1.58560738299156,9.01488471502591));
#11335=CARTESIAN_POINT('Ctrl Pts',(-0.385230466394427,2.32572438975891,
9.1418549222798));
#11336=CARTESIAN_POINT('Ctrl Pts',(-1.81336359917182,1.21101525639225,9.24387831106957));
#11337=CARTESIAN_POINT('Ctrl Pts',(-1.99306074280009,0.274066470185944,
9.30357829744137));
#11338=CARTESIAN_POINT('Ctrl Pts',(-1.99190842477769,0.000930945868489394,
9.32095488139522));
#11339=CARTESIAN_POINT('Ctrl Pts',(-1.991995621869,0.00101962588792109,
8.67904511860479));
#11340=CARTESIAN_POINT('Ctrl Pts',(-1.99015055945641,-0.397440654073741,
8.70439752221052));
#11341=CARTESIAN_POINT('Ctrl Pts',(-1.68109935098533,-1.46397429262776,
8.77208903245758));
#11342=CARTESIAN_POINT('Ctrl Pts',(0.0569267623458949,-2.35702039553327,
8.882119649346));
#11343=CARTESIAN_POINT('Ctrl Pts',(2.01116447809095,-1.23044839115509,9.00913696927002));
#11344=CARTESIAN_POINT('Ctrl Pts',(2.12449185277921,1.02240900265292,9.13615428919402));
#11345=CARTESIAN_POINT('Ctrl Pts',(0.293175184736282,2.33940892369971,9.26317160911806));
#11346=CARTESIAN_POINT('Ctrl Pts',(-1.59622253240353,1.59759918753759,9.37746855225496));
#11347=CARTESIAN_POINT('Ctrl Pts',(-1.98967226244618,0.462955876563709,
9.44942638875054));
#11348=CARTESIAN_POINT('Ctrl Pts',(-1.99344998719875,-0.0017036498786095,
9.47904511860478));
#11349=CARTESIAN_POINT('Origin',(0.,0.,-1.47904511860479));
#11350=CARTESIAN_POINT('',(-1.99559319474839,-0.00173033593146375,7.72095488139522));
#11351=CARTESIAN_POINT('',(-1.99717077118997,0.00115749627489468,7.87904511860478));
#11352=CARTESIAN_POINT('',(-1.99475,4.03981020633857E-13,-1.47904511860479));
#11353=CARTESIAN_POINT('Ctrl Pts',(-1.99559319474839,-0.00173033593146354,
7.72095488139522));
#11354=CARTESIAN_POINT('Ctrl Pts',(-1.99674614175328,-0.128078601059412,
7.72903080175916));
#11355=CARTESIAN_POINT('Ctrl Pts',(-1.92827410556723,-0.91533394716936,
7.77943012454107));
#11356=CARTESIAN_POINT('Ctrl Pts',(-0.8816112114347,-2.18635727209223,7.87215284974095));
#11357=CARTESIAN_POINT('Ctrl Pts',(1.35807126336241,-1.92692472426588,7.99912305699481));
#11358=CARTESIAN_POINT('Ctrl Pts',(2.35549362254096,0.0951117423181714,
8.12609326424872));
#11359=CARTESIAN_POINT('Ctrl Pts',(1.19828988895336,2.03014723391927,8.25306347150259));
#11360=CARTESIAN_POINT('Ctrl Pts',(-1.05501813323409,2.10815871980864,8.38003367875648));
#11361=CARTESIAN_POINT('Ctrl Pts',(-1.96103960865442,0.806807176619804,
8.46933081538736));
#11362=CARTESIAN_POINT('Ctrl Pts',(-1.99758252252093,0.0738345577621752,
8.51630454960027));
#11363=CARTESIAN_POINT('Ctrl Pts',(-1.99706026989319,0.00121875038140875,
8.52095488139522));
#11364=CARTESIAN_POINT('Ctrl Pts',(-1.99717077118997,0.00115749627489461,
7.87904511860478));
#11365=CARTESIAN_POINT('Ctrl Pts',(-1.9930751220383,-0.591890300141836,
7.91702954902914));
#11366=CARTESIAN_POINT('Ctrl Pts',(-1.39868792096064,-1.85310383721029,
7.99735308609486));
#11367=CARTESIAN_POINT('Ctrl Pts',(0.745643944080418,-2.23669419230417,
8.1200157298019));
#11368=CARTESIAN_POINT('Ctrl Pts',(2.28358043018348,-0.586554532941333,
8.24703304972591));
#11369=CARTESIAN_POINT('Ctrl Pts',(1.73125186121253,1.60048517465147,8.37405036964994));
#11370=CARTESIAN_POINT('Ctrl Pts',(-0.405770296472382,2.32252799073159,
8.50106768957393));
#11371=CARTESIAN_POINT('Ctrl Pts',(-1.81896177685869,1.19886546994113,8.60273260589224));
#11372=CARTESIAN_POINT('Ctrl Pts',(-1.99323185681431,0.267997327586453,
8.66205841556918));
#11373=CARTESIAN_POINT('Ctrl Pts',(-1.991995621869,0.00101962588792109,
8.67904511860479));
#11374=CARTESIAN_POINT('Origin',(0.,0.,-1.47904511860479));
#11375=CARTESIAN_POINT('',(-1.99148666886423,-9.26359632818219E-5,6.92095488139522));
#11376=CARTESIAN_POINT('',(-1.995501255299,-0.00174979995018254,7.07904511860477));
#11377=CARTESIAN_POINT('',(-1.99475,4.03981020633857E-13,-1.47904511860479));
#11378=CARTESIAN_POINT('Ctrl Pts',(-1.99148666886423,-9.26359632821144E-5,
6.92095488139522));
#11379=CARTESIAN_POINT('Ctrl Pts',(-1.99162228600117,-0.327246622674157,
6.94175705391806));
#11380=CARTESIAN_POINT('Ctrl Pts',(-1.76063412440334,-1.31983678912773,
7.00488262885886));
#11381=CARTESIAN_POINT('Ctrl Pts',(-0.1964626520611,-2.34921239476192,7.11033160621761));
#11382=CARTESIAN_POINT('Ctrl Pts',(1.86665183793563,-1.43979420935406,7.23730181347151));
#11383=CARTESIAN_POINT('Ctrl Pts',(2.22229545319173,0.786638015914119,7.36427202072539));
#11384=CARTESIAN_POINT('Ctrl Pts',(0.54515251217721,2.29351372087127,7.49124222797928));
#11385=CARTESIAN_POINT('Ctrl Pts',(-1.49226254770249,1.74005184336971,7.61013651486923));
#11386=CARTESIAN_POINT('Ctrl Pts',(-1.99070390286835,0.534073603127432,
7.6867073993412));
#11387=CARTESIAN_POINT('Ctrl Pts',(-1.99559319474839,-0.00173033593146354,
7.72095488139522));
#11388=CARTESIAN_POINT('Ctrl Pts',(-1.995501255299,-0.00174979995018244,
7.07904511860477));
#11389=CARTESIAN_POINT('Ctrl Pts',(-1.99668912531657,-0.131264798487339,
7.08732246920644));
#11390=CARTESIAN_POINT('Ctrl Pts',(-1.92618348836682,-0.921968576958176,
7.13793892644944));
#11391=CARTESIAN_POINT('Ctrl Pts',(-0.870522872770069,-2.19111289741426,
7.23089449033379));
#11392=CARTESIAN_POINT('Ctrl Pts',(1.3687932043082,-1.91968512133389,7.3579118102578));
#11393=CARTESIAN_POINT('Ctrl Pts',(2.35519059073263,0.108917778877055,7.48492913018183));
#11394=CARTESIAN_POINT('Ctrl Pts',(1.18577488435873,2.03782328106611,7.61194645010582));
#11395=CARTESIAN_POINT('Ctrl Pts',(-1.06903451833457,2.10141642704157,7.73896377002986));
#11396=CARTESIAN_POINT('Ctrl Pts',(-1.96363940588376,0.797697806598223,
7.8279966595295));
#11397=CARTESIAN_POINT('Ctrl Pts',(-1.99764031162416,0.0691466988436851,
7.87469044238781));
#11398=CARTESIAN_POINT('Ctrl Pts',(-1.99717077118997,0.00115749627489461,
7.87904511860478));
#11399=CARTESIAN_POINT('Origin',(0.,0.,-1.47904511860479));
#11400=CARTESIAN_POINT('',(-1.99525355952187,0.00178111082825299,6.12095488139522));
#11401=CARTESIAN_POINT('',(-1.99147941923728,-6.71563141235731E-5,6.27904511860477));
#11402=CARTESIAN_POINT('',(-1.99475,4.03981020633857E-13,-1.47904511860479));
#11403=CARTESIAN_POINT('Ctrl Pts',(-1.99525355952187,0.00178111082825295,
6.12095488139522));
#11404=CARTESIAN_POINT('Ctrl Pts',(-1.99041683713606,-0.523003000897414,
6.15448330607696));
#11405=CARTESIAN_POINT('Ctrl Pts',(-1.50926405869879,-1.71807636877895,
6.23033513317666));
#11406=CARTESIAN_POINT('Ctrl Pts',(0.506218527102226,-2.3024203031107,6.3485103626943));
#11407=CARTESIAN_POINT('Ctrl Pts',(2.20864962127088,-0.824174313976057,
6.4754805699482));
#11408=CARTESIAN_POINT('Ctrl Pts',(1.8907763264874,1.40796354091743,6.60245077720207));
#11409=CARTESIAN_POINT('Ctrl Pts',(-0.156635087036384,2.35220362614869,
6.72942098445597));
#11410=CARTESIAN_POINT('Ctrl Pts',(-1.74880480475359,1.34263767884721,6.835589019187));
#11411=CARTESIAN_POINT('Ctrl Pts',(-1.99134636392355,0.338369904494061,
6.89943365150009));
#11412=CARTESIAN_POINT('Ctrl Pts',(-1.99148666886423,-9.26359632821144E-5,
6.92095488139522));
#11413=CARTESIAN_POINT('Ctrl Pts',(-1.99147941923728,-6.7156314123816E-5,
6.27904511860477));
#11414=CARTESIAN_POINT('Ctrl Pts',(-1.99157816546678,-0.32890987126841,
6.29995449602507));
#11415=CARTESIAN_POINT('Ctrl Pts',(-1.75884540947334,-1.32349005241169,
6.3632029800867));
#11416=CARTESIAN_POINT('Ctrl Pts',(-0.189682276366992,-2.35006519808776,
6.46879057078969));
#11417=CARTESIAN_POINT('Ctrl Pts',(1.87157814575952,-1.43386925678263,6.5958078907137));
#11418=CARTESIAN_POINT('Ctrl Pts',(2.21969794703782,0.794812446522514,6.72282521063772));
#11419=CARTESIAN_POINT('Ctrl Pts',(0.536027236282382,2.29596615898285,6.84984253056173));
#11420=CARTESIAN_POINT('Ctrl Pts',(-1.4965994031063,1.73464708792947,6.96858249988409));
#11421=CARTESIAN_POINT('Ctrl Pts',(-1.99061310440479,0.531211590227516,
7.0449833625651));
#11422=CARTESIAN_POINT('Ctrl Pts',(-1.995501255299,-0.00174979995018244,
7.07904511860477));
#11423=CARTESIAN_POINT('Origin',(0.,0.,-1.47904511860479));
#11424=CARTESIAN_POINT('',(-1.99730956637596,-0.00106064172337803,5.32095488139522));
#11425=CARTESIAN_POINT('',(-1.99525472473012,0.0017845551702237,5.47904511860478));
#11426=CARTESIAN_POINT('',(-1.99475,4.03981020633857E-13,-1.47904511860479));
#11427=CARTESIAN_POINT('Ctrl Pts',(-1.99730956637596,-0.00106064172337789,
5.32095488139522));
#11428=CARTESIAN_POINT('Ctrl Pts',(-1.99770497237211,-0.0624280686180993,
5.32488615581789));
#11429=CARTESIAN_POINT('Ctrl Pts',(-1.96730967016266,-0.784069391199876,
5.37114083265851));
#11430=CARTESIAN_POINT('Ctrl Pts',(-1.09058225712671,-2.08998248552431,
5.4597189119171));
#11431=CARTESIAN_POINT('Ctrl Pts',(1.16372401066593,-2.05015679311548,5.58668911917098));
#11432=CARTESIAN_POINT('Ctrl Pts',(2.35354422162328,-0.13500387483914,5.71365932642487));
#11433=CARTESIAN_POINT('Ctrl Pts',(1.39052150324245,1.903640301732,5.84062953367876));
#11434=CARTESIAN_POINT('Ctrl Pts',(-0.844444337704187,2.20097937515945,
5.96759974093265));
#11435=CARTESIAN_POINT('Ctrl Pts',(-1.92077276943005,0.938152829706547,
6.0610415235048));
#11436=CARTESIAN_POINT('Ctrl Pts',(-1.99652229988481,0.139439370134114,
6.11215990365899));
#11437=CARTESIAN_POINT('Ctrl Pts',(-1.99525355952187,0.00178111082825295,
6.12095488139522));
#11438=CARTESIAN_POINT('Ctrl Pts',(-1.99525472473012,0.0017845551702237,
5.47904511860478));
#11439=CARTESIAN_POINT('Ctrl Pts',(-1.99041023735962,-0.523201771333229,
5.51258652284371));
#11440=CARTESIAN_POINT('Ctrl Pts',(-1.50887731739964,-1.71873699628024,
5.58846703372397));
#11441=CARTESIAN_POINT('Ctrl Pts',(0.507837960106644,-2.30236539400368,
5.70668665124559));
#11442=CARTESIAN_POINT('Ctrl Pts',(2.20978656254498,-0.821966635105482,
5.83370397116961));
#11443=CARTESIAN_POINT('Ctrl Pts',(1.88901699407625,1.41081557877779,5.96072129109363));
#11444=CARTESIAN_POINT('Ctrl Pts',(-0.160855766453599,2.35221411092393,
6.08773861101763));
#11445=CARTESIAN_POINT('Ctrl Pts',(-1.75028149311093,1.3399904347984,6.19384655352136));
#11446=CARTESIAN_POINT('Ctrl Pts',(-1.99137821560422,0.336959154710372,
6.25761538938374));
#11447=CARTESIAN_POINT('Ctrl Pts',(-1.99147941923728,-6.7156314123816E-5,
6.27904511860477));
#11448=CARTESIAN_POINT('Origin',(0.,0.,-1.47904511860479));
#11449=CARTESIAN_POINT('',(-1.99208101634156,-0.00108597322356468,4.52095488139522));
#11450=CARTESIAN_POINT('',(-1.99734577058445,-0.00103987188155213,4.67904511860477));
#11451=CARTESIAN_POINT('',(-1.99475,4.03981020633857E-13,-1.47904511860479));
#11452=CARTESIAN_POINT('Ctrl Pts',(-1.99208101634156,-0.00108597322356466,
4.52095488139522));
#11453=CARTESIAN_POINT('Ctrl Pts',(-1.99337623546945,-0.262862144141555,
4.53761240797678));
#11454=CARTESIAN_POINT('Ctrl Pts',(-1.82368896996318,-1.18814603783072,
4.5965933369763));
#11455=CARTESIAN_POINT('Ctrl Pts',(-0.424576623578355,-2.31886419181245,
4.69789766839378));
#11456=CARTESIAN_POINT('Ctrl Pts',(1.71737702962559,-1.61493423626845,4.82486787564767));
#11457=CARTESIAN_POINT('Ctrl Pts',(2.28840502897144,0.566214511237573,4.95183808290156));
#11458=CARTESIAN_POINT('Ctrl Pts',(0.766174469238656,2.22943336568846,5.07880829015544));
#11459=CARTESIAN_POINT('Ctrl Pts',(-1.3880630675663,1.86498122595536,5.20184722298667));
#11460=CARTESIAN_POINT('Ctrl Pts',(-1.99344810162381,0.59824275325246,5.28256275339993));
#11461=CARTESIAN_POINT('Ctrl Pts',(-1.99730956637596,-0.00106064172337789,
5.32095488139522));
#11462=CARTESIAN_POINT('Ctrl Pts',(-1.99734577058445,-0.00103987188155228,
4.67904511860477));
#11463=CARTESIAN_POINT('Ctrl Pts',(-1.99772514422821,-0.0608910454152072,
4.682879443021));
#11464=CARTESIAN_POINT('Ctrl Pts',(-1.96813705138938,-0.781246353584555,
4.72905287407857));
#11465=CARTESIAN_POINT('Ctrl Pts',(-1.09471794236404,-2.08815191686271,
4.81756541177748));
#11466=CARTESIAN_POINT('Ctrl Pts',(1.16070165538423,-2.05220794960434,4.94458273170149));
#11467=CARTESIAN_POINT('Ctrl Pts',(2.35367822395426,-0.13778468461515,5.07160005162551));
#11468=CARTESIAN_POINT('Ctrl Pts',(1.3922260378406,1.90275917046527,5.19861737154953));
#11469=CARTESIAN_POINT('Ctrl Pts',(-0.843593977493136,2.20162099426043,
5.32563469147353));
#11470=CARTESIAN_POINT('Ctrl Pts',(-1.9207312990425,0.938483163076661,5.41911060715863));
#11471=CARTESIAN_POINT('Ctrl Pts',(-1.99652540373551,0.13948521412321,5.47024741620237));
#11472=CARTESIAN_POINT('Ctrl Pts',(-1.99525472473012,0.0017845551702237,
5.47904511860478));
#11473=CARTESIAN_POINT('Origin',(0.,0.,-1.47904511860479));
#11474=CARTESIAN_POINT('',(-1.99335826076814,0.00167831318840674,3.72095488139522));
#11475=CARTESIAN_POINT('',(-1.99212878278616,-0.00112883914168277,3.87904511860477));
#11476=CARTESIAN_POINT('',(-1.99475,4.03981020633857E-13,-1.47904511860479));
#11477=CARTESIAN_POINT('Ctrl Pts',(-1.99335826076814,0.00167831318840671,
3.72095488139522));
#11478=CARTESIAN_POINT('Ctrl Pts',(-1.98967611077165,-0.459349191220618,
3.75033866013568));
#11479=CARTESIAN_POINT('Ctrl Pts',(-1.60123477712065,-1.59002462297684,
3.82204584129409));
#11480=CARTESIAN_POINT('Ctrl Pts',(0.279318860454586,-2.34080700264011,
3.93607642487046));
#11481=CARTESIAN_POINT('Ctrl Pts',(2.11776876365419,-1.03559254199705,4.06304663212436));
#11482=CARTESIAN_POINT('Ctrl Pts',(2.01904516192129,1.21690307069604,4.19001683937824));
#11483=CARTESIAN_POINT('Ctrl Pts',(0.0734528840375746,2.35626847434518,
4.31698704663213));
#11484=CARTESIAN_POINT('Ctrl Pts',(-1.67526686991482,1.47358648511445,4.42729972730445));
#11485=CARTESIAN_POINT('Ctrl Pts',(-1.99008534590667,0.402258104711046,
4.49528900555882));
#11486=CARTESIAN_POINT('Ctrl Pts',(-1.99208101634156,-0.00108597322356466,
4.52095488139522));
#11487=CARTESIAN_POINT('Ctrl Pts',(-1.99212878278616,-0.00112883914168287,
3.87904511860477));
#11488=CARTESIAN_POINT('Ctrl Pts',(-1.99346081133728,-0.25988492631503,
3.89551146983963));
#11489=CARTESIAN_POINT('Ctrl Pts',(-1.82636130136228,-1.1823140336403,3.95431692771583));
#11490=CARTESIAN_POINT('Ctrl Pts',(-0.434214441284883,-2.31737860959731,
4.05546149223338));
#11491=CARTESIAN_POINT('Ctrl Pts',(1.71149948445725,-1.62159036625522,4.18247881215739));
#11492=CARTESIAN_POINT('Ctrl Pts',(2.29060007052677,0.558513310613506,4.30949613208142));
#11493=CARTESIAN_POINT('Ctrl Pts',(0.77301020537091,2.22738434573485,4.43651345200542));
#11494=CARTESIAN_POINT('Ctrl Pts',(-1.38497920298751,1.86859714880058,4.55969644751322));
#11495=CARTESIAN_POINT('Ctrl Pts',(-1.99353605133559,0.599993361789769,
4.64054033637966));
#11496=CARTESIAN_POINT('Ctrl Pts',(-1.99734577058445,-0.00103987188155228,
4.67904511860477));
#11497=CARTESIAN_POINT('Origin',(0.,0.,-1.47904511860479));
#11498=CARTESIAN_POINT('',(-1.99801366137741,6.20784135630644E-5,2.92095488139522));
#11499=CARTESIAN_POINT('',(-1.99323413496252,0.00164975376670227,3.07904511860477));
#11500=CARTESIAN_POINT('',(-1.99475,4.03981020633857E-13,-1.47904511860479));
#11501=CARTESIAN_POINT('Ctrl Pts',(-1.99801366137741,6.20784135629766E-5,
2.92095488139522));
#11502=CARTESIAN_POINT('Ctrl Pts',(-1.9977139479877,-0.656661905859173,
2.96306491229457));
#11503=CARTESIAN_POINT('Ctrl Pts',(-1.28538422970207,-1.97399479890882,
3.04749834561188));
#11504=CARTESIAN_POINT('Ctrl Pts',(0.958287513109827,-2.15385270943036,
3.17425518134715));
#11505=CARTESIAN_POINT('Ctrl Pts',(2.32916765789381,-0.363833025997572,
3.30122538860104));
#11506=CARTESIAN_POINT('Ctrl Pts',(1.56950269631471,1.75899338684286,3.42819559585493));
#11507=CARTESIAN_POINT('Ctrl Pts',(-0.6258237459619,2.27282667370784,3.55516580310881));
#11508=CARTESIAN_POINT('Ctrl Pts',(-1.87312534234062,1.06986828966388,3.65275223162224));
#11509=CARTESIAN_POINT('Ctrl Pts',(-1.99497975525663,0.204699254256833,
3.70801525771771));
#11510=CARTESIAN_POINT('Ctrl Pts',(-1.99335826076814,0.00167831318840671,
3.72095488139522));
#11511=CARTESIAN_POINT('Ctrl Pts',(-1.99323413496252,0.00164975376670215,
3.07904511860477));
#11512=CARTESIAN_POINT('Ctrl Pts',(-1.98966787406762,-0.454971437589277,
3.10814349665827));
#11513=CARTESIAN_POINT('Ctrl Pts',(-1.60712975765151,-1.5813915076858,3.1795809813531));
#11514=CARTESIAN_POINT('Ctrl Pts',(0.264471544354857,-2.34282748059378,
3.29335757268928));
#11515=CARTESIAN_POINT('Ctrl Pts',(2.11179724612446,-1.04837884014621,3.42037489261329));
#11516=CARTESIAN_POINT('Ctrl Pts',(2.02609885609852,1.2056986466197,3.54739221253732));
#11517=CARTESIAN_POINT('Ctrl Pts',(0.0858200094412126,2.35614531115273,
3.67440953246132));
#11518=CARTESIAN_POINT('Ctrl Pts',(-1.67129494903997,1.48035260045669,3.78496050115049));
#11519=CARTESIAN_POINT('Ctrl Pts',(-1.99003583284199,0.405441678994632,
3.8531723631983));
#11520=CARTESIAN_POINT('Ctrl Pts',(-1.99212878278616,-0.00112883914168287,
3.87904511860477));
#11521=CARTESIAN_POINT('Origin',(0.,0.,-1.47904511860479));
#11522=CARTESIAN_POINT('',(-1.99353828631959,-0.00171873314672716,2.12095488139522));
#11523=CARTESIAN_POINT('',(-1.99800195695475,0.000177068703322431,2.27904511860477));
#11524=CARTESIAN_POINT('',(-1.99475,4.03981020633857E-13,-1.47904511860479));
#11525=CARTESIAN_POINT('Ctrl Pts',(-1.99353828631959,-0.00171873314672709,
2.12095488139522));
#11526=CARTESIAN_POINT('Ctrl Pts',(-1.99515465902021,-0.197999298554213,
2.1334677620355));
#11527=CARTESIAN_POINT('Ctrl Pts',(-1.87838664997211,-1.05629559439167,
2.18830404509374));
#11528=CARTESIAN_POINT('Ctrl Pts',(-0.648644751766769,-2.26641924187756,
2.28546373056995));
#11529=CARTESIAN_POINT('Ctrl Pts',(1.55173715555782,-1.77468541835342,2.41243393782384));
#11530=CARTESIAN_POINT('Ctrl Pts',(2.33270816248269,0.340395505542482,2.53940414507772));
#11531=CARTESIAN_POINT('Ctrl Pts',(0.979895470300759,2.14410850487368,2.66637435233161));
#11532=CARTESIAN_POINT('Ctrl Pts',(-1.2692509317393,1.98655443822406,2.7933445595855));
#11533=CARTESIAN_POINT('Ctrl Pts',(-1.99650109561173,0.666767500964708,
2.87820473594003));
#11534=CARTESIAN_POINT('Ctrl Pts',(-1.9980151800251,0.00338969871783043,
2.9207415098766));
#11535=CARTESIAN_POINT('Ctrl Pts',(-1.99801366137741,6.20784135629766E-5,
2.92095488139522));
#11536=CARTESIAN_POINT('Ctrl Pts',(-1.99800195695475,0.000177068703322262,
2.27904511860477));
#11537=CARTESIAN_POINT('Ctrl Pts',(-1.9971755937525,-0.650636966490359,
2.3207755234769));
#11538=CARTESIAN_POINT('Ctrl Pts',(-1.29615928203765,-1.96328542074049,
2.40484503499037));
#11539=CARTESIAN_POINT('Ctrl Pts',(0.939901322271841,-2.16226069656491,
2.53125365314518));
#11540=CARTESIAN_POINT('Ctrl Pts',(2.32639490702415,-0.382978510636179,
2.6582709730692));
#11541=CARTESIAN_POINT('Ctrl Pts',(1.58343339573353,1.74686132178264,2.78528829299322));
#11542=CARTESIAN_POINT('Ctrl Pts',(-0.608916736747748,2.27771951988605,
2.91230561291723));
#11543=CARTESIAN_POINT('Ctrl Pts',(-1.8693401495715,1.07969268184623,3.01022455478775));
#11544=CARTESIAN_POINT('Ctrl Pts',(-1.99485690213174,0.209427563618705,
3.06580439001693));
#11545=CARTESIAN_POINT('Ctrl Pts',(-1.99323413496252,0.00164975376670215,
3.07904511860477));
#11546=CARTESIAN_POINT('Origin',(0.,0.,-1.47904511860479));
#11547=CARTESIAN_POINT('',(-1.99197487574581,0.000997555507514769,1.32095488139522));
#11548=CARTESIAN_POINT('',(-1.99375138711093,-0.00176081023319702,1.47904511860477));
#11549=CARTESIAN_POINT('',(-1.99475,4.03981020633857E-13,-1.47904511860479));
#11550=CARTESIAN_POINT('Ctrl Pts',(-1.99197487574581,0.000997555507514826,
1.32095488139522));
#11551=CARTESIAN_POINT('Ctrl Pts',(-1.99018227073014,-0.395693898889233,
1.34619401419439));
#11552=CARTESIAN_POINT('Ctrl Pts',(-1.68326915044115,-1.46015401124514,
1.41375654941153));
#11553=CARTESIAN_POINT('Ctrl Pts',(0.0497579841286025,-2.35688535243524,
1.52364248704663));
#11554=CARTESIAN_POINT('Ctrl Pts',(2.00670723621032,-1.23714384781738,1.65061269430052));
#11555=CARTESIAN_POINT('Ctrl Pts',(2.1280744337024,1.01424731308453,1.77758290155441));
#11556=CARTESIAN_POINT('Ctrl Pts',(0.302840850211159,2.33787982927957,1.90455310880829));
#11557=CARTESIAN_POINT('Ctrl Pts',(-1.59223214373163,1.60330557312612,2.0190104354219));
#11558=CARTESIAN_POINT('Ctrl Pts',(-1.98968746131953,0.465897496706805,
2.09114435961754));
#11559=CARTESIAN_POINT('Ctrl Pts',(-1.99353828631959,-0.00171873314672709,
2.12095488139522));
#11560=CARTESIAN_POINT('Ctrl Pts',(-1.99375138711093,-0.00176081023319709,
1.47904511860477));
#11561=CARTESIAN_POINT('Ctrl Pts',(-1.99535436761224,-0.190310974989928,
1.4910684436542));
#11562=CARTESIAN_POINT('Ctrl Pts',(-1.88430048103082,-1.04097352315297,
1.54543087534496));
#11563=CARTESIAN_POINT('Ctrl Pts',(-0.673992169187479,-2.25931816777247,
1.64213241367707));
#11564=CARTESIAN_POINT('Ctrl Pts',(1.53268116536722,-1.79155650545778,1.76914973360108));
#11565=CARTESIAN_POINT('Ctrl Pts',(2.33642193463667,0.316098985050819,1.8961670535251));
#11566=CARTESIAN_POINT('Ctrl Pts',(1.00152929412067,2.13441435022671,2.02318437344912));
#11567=CARTESIAN_POINT('Ctrl Pts',(-1.25010860812744,1.99900333994266,2.15020169337313));
#11568=CARTESIAN_POINT('Ctrl Pts',(-1.9936531346221,0.679459076978294,2.23548860842502));
#11569=CARTESIAN_POINT('Ctrl Pts',(-1.99801401072573,0.0096701866316292,
2.27843641683556));
#11570=CARTESIAN_POINT('Ctrl Pts',(-1.99800195695475,0.000177068703322262,
2.27904511860477));
#11571=CARTESIAN_POINT('Origin',(0.,0.,-1.47904511860479));
#11572=CARTESIAN_POINT('',(-1.99714087507904,0.0012938138350061,0.52095488139522));
#11573=CARTESIAN_POINT('',(-1.99183435874083,0.000880024085723324,0.679045118604771));
#11574=CARTESIAN_POINT('',(-1.99475,4.03981020633857E-13,-1.47904511860479));
#11575=CARTESIAN_POINT('Ctrl Pts',(-1.99714087507904,0.00129381383500625,
0.52095488139522));
#11576=CARTESIAN_POINT('Ctrl Pts',(-1.99304294628744,-0.591424958441748,
0.55892026635329));
#11577=CARTESIAN_POINT('Ctrl Pts',(-1.39932480947917,-1.85249014707753,
0.639209053729322));
#11578=CARTESIAN_POINT('Ctrl Pts',(0.743740789408913,-2.23690209703098,
0.761821243523316));
#11579=CARTESIAN_POINT('Ctrl Pts',(2.28258498544192,-0.589259358513722,
0.888791450777202));
#11580=CARTESIAN_POINT('Ctrl Pts',(1.73353383587625,1.59761854395386,1.01576165803109));
#11581=CARTESIAN_POINT('Ctrl Pts',(-0.401242712543095,2.32299828124824,
1.14273186528497));
#11582=CARTESIAN_POINT('Ctrl Pts',(-1.8175909465059,1.20172296388846,1.24446293973969));
#11583=CARTESIAN_POINT('Ctrl Pts',(-1.99318828302297,0.269516439112097,
1.30387061177643));
#11584=CARTESIAN_POINT('Ctrl Pts',(-1.99197487574581,0.000997555507514826,
1.32095488139522));
#11585=CARTESIAN_POINT('Ctrl Pts',(-1.99183435874083,0.00088002408572329,
0.679045118604771));
#11586=CARTESIAN_POINT('Ctrl Pts',(-1.9903216505241,-0.386707492335019,
0.703700470472832));
#11587=CARTESIAN_POINT('Ctrl Pts',(-1.69400858548477,-1.44203090012767,
0.770694928982232));
#11588=CARTESIAN_POINT('Ctrl Pts',(0.0182153715595747,-2.3576204698764,
0.88002849413297));
#11589=CARTESIAN_POINT('Ctrl Pts',(1.9906822371454,-1.26332101110348,1.00704581405699));
#11590=CARTESIAN_POINT('Ctrl Pts',(2.14099816144828,0.987384922727256,1.134063133981));
#11591=CARTESIAN_POINT('Ctrl Pts',(0.331555254300241,2.33427609427238,1.26108045390502));
#11592=CARTESIAN_POINT('Ctrl Pts',(-1.58136473144127,1.61926551238329,1.37607444877961));
#11593=CARTESIAN_POINT('Ctrl Pts',(-1.98970960943512,0.473652238186084,
1.44872933701286));
#11594=CARTESIAN_POINT('Ctrl Pts',(-1.99375138711093,-0.00176081023319709,
1.47904511860477));
#11595=CARTESIAN_POINT('Origin',(0.,0.,24.5));
#11596=CARTESIAN_POINT('',(-2.39498807124001,0.000954274581741462,24.1082520126806));
#11597=CARTESIAN_POINT('Ctrl Pts',(-0.4076525627588,1.95265126189399,24.50525));
#11598=CARTESIAN_POINT('Ctrl Pts',(-0.337699253117069,1.97023462451848,
24.5023335797628));
#11599=CARTESIAN_POINT('Ctrl Pts',(-0.266932744787586,1.98367656997238,
24.4994292108287));
#11600=CARTESIAN_POINT('Ctrl Pts',(-0.195667102851186,1.99314829867957,
24.4965325858746));
#11601=CARTESIAN_POINT('Ctrl Pts',(-0.12076554741437,2.00310326707061,24.4934881775358));
#11602=CARTESIAN_POINT('Ctrl Pts',(-0.0453118238453052,2.00867281937902,
24.4904523235171));
#11603=CARTESIAN_POINT('Ctrl Pts',(0.0303460012294243,2.00999925550285,
24.4874200230199));
#11604=CARTESIAN_POINT('Ctrl Pts',(0.0650184974572605,2.01060713514325,
24.4860303792198));
#11605=CARTESIAN_POINT('Ctrl Pts',(0.0997340039424784,2.01032309156194,
24.4846414817334));
#11606=CARTESIAN_POINT('Ctrl Pts',(0.134459334270958,2.00915694524383,24.4832528492418));
#11607=CARTESIAN_POINT('Ctrl Pts',(0.147933596547958,2.00870445246132,24.4827140264798));
#11608=CARTESIAN_POINT('Ctrl Pts',(0.161409337218446,2.00811912255674,24.482175243616));
#11609=CARTESIAN_POINT('Ctrl Pts',(0.174884610787376,2.00740143335556,24.4816364725311));
#11610=CARTESIAN_POINT('Ctrl Pts',(0.189332023983714,2.00663196827694,24.4810588331649));
#11611=CARTESIAN_POINT('Ctrl Pts',(0.203769295159425,2.00571085084408,24.4804815912802));
#11612=CARTESIAN_POINT('Ctrl Pts',(0.218191263309744,2.00463947026819,24.4799048229404));
#11613=CARTESIAN_POINT('Ctrl Pts',(0.293616304880072,1.99903628742713,24.4768883985829));
#11614=CARTESIAN_POINT('Ctrl Pts',(0.368646680368959,1.9893261617957,24.4738839495771));
#11615=CARTESIAN_POINT('Ctrl Pts',(0.44294146325047,1.97565502596793,24.4708866901775));
#11616=CARTESIAN_POINT('Ctrl Pts',(0.517780644499032,1.96188371427677,24.4678674682248));
#11617=CARTESIAN_POINT('Ctrl Pts',(0.591874413926822,1.94409297499423,24.4648555416287));
#11618=CARTESIAN_POINT('Ctrl Pts',(0.664872416764246,1.92237927515082,24.4618460186679));
#11619=CARTESIAN_POINT('Ctrl Pts',(0.693612873435508,1.91383025154381,24.4606611223571));
#11620=CARTESIAN_POINT('Ctrl Pts',(0.722183370632896,1.90467256243273,24.4594765986387));
#11621=CARTESIAN_POINT('Ctrl Pts',(0.750561917361623,1.89490995728419,24.4582921489677));
#11622=CARTESIAN_POINT('Ctrl Pts',(0.762696377885477,1.8907355382092,24.4577856868887));
#11623=CARTESIAN_POINT('Ctrl Pts',(0.774794416283802,1.88645088041849,24.4572792924806));
#11624=CARTESIAN_POINT('Ctrl Pts',(0.786842875051873,1.88206068413371,24.4567734253696));
#11625=CARTESIAN_POINT('Ctrl Pts',(0.859169502120084,1.85570643455227,24.4537367164772));
#11626=CARTESIAN_POINT('Ctrl Pts',(0.929822756867472,1.82551496441967,24.4507143015495));
#11627=CARTESIAN_POINT('Ctrl Pts',(0.998456357996127,1.79162107203564,24.4477013393046));
#11628=CARTESIAN_POINT('Ctrl Pts',(1.06668990494531,1.75792474167785,24.4447059391301));
#11629=CARTESIAN_POINT('Ctrl Pts',(1.13292826279404,1.7205687402294,24.4417198817631));
#11630=CARTESIAN_POINT('Ctrl Pts',(1.19681843662805,1.67963606311431,24.4387384100862));
#11631=CARTESIAN_POINT('Ctrl Pts',(1.24693212411197,1.64752960188985,24.4363998260615));
#11632=CARTESIAN_POINT('Ctrl Pts',(1.29560102816851,1.61322162205542,24.4340640633369));
#11633=CARTESIAN_POINT('Ctrl Pts',(1.34264328707622,1.57673230368136,24.4317288262356));
#11634=CARTESIAN_POINT('Ctrl Pts',(1.36662257672075,1.55813226289803,24.4305384640349));
#11635=CARTESIAN_POINT('Ctrl Pts',(1.39017901233764,1.53896516305314,24.429348238409));
#11636=CARTESIAN_POINT('Ctrl Pts',(1.41328706967152,1.51923201753369,24.4281578453009));
#11637=CARTESIAN_POINT('Ctrl Pts',(1.42306877589838,1.51087892105247,24.4276539485212));
#11638=CARTESIAN_POINT('Ctrl Pts',(1.4327701259467,1.50242438406759,24.427150021731));
#11639=CARTESIAN_POINT('Ctrl Pts',(1.44238912178932,1.49386842480447,24.4266460418679));
#11640=CARTESIAN_POINT('Ctrl Pts',(1.45230713194123,1.48504649658875,24.4261263953808));
#11641=CARTESIAN_POINT('Ctrl Pts',(1.46213208274873,1.47612156735597,24.4256069790412));
#11642=CARTESIAN_POINT('Ctrl Pts',(1.47185655624505,1.46709927890788,24.425088065848));
#11643=CARTESIAN_POINT('Ctrl Pts',(1.47412964601262,1.46499032446843,24.4249667702046));
#11644=CARTESIAN_POINT('Ctrl Pts',(1.47639734253898,1.4628759644146,24.4248454969878));
#11645=CARTESIAN_POINT('Ctrl Pts',(1.47865962347614,1.46075620613088,24.4247242458888));
#11646=CARTESIAN_POINT('Ctrl Pts',(1.53215475670349,1.41063124157184,24.4218570760403));
#11647=CARTESIAN_POINT('Ctrl Pts',(1.5826240221007,1.35749162418093,24.4190022736264));
#11648=CARTESIAN_POINT('Ctrl Pts',(1.6300398879693,1.30171088713118,24.4161557575599));
#11649=CARTESIAN_POINT('Ctrl Pts',(1.68078212606171,1.24201695581728,24.4131095494325));
#11650=CARTESIAN_POINT('Ctrl Pts',(1.72802829283498,1.17929792584938,24.4100728310601));
#11651=CARTESIAN_POINT('Ctrl Pts',(1.77170626798428,1.11396230694137,24.4070406007886));
#11652=CARTESIAN_POINT('Ctrl Pts',(1.80992449623993,1.05679364039686,24.404387399301));
#11653=CARTESIAN_POINT('Ctrl Pts',(1.84541040747536,0.997620449183277,24.4017376340156));
#11654=CARTESIAN_POINT('Ctrl Pts',(1.87808726172145,0.936693707274591,24.3990879542148));
#11655=CARTESIAN_POINT('Ctrl Pts',(1.88890052248433,0.916532135333474,24.3982111354608));
#11656=CARTESIAN_POINT('Ctrl Pts',(1.89940594781383,0.896178406839887,24.3973343260678));
#11657=CARTESIAN_POINT('Ctrl Pts',(1.90960005205868,0.875641268784333,24.3964574046166));
#11658=CARTESIAN_POINT('Ctrl Pts',(1.91547518951183,0.863805161749081,24.3959520111129));
#11659=CARTESIAN_POINT('Ctrl Pts',(1.92124762238796,0.851906634807171,24.3954465171147));
#11660=CARTESIAN_POINT('Ctrl Pts',(1.92691441011101,0.839952030543744,24.3949410974597));
#11661=CARTESIAN_POINT('Ctrl Pts',(1.96031903083694,0.769481943985819,24.3919617460688));
#11662=CARTESIAN_POINT('Ctrl Pts',(1.98992816786267,0.697337983571344,24.3889964420272));
#11663=CARTESIAN_POINT('Ctrl Pts',(2.0156863162126,0.623908778644958,24.3860406309664));
#11664=CARTESIAN_POINT('Ctrl Pts',(2.04178778214467,0.549500872270339,24.3830454233662));
#11665=CARTESIAN_POINT('Ctrl Pts',(2.06393536696727,0.473772310543712,24.3800599634878));
#11666=CARTESIAN_POINT('Ctrl Pts',(2.08202723354027,0.397097517940733,24.3770795124158));
#11667=CARTESIAN_POINT('Ctrl Pts',(2.09876155552511,0.326176109010256,24.3743227030122));
#11668=CARTESIAN_POINT('Ctrl Pts',(2.11202575380227,0.2544442193714,24.3715701789334));
#11669=CARTESIAN_POINT('Ctrl Pts',(2.12170133232151,0.182186358988051,24.3688181899904));
#11670=CARTESIAN_POINT('Ctrl Pts',(2.12533324744348,0.155062976620213,24.3677851778312));
#11671=CARTESIAN_POINT('Ctrl Pts',(2.12845912993511,0.127865424475548,24.3667522410737));
#11672=CARTESIAN_POINT('Ctrl Pts',(2.13107126614788,0.100608649754695,24.3657191813693));
#11673=CARTESIAN_POINT('Ctrl Pts',(2.1325759123382,0.0849081659730918,24.3651241169385));
#11674=CARTESIAN_POINT('Ctrl Pts',(2.13391008218326,0.0691880322062874,
24.3645290117138));
#11675=CARTESIAN_POINT('Ctrl Pts',(2.13507217604384,0.0534511129096754,
24.363933827786));
#11676=CARTESIAN_POINT('Ctrl Pts',(2.1358949975935,0.0423085737726864,24.363512407298));
#11677=CARTESIAN_POINT('Ctrl Pts',(2.13663134775102,0.0311597107005095,
24.3630910265538));
#11678=CARTESIAN_POINT('Ctrl Pts',(2.13728034324863,0.0200145848943864,
24.3626700130043));
#11679=CARTESIAN_POINT('Ctrl Pts',(2.14206066436502,-0.0620773254988428,
24.3595689437853));
#11680=CARTESIAN_POINT('Ctrl Pts',(2.14211688472276,-0.144103698334206,
24.3564825474227));
#11681=CARTESIAN_POINT('Ctrl Pts',(2.13733830774908,-0.22565130659055,24.3534056763928));
#11682=CARTESIAN_POINT('Ctrl Pts',(2.13255973077539,-0.307198914846895,
24.3503288053629));
#11683=CARTESIAN_POINT('Ctrl Pts',(2.1229467821906,-0.38826895977034,24.3472614596657));
#11684=CARTESIAN_POINT('Ctrl Pts',(2.10832870393275,-0.468456219886853,
24.3441984917776));
#11685=CARTESIAN_POINT('Ctrl Pts',(2.09441595298606,-0.544774417082047,
24.3412833131451));
#11686=CARTESIAN_POINT('Ctrl Pts',(2.07596888070456,-0.620293811415302,
24.3383721000521));
#11687=CARTESIAN_POINT('Ctrl Pts',(2.05323813750186,-0.694760696394361,
24.3354604147107));
#11688=CARTESIAN_POINT('Ctrl Pts',(2.04535336849461,-0.720591536218365,
24.3344504184191));
#11689=CARTESIAN_POINT('Ctrl Pts',(2.0369527279183,-0.746295609744288,24.3334403653049));
#11690=CARTESIAN_POINT('Ctrl Pts',(2.02804532218294,-0.771861842203744,
24.3324300701461));
#11691=CARTESIAN_POINT('Ctrl Pts',(2.02399375543204,-0.783490738479032,
24.3319705336217));
#11692=CARTESIAN_POINT('Ctrl Pts',(2.0198389575898,-0.795086319358417,24.3315111358951));
#11693=CARTESIAN_POINT('Ctrl Pts',(2.01558473198086,-0.806640549867355,
24.3310521410104));
#11694=CARTESIAN_POINT('Ctrl Pts',(1.98850593400829,-0.880184997774034,
24.3281305682272));
#11695=CARTESIAN_POINT('Ctrl Pts',(1.95737281308123,-0.952142606058721,
24.3252218392429));
#11696=CARTESIAN_POINT('Ctrl Pts',(1.92249757285567,-1.02227201743633,24.3223216485138));
#11697=CARTESIAN_POINT('Ctrl Pts',(1.88695067262014,-1.09375204664024,24.3193656031979));
#11698=CARTESIAN_POINT('Ctrl Pts',(1.84751568956125,-1.16333359394599,24.3164184281795));
#11699=CARTESIAN_POINT('Ctrl Pts',(1.80446912728237,-1.23074844857256,24.3134755643329));
#11700=CARTESIAN_POINT('Ctrl Pts',(1.76126023236668,-1.29841753095931,24.3105216026698));
#11701=CARTESIAN_POINT('Ctrl Pts',(1.71441188113122,-1.36390438374644,24.3075719847555));
#11702=CARTESIAN_POINT('Ctrl Pts',(1.66415769946571,-1.42691271211585,24.3046220996905));
#11703=CARTESIAN_POINT('Ctrl Pts',(1.64674427416882,-1.44874553841568,24.3035999438916));
#11704=CARTESIAN_POINT('Ctrl Pts',(1.62892155760558,-1.47028049720965,24.3025777560166));
#11705=CARTESIAN_POINT('Ctrl Pts',(1.61069818584296,-1.49150427719069,24.3015553442334));
#11706=CARTESIAN_POINT('Ctrl Pts',(1.60049069069606,-1.5033923972366,24.3009826585937));
#11707=CARTESIAN_POINT('Ctrl Pts',(1.59015563953053,-1.51518477143648,24.3004098063768));
#11708=CARTESIAN_POINT('Ctrl Pts',(1.57971072759172,-1.52686130763077,24.2998376300385));
#11709=CARTESIAN_POINT('Ctrl Pts',(1.5241196874745,-1.58900743158191,24.2967923312403));
#11710=CARTESIAN_POINT('Ctrl Pts',(1.46532985685416,-1.6479828288116,24.2937609986882));
#11711=CARTESIAN_POINT('Ctrl Pts',(1.40364751528756,-1.70349947958641,24.290738760932));
#11712=CARTESIAN_POINT('Ctrl Pts',(1.34352976106267,-1.75760793724063,24.2877931829591));
#11713=CARTESIAN_POINT('Ctrl Pts',(1.28066352510377,-1.80843159489564,24.2848562442503));
#11714=CARTESIAN_POINT('Ctrl Pts',(1.21529029695891,-1.85567350385066,24.2819234347283));
#11715=CARTESIAN_POINT('Ctrl Pts',(1.151018429448,-1.90211951545945,24.2790400350497));
#11716=CARTESIAN_POINT('Ctrl Pts',(1.08432265151975,-1.94510411645588,24.2761606265988));
#11717=CARTESIAN_POINT('Ctrl Pts',(1.01540230218933,-1.98430534234295,24.2732809234275));
#11718=CARTESIAN_POINT('Ctrl Pts',(0.991413070221145,-1.99795018469181,
24.2722785798809));
#11719=CARTESIAN_POINT('Ctrl Pts',(0.967154098038469,-2.01113625193634,
24.2712762006278));
#11720=CARTESIAN_POINT('Ctrl Pts',(0.942633141242275,-2.02384857830255,
24.2702736049284));
#11721=CARTESIAN_POINT('Ctrl Pts',(0.927689229189158,-2.03159590597765,
24.2696625887238));
#11722=CARTESIAN_POINT('Ctrl Pts',(0.91264425065672,-2.03916896131714,24.269051342741));
#11723=CARTESIAN_POINT('Ctrl Pts',(0.89752523548915,-2.04655226315939,24.2684408416994));
#11724=CARTESIAN_POINT('Ctrl Pts',(0.858076293954018,-2.06581697316084,
24.2668479059406));
#11725=CARTESIAN_POINT('Ctrl Pts',(0.818092741329694,-2.08380677668847,
24.2652587702448));
#11726=CARTESIAN_POINT('Ctrl Pts',(0.777614563358231,-2.10047761443662,
24.2636727376664));
#11727=CARTESIAN_POINT('Ctrl Pts',(0.705244379734806,-2.13028309604305,
24.2608370994365));
#11728=CARTESIAN_POINT('Ctrl Pts',(0.631294604316736,-2.15587544510049,
24.2580113803836));
#11729=CARTESIAN_POINT('Ctrl Pts',(0.556119155090156,-2.17737629254266,
24.2551915974639));
#11730=CARTESIAN_POINT('Ctrl Pts',(0.474948448561465,-2.20059183692319,
24.2521469362853));
#11731=CARTESIAN_POINT('Ctrl Pts',(0.392348029526542,-2.21903791275238,
24.24910919581));
#11732=CARTESIAN_POINT('Ctrl Pts',(0.308737702730448,-2.23280813351095,
24.2460733620308));
#11733=CARTESIAN_POINT('Ctrl Pts',(0.270500156739416,-2.23910567437389,
24.2446849828891));
#11734=CARTESIAN_POINT('Ctrl Pts',(0.232051123492098,-2.2444244113041,24.243297002535));
#11735=CARTESIAN_POINT('Ctrl Pts',(0.193429913054559,-2.24876906028139,
24.2419089413729));
#11736=CARTESIAN_POINT('Ctrl Pts',(0.161572159376237,-2.25235286191187,
24.2407639614488));
#11737=CARTESIAN_POINT('Ctrl Pts',(0.129597238881117,-2.25527382408218,
24.2396189265412));
#11738=CARTESIAN_POINT('Ctrl Pts',(0.0975271844407983,-2.25753324335174,
24.2384735674698));
#11739=CARTESIAN_POINT('Ctrl Pts',(0.0844330795511259,-2.25845575731131,
24.2380059208731));
#11740=CARTESIAN_POINT('Ctrl Pts',(0.0713229194369418,-2.25926790250605,
24.237538213561));
#11741=CARTESIAN_POINT('Ctrl Pts',(0.0582132985134477,-2.25996914699854,
24.2370709640795));
#11742=CARTESIAN_POINT('Ctrl Pts',(-0.023786791539092,-2.26435539980234,
24.2341483395591));
#11743=CARTESIAN_POINT('Ctrl Pts',(-0.105909169640656,-2.26441794064745,
24.231238450421));
#11744=CARTESIAN_POINT('Ctrl Pts',(-0.187776168973137,-2.26027172560533,
24.2283369940797));
#11745=CARTESIAN_POINT('Ctrl Pts',(-0.270727942589467,-2.25607057136317,
24.2253970921468));
#11746=CARTESIAN_POINT('Ctrl Pts',(-0.353418510685726,-2.24754840827001,
24.2224658479679));
#11747=CARTESIAN_POINT('Ctrl Pts',(-0.435464876948505,-2.23477219179204,
24.2195387856475));
#11748=CARTESIAN_POINT('Ctrl Pts',(-0.521020187243656,-2.22144956441731,
24.2164865392595));
#11749=CARTESIAN_POINT('Ctrl Pts',(-0.605876258185628,-2.20350155640051,
24.2134388400769));
#11750=CARTESIAN_POINT('Ctrl Pts',(-0.689592299481867,-2.18094418517737,
24.2103906130211));
#11751=CARTESIAN_POINT('Ctrl Pts',(-0.715540316679378,-2.17395246593974,
24.2094458066632));
#11752=CARTESIAN_POINT('Ctrl Pts',(-0.741378688380784,-2.16651748416069,
24.2085009495923));
#11753=CARTESIAN_POINT('Ctrl Pts',(-0.767093865522165,-2.15863854180591,
24.2075558906856));
#11754=CARTESIAN_POINT('Ctrl Pts',(-0.784576923837654,-2.15328186050072,
24.206913370516));
#11755=CARTESIAN_POINT('Ctrl Pts',(-0.802008196225349,-2.14771811367944,
24.2062705645783));
#11756=CARTESIAN_POINT('Ctrl Pts',(-0.819353040276014,-2.14195738810084,
24.2056285513437));
#11757=CARTESIAN_POINT('Ctrl Pts',(-0.899037670057529,-2.11549181229842,
24.2026790531084));
#11758=CARTESIAN_POINT('Ctrl Pts',(-0.977003896633911,-2.08484340063866,
24.1997424358208));
#11759=CARTESIAN_POINT('Ctrl Pts',(-1.05286862408811,-2.05008525245381,
24.1968142780767));
#11760=CARTESIAN_POINT('Ctrl Pts',(-1.12747088425221,-2.01590551569441,
24.1939348478968));
#11761=CARTESIAN_POINT('Ctrl Pts',(-1.20004195612714,-1.97775145483,24.1910635980521));
#11762=CARTESIAN_POINT('Ctrl Pts',(-1.27020612803878,-1.93564432789156,
24.1881963242159));
#11763=CARTESIAN_POINT('Ctrl Pts',(-1.31141969883518,-1.91091111990478,
24.1865121228633));
#11764=CARTESIAN_POINT('Ctrl Pts',(-1.35180254492918,-1.88481311495997,
24.1848292933302));
#11765=CARTESIAN_POINT('Ctrl Pts',(-1.3912746538158,-1.85734710164506,24.1831469835552));
#11766=CARTESIAN_POINT('Ctrl Pts',(-1.42843599657615,-1.83148899667307,
24.1815631591297));
#11767=CARTESIAN_POINT('Ctrl Pts',(-1.4647901026478,-1.80441827314899,24.1799797953884));
#11768=CARTESIAN_POINT('Ctrl Pts',(-1.50031387059669,-1.77619110968528,
24.1783961813238));
#11769=CARTESIAN_POINT('Ctrl Pts',(-1.52215895337135,-1.75883302077856,
24.1774223493707));
#11770=CARTESIAN_POINT('Ctrl Pts',(-1.54368997973301,-1.74103754278265,
24.1764484227568));
#11771=CARTESIAN_POINT('Ctrl Pts',(-1.56490095433692,-1.72281708855658,
24.1754742361418));
#11772=CARTESIAN_POINT('Ctrl Pts',(-1.57363676202097,-1.71531293624829,
24.1750730142708));
#11773=CARTESIAN_POINT('Ctrl Pts',(-1.58231716468627,-1.70773758138891,
24.1746717978913));
#11774=CARTESIAN_POINT('Ctrl Pts',(-1.59093464169824,-1.7000984316877,24.1742709109446));
#11775=CARTESIAN_POINT('Ctrl Pts',(-1.65233345722648,-1.6456701178499,24.1714146243938));
#11776=CARTESIAN_POINT('Ctrl Pts',(-1.71064235138754,-1.5879200224839,24.1685703732265));
#11777=CARTESIAN_POINT('Ctrl Pts',(-1.7657711224227,-1.52723905871173,24.1657341439519));
#11778=CARTESIAN_POINT('Ctrl Pts',(-1.82208471200389,-1.46525394957374,
24.1628369589008));
#11779=CARTESIAN_POINT('Ctrl Pts',(-1.87508056446529,-1.40020996058436,
24.1599481442582));
#11780=CARTESIAN_POINT('Ctrl Pts',(-1.9246306784322,-1.33247774123381,24.1570634221601));
#11781=CARTESIAN_POINT('Ctrl Pts',(-1.97456954733109,-1.26421411575282,
24.154156067421));
#11782=CARTESIAN_POINT('Ctrl Pts',(-2.02100893183075,-1.19321907898066,
24.1512528696959));
#11783=CARTESIAN_POINT('Ctrl Pts',(-2.0637776491882,-1.11983747840203,24.1483494496407));
#11784=CARTESIAN_POINT('Ctrl Pts',(-2.0795834502622,-1.09271824142458,24.1472764485627));
#11785=CARTESIAN_POINT('Ctrl Pts',(-2.09488748613988,-1.06527277805129,
24.1462034171193));
#11786=CARTESIAN_POINT('Ctrl Pts',(-2.10967951463669,-1.03751766643348,
24.1451301342659));
#11787=CARTESIAN_POINT('Ctrl Pts',(-2.11587483425371,-1.02589304121624,
24.1446806130716));
#11788=CARTESIAN_POINT('Ctrl Pts',(-2.12198032795743,-1.01421409411385,
24.1442310477757));
#11789=CARTESIAN_POINT('Ctrl Pts',(-2.12799519446604,-1.00248202627111,
24.1437814221381));
#11790=CARTESIAN_POINT('Ctrl Pts',(-2.13396603477409,-0.990835832050165,
24.1433350875641));
#11791=CARTESIAN_POINT('Ctrl Pts',(-2.13984317964154,-0.979145837240882,
24.1428890211268));
#11792=CARTESIAN_POINT('Ctrl Pts',(-2.14562556976068,-0.967414792131108,
24.142443258451));
#11793=CARTESIAN_POINT('Ctrl Pts',(-2.18361797146055,-0.890337568182734,
24.1395144358891));
#11794=CARTESIAN_POINT('Ctrl Pts',(-2.21753276717342,-0.811472272895308,
24.136598003258));
#11795=CARTESIAN_POINT('Ctrl Pts',(-2.24724034073236,-0.731200385356096,
24.133689629466));
#11796=CARTESIAN_POINT('Ctrl Pts',(-2.27690411613959,-0.651046843406481,
24.1307855435165));
#11797=CARTESIAN_POINT('Ctrl Pts',(-2.30237352692883,-0.56948993524845,
24.1278894926613));
#11798=CARTESIAN_POINT('Ctrl Pts',(-2.32347574001613,-0.486881735692151,
24.1249971649368));
#11799=CARTESIAN_POINT('Ctrl Pts',(-2.34386305936945,-0.407072109157236,
24.1222028225259));
#11800=CARTESIAN_POINT('Ctrl Pts',(-2.36017424532588,-0.326280337423849,
24.1194119552567));
#11801=CARTESIAN_POINT('Ctrl Pts',(-2.37220829744034,-0.244811300888254,
24.1166206747247));
#11802=CARTESIAN_POINT('Ctrl Pts',(-2.37735577292346,-0.209963531889701,
24.1154267254241));
#11803=CARTESIAN_POINT('Ctrl Pts',(-2.38172009802993,-0.174991762461182,
24.1142327005114));
#11804=CARTESIAN_POINT('Ctrl Pts',(-2.38528276313686,-0.139919699510735,
24.1130382956749));
#11805=CARTESIAN_POINT('Ctrl Pts',(-2.38690272774666,-0.123972227866057,
24.1124951928273));
#11806=CARTESIAN_POINT('Ctrl Pts',(-2.38835698230774,-0.10800180593106,
24.1119519365248));
#11807=CARTESIAN_POINT('Ctrl Pts',(-2.38964215962342,-0.0920336681917538,
24.1114092786465));
#11808=CARTESIAN_POINT('Ctrl Pts',(-2.39213828655412,-0.0610196608964784,
24.1103553050604));
#11809=CARTESIAN_POINT('Ctrl Pts',(-2.3939987663675,-0.0299955611709274,
24.1093029502777));
#11810=CARTESIAN_POINT('Ctrl Pts',(-2.39521656654617,0.001021571385391,
24.1082520127107));
#11811=CARTESIAN_POINT('',(0.159585929069883,2.44139648025874,24.0495));
#11812=CARTESIAN_POINT('Ctrl Pts',(0.159495341663529,2.44078487595686,24.0495));
#11813=CARTESIAN_POINT('Ctrl Pts',(0.074066622340348,2.43585402826852,24.0598924200211));
#11814=CARTESIAN_POINT('Ctrl Pts',(-0.010859609583587,2.42667871388636,
24.0703216585747));
#11815=CARTESIAN_POINT('Ctrl Pts',(-0.094920089983451,2.41327471514423,
24.080805508462));
#11816=CARTESIAN_POINT('Ctrl Pts',(-0.176987040604973,2.4001885978907,24.0910407294235));
#11817=CARTESIAN_POINT('Ctrl Pts',(-0.258229635425402,2.38307157874212,
24.1013280021715));
#11818=CARTESIAN_POINT('Ctrl Pts',(-0.338289104553414,2.36189432291947,
24.1116838833996));
#11819=CARTESIAN_POINT('Ctrl Pts',(-0.397114404548053,2.3463339096367,24.1192930747493));
#11820=CARTESIAN_POINT('Ctrl Pts',(-0.455300575655561,2.32858051294793,
24.126939306927));
#11821=CARTESIAN_POINT('Ctrl Pts',(-0.512694147882364,2.30860859110673,
24.1346291478542));
#11822=CARTESIAN_POINT('Ctrl Pts',(-0.555739327052466,2.29362964972583,
24.1403965285497));
#11823=CARTESIAN_POINT('Ctrl Pts',(-0.598338485322387,2.2774025434246,24.1461884391666));
#11824=CARTESIAN_POINT('Ctrl Pts',(-0.640422373698764,2.25991242064119,
24.152007650547));
#11825=CARTESIAN_POINT('Ctrl Pts',(-0.653200954142075,2.25460162476243,
24.1537746274973));
#11826=CARTESIAN_POINT('Ctrl Pts',(-0.665933630679759,2.2491736383325,24.1555443500471));
#11827=CARTESIAN_POINT('Ctrl Pts',(-0.678613238495502,2.24363023951219,
24.1573161763736));
#11828=CARTESIAN_POINT('Ctrl Pts',(-0.751691414929867,2.21168118533612,
24.1675279935516));
#11829=CARTESIAN_POINT('Ctrl Pts',(-0.822765594480603,2.17600952669347,
24.1777755768916));
#11830=CARTESIAN_POINT('Ctrl Pts',(-0.891516000215402,2.1365999170335,24.1880762105869));
#11831=CARTESIAN_POINT('Ctrl Pts',(-0.928691853481322,2.11528970292891,
24.1936461391234));
#11832=CARTESIAN_POINT('Ctrl Pts',(-0.965187750721331,2.09288581138188,
24.1992315793692));
#11833=CARTESIAN_POINT('Ctrl Pts',(-1.00094891382958,2.06938099984342,24.2048352641135));
#11834=CARTESIAN_POINT('Ctrl Pts',(-1.06863380541471,2.02489361513802,24.215441317201));
#11835=CARTESIAN_POINT('Ctrl Pts',(-1.13368940850762,1.97646369796482,24.2261127272925));
#11836=CARTESIAN_POINT('Ctrl Pts',(-1.19591823356727,1.92440867374989,24.236868023152));
#11837=CARTESIAN_POINT('Ctrl Pts',(-1.25694043864282,1.8733629990194,24.247414773295));
#11838=CARTESIAN_POINT('Ctrl Pts',(-1.31524464581085,1.8188304042027,24.2580421876465));
#11839=CARTESIAN_POINT('Ctrl Pts',(-1.37059918672337,1.76109384934245,24.2687677379139));
#11840=CARTESIAN_POINT('Ctrl Pts',(-1.37922787016168,1.75209385681257,24.2704396400999));
#11841=CARTESIAN_POINT('Ctrl Pts',(-1.38778631348174,1.74301434343772,24.2721142293588));
#11842=CARTESIAN_POINT('Ctrl Pts',(-1.39626855939247,1.73386174862397,24.2737905875937));
#11843=CARTESIAN_POINT('Ctrl Pts',(-1.44977170631647,1.6761302668667,24.2843644900577));
#11844=CARTESIAN_POINT('Ctrl Pts',(-1.50010267921852,1.61565151228324,24.2949800103224));
#11845=CARTESIAN_POINT('Ctrl Pts',(-1.54711077140567,1.55273985902926,24.3056567313238));
#11846=CARTESIAN_POINT('Ctrl Pts',(-1.59401007223834,1.48997380291934,24.3163087430701));
#11847=CARTESIAN_POINT('Ctrl Pts',(-1.63760217101603,1.42478505545467,24.3270216726058));
#11848=CARTESIAN_POINT('Ctrl Pts',(-1.67768937555964,1.35746710940028,24.3378149672182));
#11849=CARTESIAN_POINT('Ctrl Pts',(-1.71708448207235,1.2913113949966,24.3484219176335));
#11850=CARTESIAN_POINT('Ctrl Pts',(-1.75309481729665,1.22309842468162,24.3591064821044));
#11851=CARTESIAN_POINT('Ctrl Pts',(-1.78548310123427,1.15310335933718,24.3698871179472));
#11852=CARTESIAN_POINT('Ctrl Pts',(-1.79513059553039,1.13225393752258,24.3730983446674));
#11853=CARTESIAN_POINT('Ctrl Pts',(-1.80445637075224,1.11124642477179,24.376318095461));
#11854=CARTESIAN_POINT('Ctrl Pts',(-1.81345325565301,1.09008821973168,24.3795468581352));
#11855=CARTESIAN_POINT('Ctrl Pts',(-1.82117410078255,1.07193091015893,24.3823176812415));
#11856=CARTESIAN_POINT('Ctrl Pts',(-1.82865272688874,1.05366262327258,24.3850951411792));
#11857=CARTESIAN_POINT('Ctrl Pts',(-1.83588435026998,1.0352880996252,24.3878795462433));
#11858=CARTESIAN_POINT('Ctrl Pts',(-1.84027022210393,1.02414422480222,24.3895682464287));
#11859=CARTESIAN_POINT('Ctrl Pts',(-1.84456465303352,1.01296257609607,24.3912593019588));
#11860=CARTESIAN_POINT('Ctrl Pts',(-1.84876261773455,1.00175544207809,24.3929510965693));
#11861=CARTESIAN_POINT('Ctrl Pts',(-1.87498362800088,0.931754287454496,
24.4035182563739));
#11862=CARTESIAN_POINT('Ctrl Pts',(-1.89749241407045,0.860640587905358,
24.4141322445436));
#11863=CARTESIAN_POINT('Ctrl Pts',(-1.91611893315911,0.788676151971129,
24.4248130114787));
#11864=CARTESIAN_POINT('Ctrl Pts',(-1.93444514215941,0.717871978242132,
24.4353215754354));
#11865=CARTESIAN_POINT('Ctrl Pts',(-1.94901332439558,0.646243438436678,
24.4458947822059));
#11866=CARTESIAN_POINT('Ctrl Pts',(-1.95961190993143,0.57404300926657,24.4565516327006));
#11867=CARTESIAN_POINT('Ctrl Pts',(-1.96989411958387,0.503997818121701,
24.4668903680583));
#11868=CARTESIAN_POINT('Ctrl Pts',(-1.97644009504731,0.433413724452126,
24.4773078280141));
#11869=CARTESIAN_POINT('Ctrl Pts',(-1.97900996395521,0.362534966344129,
24.4878213621914));
#11870=CARTESIAN_POINT('Ctrl Pts',(-1.98042268495318,0.323571146212466,
24.4936009140003));
#11871=CARTESIAN_POINT('Ctrl Pts',(-1.98063301484526,0.284518578367179,
24.4994094991982));
#11872=CARTESIAN_POINT('Ctrl Pts',(-1.97959496748079,0.245420714742538,
24.50525));
#11873=CARTESIAN_POINT('',(-1.82664886469444,1.63001483842228,24.0495));
#11874=CARTESIAN_POINT('Origin',(0.,0.,24.0495));
#11875=CARTESIAN_POINT('Ctrl Pts',(-2.39521656654617,0.001021571385391,
24.1082520127107));
#11876=CARTESIAN_POINT('Ctrl Pts',(-2.39739631790017,0.0565394123832736,
24.1063709302271));
#11877=CARTESIAN_POINT('Ctrl Pts',(-2.39751759691081,0.112034830010131,
24.1044943877483));
#11878=CARTESIAN_POINT('Ctrl Pts',(-2.39553324020752,0.167412233368244,
24.1026212294439));
#11879=CARTESIAN_POINT('Ctrl Pts',(-2.39254564629891,0.250786957616897,
24.0998010528444));
#11880=CARTESIAN_POINT('Ctrl Pts',(-2.38478792175979,0.333894356888358,
24.0969885473228));
#11881=CARTESIAN_POINT('Ctrl Pts',(-2.37251451712036,0.416446035661837,
24.0941797683107));
#11882=CARTESIAN_POINT('Ctrl Pts',(-2.35999928411089,0.50062426701053,24.0913156466721));
#11883=CARTESIAN_POINT('Ctrl Pts',(-2.34278840534906,0.584225486929525,
24.0884553998398));
#11884=CARTESIAN_POINT('Ctrl Pts',(-2.32109729603087,0.666939404154293,
24.0855948454564));
#11885=CARTESIAN_POINT('Ctrl Pts',(-2.31259055669967,0.699377843450882,
24.084473003778));
#11886=CARTESIAN_POINT('Ctrl Pts',(-2.30339418836639,0.731679697293737,
24.0833511147976));
#11887=CARTESIAN_POINT('Ctrl Pts',(-2.29351910700337,0.763825629065356,
24.0822289262454));
#11888=CARTESIAN_POINT('Ctrl Pts',(-2.28936411833043,0.77735118672735,24.0817567599358));
#11889=CARTESIAN_POINT('Ctrl Pts',(-2.28508844313765,0.790850716500235,
24.0812844851308));
#11890=CARTESIAN_POINT('Ctrl Pts',(-2.28069445625563,0.804317800009188,
24.0808122566953));
#11891=CARTESIAN_POINT('Ctrl Pts',(-2.2540220454743,0.886065787206666,24.0779457322492));
#11892=CARTESIAN_POINT('Ctrl Pts',(-2.22309404362808,0.966317231109224,
24.0750914824426));
#11893=CARTESIAN_POINT('Ctrl Pts',(-2.18818569208204,1.04477343365878,24.0722454631076));
#11894=CARTESIAN_POINT('Ctrl Pts',(-2.15278423629671,1.12433788350052,24.0693592418114));
#11895=CARTESIAN_POINT('Ctrl Pts',(-2.11328881800044,1.20205688667092,24.0664814851511));
#11896=CARTESIAN_POINT('Ctrl Pts',(-2.06993298717036,1.27760977683417,24.0636079751466));
#11897=CARTESIAN_POINT('Ctrl Pts',(-2.02664727870796,1.35304047011081,24.0607391126676));
#11898=CARTESIAN_POINT('Ctrl Pts',(-1.97951314196675,1.42631291964495,24.0578744831188));
#11899=CARTESIAN_POINT('Ctrl Pts',(-1.92871671623399,1.49708592005729,24.0550098889532));
#11900=CARTESIAN_POINT('Ctrl Pts',(-1.89615495226116,1.54245316198097,24.0531736133146));
#11901=CARTESIAN_POINT('Ctrl Pts',(-1.86208739606077,1.58679286825759,24.0513373522154));
#11902=CARTESIAN_POINT('Ctrl Pts',(-1.82655445601515,1.63000783787766,24.0495));
#11903=CARTESIAN_POINT('',(-1.5,-1.83697019872103E-16,25.));
#11904=CARTESIAN_POINT('',(-2.,-2.44929359829471E-16,24.5));
#11905=CARTESIAN_POINT('Origin',(0.,0.,25.));
#11906=CARTESIAN_POINT('Ctrl Pts',(1.42545942445496,-1.99324250386964,-0.263127385183172));
#11907=CARTESIAN_POINT('Ctrl Pts',(2.08802763447242,-1.51940949184021,-0.22080398276521));
#11908=CARTESIAN_POINT('Ctrl Pts',(2.89213498951261,0.132635996242408,-0.136157177929286));
#11909=CARTESIAN_POINT('Ctrl Pts',(1.45520218380153,2.50608301571523,-0.00918697067539983));
#11910=CARTESIAN_POINT('Ctrl Pts',(-1.31405113801543,2.57978936419321,0.117783236578486));
#11911=CARTESIAN_POINT('Ctrl Pts',(-2.88067287706129,0.297396321818725,
0.244753443832372));
#11912=CARTESIAN_POINT('Ctrl Pts',(-1.81260958243465,-2.25895247596901,
0.371723651086258));
#11913=CARTESIAN_POINT('Ctrl Pts',(0.913666777514348,-2.74797773594403,
0.498693858340144));
#11914=CARTESIAN_POINT('Ctrl Pts',(2.80409801069081,-0.723890240901197,
0.62566406559403));
#11915=CARTESIAN_POINT('Ctrl Pts',(2.12960253907237,1.96263403532227,0.752634272847918));
#11916=CARTESIAN_POINT('Ctrl Pts',(-0.492916539459615,2.8537447239999,0.879604480101801));
#11917=CARTESIAN_POINT('Ctrl Pts',(-2.66453975376405,1.13454357669983,1.00657468735569));
#11918=CARTESIAN_POINT('Ctrl Pts',(-2.39885204218408,-1.62249170425571,
1.13354489460957));
#11919=CARTESIAN_POINT('Ctrl Pts',(0.061126426924356,-2.89537413517611,
1.26051510186346));
#11920=CARTESIAN_POINT('Ctrl Pts',(2.46518916271889,-1.51979997447114,1.38748530911735));
#11921=CARTESIAN_POINT('Ctrl Pts',(2.61428569985594,1.24597721053458,1.51445551637123));
#11922=CARTESIAN_POINT('Ctrl Pts',(0.372032336604703,2.8720263299409,1.64142572362512));
#11923=CARTESIAN_POINT('Ctrl Pts',(-2.21052758161165,1.870966192965,1.76839593087901));
#11924=CARTESIAN_POINT('Ctrl Pts',(-2.77106544293345,-0.841512102466542,
1.89536613813289));
#11925=CARTESIAN_POINT('Ctrl Pts',(-0.796843696806246,-2.7842388029683,
2.02233634538678));
#11926=CARTESIAN_POINT('Ctrl Pts',(1.90626990835674,-2.1801562189121,2.14930655264067));
#11927=CARTESIAN_POINT('Ctrl Pts',(2.8656730678851,0.418167282282024,2.27627675989455));
#11928=CARTESIAN_POINT('Ctrl Pts',(1.20377683918878,2.63398315136886,2.40324696714844));
#11929=CARTESIAN_POINT('Ctrl Pts',(-1.5592427162438,2.4404319593272,2.53021717440232));
#11930=CARTESIAN_POINT('Ctrl Pts',(-2.89598584198633,0.0145595381614903,
2.65718738165621));
#11931=CARTESIAN_POINT('Ctrl Pts',(-1.58370177295115,-2.42463082992762,
2.7841575889101));
#11932=CARTESIAN_POINT('Ctrl Pts',(1.17723200946275,-2.64595366058855,2.91112779616398));
#11933=CARTESIAN_POINT('Ctrl Pts',(2.86132364740886,-0.446959684274638,
3.03809800341787));
#11934=CARTESIAN_POINT('Ctrl Pts',(1.92809442652916,2.16087895448481,3.16506821067175));
#11935=CARTESIAN_POINT('Ctrl Pts',(-0.768808667492088,2.79211017115979,
3.29203841792564));
#11936=CARTESIAN_POINT('Ctrl Pts',(-2.76246417072418,0.869331743334865,
3.41900862517952));
#11937=CARTESIAN_POINT('Ctrl Pts',(-2.22922793215949,-1.84864512573327,
3.54597883243341));
#11938=CARTESIAN_POINT('Ctrl Pts',(0.343136166208384,-2.87562228849207,
3.67294903968729));
#11939=CARTESIAN_POINT('Ctrl Pts',(2.60162544445905,-1.27219928520545,3.79991924694119));
#11940=CARTESIAN_POINT('Ctrl Pts',(2.4803459928753,1.49493469093412,3.92688945419507));
#11941=CARTESIAN_POINT('Ctrl Pts',(0.0902350130762593,2.89461631602099,
4.05385966144895));
#11942=CARTESIAN_POINT('Ctrl Pts',(-2.38241608137131,1.64652348594472,4.18082986870284));
#11943=CARTESIAN_POINT('Ctrl Pts',(-2.67581446902845,-1.10768357480063,
4.30780007595673));
#11944=CARTESIAN_POINT('Ctrl Pts',(-0.521581659896502,-2.84866609952948,
4.43477028321062));
#11945=CARTESIAN_POINT('Ctrl Pts',(2.10975431061419,-1.98390592604371,4.5617404904645));
#11946=CARTESIAN_POINT('Ctrl Pts',(2.8112477871886,0.695580227992425,4.68871069771839));
#11947=CARTESIAN_POINT('Ctrl Pts',(0.941225986649517,2.73880258810359,4.81568090497227));
#11948=CARTESIAN_POINT('Ctrl Pts',(-1.78975763124189,2.27677701937592,4.94265111222616));
#11949=CARTESIAN_POINT('Ctrl Pts',(-2.88360733584287,-0.267870691230269,
5.06962131948004));
#11950=CARTESIAN_POINT('Ctrl Pts',(-1.33975276154346,-2.56749070348536,
5.19659152673394));
#11951=CARTESIAN_POINT('Ctrl Pts',(1.42960555866,-2.51856584611072,5.32356173398781));
#11952=CARTESIAN_POINT('Ctrl Pts',(2.89126964034985,-0.165848850880107,
5.4505319412417));
#11953=CARTESIAN_POINT('Ctrl Pts',(1.70822055079356,2.33857403654312,5.57750214849559));
#11954=CARTESIAN_POINT('Ctrl Pts',(-1.03737854344871,2.70384757930976,5.70447235574947));
#11955=CARTESIAN_POINT('Ctrl Pts',(-2.83406278757172,0.595847371940374,
5.83144256300336));
#11956=CARTESIAN_POINT('Ctrl Pts',(-2.03836233058378,-2.05718861162609,
5.95841277025725));
#11957=CARTESIAN_POINT('Ctrl Pts',(0.621876676608205,-2.82846519752988,
6.08538297751113));
#11958=CARTESIAN_POINT('Ctrl Pts',(2.71327028295494,-1.01247733119344,6.21235318476502));
#11959=CARTESIAN_POINT('Ctrl Pts',(2.32277096781915,1.72964765359987,6.33932339201891));
#11960=CARTESIAN_POINT('Ctrl Pts',(-0.192422248794526,2.88962275266442,
6.46629359927278));
#11961=CARTESIAN_POINT('Ctrl Pts',(-2.53160225352177,1.40639112785544,6.59326380652668));
#11962=CARTESIAN_POINT('Ctrl Pts',(-2.55506540818197,-1.3632999429542,6.72023401378057));
#11963=CARTESIAN_POINT('Ctrl Pts',(-0.241349406630154,-2.88594810044572,
6.84720422103445));
#11964=CARTESIAN_POINT('Ctrl Pts',(2.29313464286823,-1.76875082592903,6.97417442828833));
#11965=CARTESIAN_POINT('Ctrl Pts',(2.73003384286064,0.966364936958393,7.10114463554223));
#11966=CARTESIAN_POINT('Ctrl Pts',(0.669706094041877,2.81752368617376,7.2281148427961));
#11967=CARTESIAN_POINT('Ctrl Pts',(-2.00321776240315,2.09142644406622,7.35508505005));
#11968=CARTESIAN_POINT('Ctrl Pts',(-2.84375064183066,-0.547748356122364,
7.48205525730387));
#11969=CARTESIAN_POINT('Ctrl Pts',(-1.08303710922197,-2.6858846949553,7.60902546455777));
#11970=CARTESIAN_POINT('Ctrl Pts',(1.66835625059269,-2.36717836160593,7.73599567181165));
#11971=CARTESIAN_POINT('Ctrl Pts',(2.89366443014745,0.1168423735059,7.86296587906554));
#11972=CARTESIAN_POINT('Ctrl Pts',(1.47206886721645,2.49398460795553,7.98993608631941));
#11973=CARTESIAN_POINT('Ctrl Pts',(-1.29606313347053,2.58981974828473,8.11690629357332));
#11974=CARTESIAN_POINT('Ctrl Pts',(-2.87865533115204,0.316685110128232,
8.24387650082718));
#11975=CARTESIAN_POINT('Ctrl Pts',(-1.8280729665141,-2.24612893744935,8.37084670808109));
#11976=CARTESIAN_POINT('Ctrl Pts',(0.894691260744527,-2.75435537331231,
8.49781691533496));
#11977=CARTESIAN_POINT('Ctrl Pts',(2.79906009226845,-0.743107377447683,
8.62478712258886));
#11978=CARTESIAN_POINT('Ctrl Pts',(2.1430620213695,1.94787862740744,8.75175732984274));
#11979=CARTESIAN_POINT('Ctrl Pts',(-0.473245899435898,2.85709367946067,
8.87872753709663));
#11980=CARTESIAN_POINT('Ctrl Pts',(-2.65666452966483,1.15285712530556,9.0056977443505));
#11981=CARTESIAN_POINT('Ctrl Pts',(-2.4099688685346,-1.60592528694242,9.13266795160441));
#11982=CARTESIAN_POINT('Ctrl Pts',(0.0411826897410067,-2.8957296076486,
9.25963815885827));
#11983=CARTESIAN_POINT('Ctrl Pts',(2.45466346129185,-1.53674111884394,9.38660836611218));
#11984=CARTESIAN_POINT('Ctrl Pts',(2.62280512767723,1.22794105590498,9.51357857336605));
#11985=CARTESIAN_POINT('Ctrl Pts',(0.391804503777794,2.86939631375076,9.64054878061995));
#11986=CARTESIAN_POINT('Ctrl Pts',(-2.19758902724922,1.8861464529195,9.76751898787382));
#11987=CARTESIAN_POINT('Ctrl Pts',(-2.77679555799053,-0.822406471078079,
9.89448919512773));
#11988=CARTESIAN_POINT('Ctrl Pts',(-0.816001085855212,-2.77868461730189,
10.0214594023816));
#11989=CARTESIAN_POINT('Ctrl Pts',(1.89120900570025,-2.19323379312495,10.1484296096355));
#11990=CARTESIAN_POINT('Ctrl Pts',(2.86848519653882,0.398420195001009,10.2753998168894));
#11991=CARTESIAN_POINT('Ctrl Pts',(1.22188968930472,2.6256297457406,10.4023700241433));
#11992=CARTESIAN_POINT('Ctrl Pts',(-1.54239740574098,2.45111326080835,10.5293402313971));
#11993=CARTESIAN_POINT('Ctrl Pts',(-2.89581687456089,0.0345051236109951,
10.656310438651));
#11994=CARTESIAN_POINT('Ctrl Pts',(-1.60036370874777,-2.41366567160204,
10.7832806459049));
#11995=CARTESIAN_POINT('Ctrl Pts',(1.1589802406304,-2.6539990158957,10.9102508531588));
#11996=CARTESIAN_POINT('Ctrl Pts',(2.85817737255768,-0.466656277731571,
11.0372210604127));
#11997=CARTESIAN_POINT('Ctrl Pts',(1.94293161840177,2.14754806715978,11.1641912676666));
#11998=CARTESIAN_POINT('Ctrl Pts',(-0.749559941647221,2.79733906926294,
11.2911614749205));
#11999=CARTESIAN_POINT('Ctrl Pts',(-2.75641117861896,0.888337429658026,
11.4181316821743));
#12000=CARTESIAN_POINT('Ctrl Pts',(-2.24190748980745,-1.83324760512384,
11.5451018894282));
#12001=CARTESIAN_POINT('Ctrl Pts',(0.323322352062451,-2.87791741215828,
11.6720720966821));
#12002=CARTESIAN_POINT('Ctrl Pts',(2.59280154130405,-1.29008764894419,11.799042303936));
#12003=CARTESIAN_POINT('Ctrl Pts',(2.49058343499892,1.47781599932333,11.9260125111899));
#12004=CARTESIAN_POINT('Ctrl Pts',(0.11016936844703,2.89392617127718,12.0529827184438));
#12005=CARTESIAN_POINT('Ctrl Pts',(-2.37101924217833,1.66289317990276,12.1799529256976));
#12006=CARTESIAN_POINT('Ctrl Pts',(-2.68338010614347,-1.08922779091451,
12.3069231329516));
#12007=CARTESIAN_POINT('Ctrl Pts',(-0.541189304938158,-2.84500617060272,
12.4338933402054));
#12008=CARTESIAN_POINT('Ctrl Pts',(2.09604023735608,-1.99838967619712,12.5608635474593));
#12009=CARTESIAN_POINT('Ctrl Pts',(2.81597187500845,0.676201429833178,12.6878337547132));
#12010=CARTESIAN_POINT('Ctrl Pts',(0.960066999954102,2.73225498995722,12.8148039619671));
#12011=CARTESIAN_POINT('Ctrl Pts',(-1.77403401586218,2.28904986514295,12.941774169221));
#12012=CARTESIAN_POINT('Ctrl Pts',(-2.88538388370124,-0.248003665747437,
13.0687443764749));
#12013=CARTESIAN_POINT('Ctrl Pts',(-1.35740442202033,-2.55820233946158,
13.1957145837288));
#12014=CARTESIAN_POINT('Ctrl Pts',(1.41222517962834,-2.52835243124267,13.3226847909826));
#12015=CARTESIAN_POINT('Ctrl Pts',(2.89005878923091,-0.185758362762534,
13.4496549982365));
#12016=CARTESIAN_POINT('Ctrl Pts',(1.72428682193203,2.32675330240628,13.5766252054904));
#12017=CARTESIAN_POINT('Ctrl Pts',(-1.01873135074601,2.71092832984464,13.7035954127443));
#12018=CARTESIAN_POINT('Ctrl Pts',(-2.82989170439569,0.615352676064313,
13.8305656199982));
#12019=CARTESIAN_POINT('Ctrl Pts',(-2.05248274601473,-2.04310071994967,
13.9575358272521));
#12020=CARTESIAN_POINT('Ctrl Pts',(0.602381042723655,-2.83268124820181,
14.0845060345059));
#12021=CARTESIAN_POINT('Ctrl Pts',(2.7062325510552,-1.03114080229438,14.2114762417598));
#12022=CARTESIAN_POINT('Ctrl Pts',(2.33462871881716,1.71360868339922,14.3384464490137));
#12023=CARTESIAN_POINT('Ctrl Pts',(-0.172515582029027,2.89087951123947,
14.4654166562676));
#12024=CARTESIAN_POINT('Ctrl Pts',(-2.52185577298868,1.42379402821851,14.5923868635215));
#12025=CARTESIAN_POINT('Ctrl Pts',(-2.5643944516552,-1.34566974806862,14.7193570707754));
#12026=CARTESIAN_POINT('Ctrl Pts',(-0.261220475952221,-2.88421737001396,
14.8463272780293));
#12027=CARTESIAN_POINT('Ctrl Pts',(2.28089808786825,-1.78450270027982,14.9732974852832));
#12028=CARTESIAN_POINT('Ctrl Pts',(2.73662487035168,0.947539072291846,15.100267692537));
#12029=CARTESIAN_POINT('Ctrl Pts',(0.689095734268094,2.81284429778126,15.2272378997909));
#12030=CARTESIAN_POINT('Ctrl Pts',(-1.98876567495755,2.10517387991056,15.3542081070448));
#12031=CARTESIAN_POINT('Ctrl Pts',(-2.84745577560679,-0.528149202887348,
15.4811783142987));
#12032=CARTESIAN_POINT('Ctrl Pts',(-1.10151029014829,-2.6783616363823,15.6081485215526));
#12033=CARTESIAN_POINT('Ctrl Pts',(1.65201288089262,-2.3786129184699,15.7351187288065));
#12034=CARTESIAN_POINT('Ctrl Pts',(2.89440054101786,0.096909662586019,15.8620889360604));
#12035=CARTESIAN_POINT('Ctrl Pts',(1.48921112051991,2.48378666818768,15.9890591433142));
#12036=CARTESIAN_POINT('Ctrl Pts',(-1.27819516492898,2.59868487795254,16.1160293505682));
#12037=CARTESIAN_POINT('Ctrl Pts',(-2.87640590357244,0.33650416407621,16.242999557822));
#12038=CARTESIAN_POINT('Ctrl Pts',(-1.84349968485467,-2.23348491969114,
16.3699697650759));
#12039=CARTESIAN_POINT('Ctrl Pts',(0.875699583007191,-2.76045217579802,
16.4969399723298));
#12040=CARTESIAN_POINT('Ctrl Pts',(2.79387559488741,-0.762368109799676,
16.6239101795837));
#12041=CARTESIAN_POINT('Ctrl Pts',(2.15642708752431,1.93307221560355,16.7508803868376));
#12042=CARTESIAN_POINT('Ctrl Pts',(-0.453556613933447,2.86028536557181,
16.8778505940914));
#12043=CARTESIAN_POINT('Ctrl Pts',(-2.64866128299822,1.17112739806275,17.0048208013453));
#12044=CARTESIAN_POINT('Ctrl Pts',(-2.42097242095965,-1.58928868098272,
17.1317910085992));
#12045=CARTESIAN_POINT('Ctrl Pts',(0.0212375495843619,-2.8959445680183,
17.2587612158531));
#12046=CARTESIAN_POINT('Ctrl Pts',(2.4440210279303,-1.5536110161754,17.385731423107));
#12047=CARTESIAN_POINT('Ctrl Pts',(2.63120028826644,1.20984751831527,17.5127016303609));
#12048=CARTESIAN_POINT('Ctrl Pts',(0.411558005066825,2.8666297254812,17.6396718376148));
#12049=CARTESIAN_POINT('Ctrl Pts',(-2.1845461831526,1.90123747812324,17.7666420448687));
#12050=CARTESIAN_POINT('Ctrl Pts',(-2.78239397108689,-0.803261952420473,
17.8936122521225));
#12051=CARTESIAN_POINT('Ctrl Pts',(-0.835119754406293,-2.77299855217189,
18.0205824593764));
#12052=CARTESIAN_POINT('Ctrl Pts',(1.87605838296808,-2.20620736066268,18.1475526666303));
#12053=CARTESIAN_POINT('Ctrl Pts',(2.87116125492305,0.37865422587848,18.2745228738842));
#12054=CARTESIAN_POINT('Ctrl Pts',(1.23994457449353,2.61715177754961,18.4014930811381));
#12055=CARTESIAN_POINT('Ctrl Pts',(-1.52547892705471,2.46167829288456,18.528463288392));
#12056=CARTESIAN_POINT('Ctrl Pts',(-2.89551053760248,0.0544490695970991,
18.6554334956458));
#12057=CARTESIAN_POINT('Ctrl Pts',(-1.61694972722591,-2.40258601389651,
18.7824037028998));
#12058=CARTESIAN_POINT('Ctrl Pts',(1.14067349267392,-2.66191847314265,18.9093739101536));
#12059=CARTESIAN_POINT('Ctrl Pts',(2.85489551329953,-0.486330733852118,
19.0363441174075));
#12060=CARTESIAN_POINT('Ctrl Pts',(1.95767664263525,2.13411530556051,19.1633143246614));
#12061=CARTESIAN_POINT('Ctrl Pts',(-0.730275658617059,2.8024352690077,19.2902845319153));
#12062=CARTESIAN_POINT('Ctrl Pts',(-2.75022742957226,0.907300975517427,
19.4172547391691));
#12063=CARTESIAN_POINT('Ctrl Pts',(-2.25448069721154,-1.81776312000476,
19.5442249464231));
#12064=CARTESIAN_POINT('Ctrl Pts',(0.303493200345932,-2.88007601494976,
19.6711951536769));
#12065=CARTESIAN_POINT('Ctrl Pts',(2.58385464241264,-1.30791481428527,19.7981653609309));
#12066=CARTESIAN_POINT('Ctrl Pts',(2.5007027303468,1.4606272039764,19.9251355681847));
#12067=CARTESIAN_POINT('Ctrl Pts',(0.130098497667631,2.89309874622963,20.0521057754386));
#12068=CARTESIAN_POINT('Ctrl Pts',(-2.35950992801564,1.67918399055304,20.1790759826925));
#12069=CARTESIAN_POINT('Ctrl Pts',(-2.6908184507229,-1.07072033691426,20.3060461899464));
#12070=CARTESIAN_POINT('Ctrl Pts',(-0.560771277348947,-2.84121128199187,
20.4330163972002));
#12071=CARTESIAN_POINT('Ctrl Pts',(2.08222673337684,-2.01277862799546,20.5599866044542));
#12072=CARTESIAN_POINT('Ctrl Pts',(2.82056238055676,0.656790554509431,20.686956811708));
#12073=CARTESIAN_POINT('Ctrl Pts',(0.978862470027363,2.72557778064029,20.813927018962));
#12074=CARTESIAN_POINT('Ctrl Pts',(-1.75822624463689,2.30121412459989,20.9408972262158));
#12075=CARTESIAN_POINT('Ctrl Pts',(-2.88702355705684,-0.228124876075658,
21.0678674334697));
#12076=CARTESIAN_POINT('Ctrl Pts',(-1.37499168967642,-2.54879262012524,
21.1948376407236));
#12077=CARTESIAN_POINT('Ctrl Pts',(1.39477780622873,-2.53801907959506,21.3218078479775));
#12078=CARTESIAN_POINT('Ctrl Pts',(2.88871084525135,-0.20565905959194,21.4487780552314));
#12079=CARTESIAN_POINT('Ctrl Pts',(1.74027128981661,2.31482218714578,21.5757482624852));
#12080=CARTESIAN_POINT('Ctrl Pts',(-1.00003581763517,2.71788049248305,21.7027184697391));
#12081=CARTESIAN_POINT('Ctrl Pts',(-2.82558640606945,0.634828767624046,
21.829688676993));
#12082=CARTESIAN_POINT('Ctrl Pts',(-2.06650574459841,-2.02891586731337,
21.9566588842469));
#12083=CARTESIAN_POINT('Ctrl Pts',(0.582856733610425,-2.83676300309042,
22.0836290915008));
#12084=CARTESIAN_POINT('Ctrl Pts',(2.69906663270847,-1.04975520788588,22.2105992987547));
#12085=CARTESIAN_POINT('Ctrl Pts',(2.34637535894793,1.69748813671122,22.3375695060086));
#12086=CARTESIAN_POINT('Ctrl Pts',(-0.152600041786191,2.89199968134328,
22.4645397132624));
#12087=CARTESIAN_POINT('Ctrl Pts',(-2.5119909759523,1.44112834512521,22.5915099205164));
#12088=CARTESIAN_POINT('Ctrl Pts',(-2.57359934481574,-1.32797373282733,
22.7184801277702));
#12089=CARTESIAN_POINT('Ctrl Pts',(-0.281083919150256,-2.88235360097688,
22.8454503350241));
#12090=CARTESIAN_POINT('Ctrl Pts',(2.26856240924181,-1.80016272103242,22.972420542278));
#12091=CARTESIAN_POINT('Ctrl Pts',(2.74306879317415,0.928654543166714,23.0993907495319));
#12092=CARTESIAN_POINT('Ctrl Pts',(0.708485608711905,2.80805759792725,23.2263609567858));
#12093=CARTESIAN_POINT('Ctrl Pts',(-1.97428195070499,2.11877169925234,23.3533311640396));
#12094=CARTESIAN_POINT('Ctrl Pts',(-2.85090640203137,-0.508430235562458,
23.4803013712935));
#12095=CARTESIAN_POINT('Ctrl Pts',(-1.12015872947254,-2.6708920247376,23.6072715785474));
#12096=CARTESIAN_POINT('Ctrl Pts',(1.63602484856987,-2.38959065359107,23.7342417858013));
#12097=CARTESIAN_POINT('Ctrl Pts',(2.8941699184606,0.0763153981960129,23.8612119930552));
#12098=CARTESIAN_POINT('Ctrl Pts',(1.50789198472586,2.47473781233419,23.988182200309));
#12099=CARTESIAN_POINT('Ctrl Pts',(-1.26358600876801,2.60487763695496,24.115152407563));
#12100=CARTESIAN_POINT('Ctrl Pts',(-2.33166392375486,1.10986843944438,24.1997992123989));
#12101=CARTESIAN_POINT('Ctrl Pts',(-2.43188242527222,0.301493150257353,
24.2421226148168));
#12102=CARTESIAN_POINT('Ctrl Pts',(1.33708927785964,-1.86967312739702,-0.175418256788781));
#12103=CARTESIAN_POINT('Ctrl Pts',(1.9585821343145,-1.42521499059475,-0.133094854370819));
#12104=CARTESIAN_POINT('Ctrl Pts',(2.71283953668389,0.124413340282714,-0.0484480495348954));
#12105=CARTESIAN_POINT('Ctrl Pts',(1.36498816009652,2.3507205271874,0.0785221577189909));
#12106=CARTESIAN_POINT('Ctrl Pts',(-1.23258765353597,2.419857513179,0.205492364972877));
#12107=CARTESIAN_POINT('Ctrl Pts',(-2.70208800816096,0.278959489380628,
0.332462572226763));
#12108=CARTESIAN_POINT('Ctrl Pts',(-1.70023839054259,-2.11891063540273,
0.459432779480649));
#12109=CARTESIAN_POINT('Ctrl Pts',(0.857024781479203,-2.57761918963968,
0.586402986734535));
#12110=CARTESIAN_POINT('Ctrl Pts',(2.63026033560785,-0.679013280105372,
0.713373193988421));
#12111=CARTESIAN_POINT('Ctrl Pts',(1.997579638007,1.84096220486614,0.840343401242307));
#12112=CARTESIAN_POINT('Ctrl Pts',(-0.462358597154108,2.67682924308268,
0.967313608496194));
#12113=CARTESIAN_POINT('Ctrl Pts',(-2.49935387431386,1.06420851105598,1.09428381575008));
#12114=CARTESIAN_POINT('Ctrl Pts',(-2.25013724680555,-1.5219067087834,1.22125402300397));
#12115=CARTESIAN_POINT('Ctrl Pts',(0.0573369459924396,-2.71587787426249,
1.34822423025785));
#12116=CARTESIAN_POINT('Ctrl Pts',(2.3123618538827,-1.42558126558655,1.47519443751174));
#12117=CARTESIAN_POINT('Ctrl Pts',(2.45221527780476,1.16873391138456,1.60216464476562));
#12118=CARTESIAN_POINT('Ctrl Pts',(0.348968507806855,2.69397749638712,1.72913485201951));
#12119=CARTESIAN_POINT('Ctrl Pts',(-2.07348780125123,1.75497723255643,1.85610505927339));
#12120=CARTESIAN_POINT('Ctrl Pts',(-2.59927559383913,-0.789343274241099,
1.98307526652729));
#12121=CARTESIAN_POINT('Ctrl Pts',(-0.747444048459754,-2.61163228260472,
2.11004547378116));
#12122=CARTESIAN_POINT('Ctrl Pts',(1.78809232409043,-2.04499928539254,2.23701568103506));
#12123=CARTESIAN_POINT('Ctrl Pts',(2.68801809941763,0.392243356702178,2.36398588828894));
#12124=CARTESIAN_POINT('Ctrl Pts',(1.1291497162261,2.47069160253713,2.49095609554283));
#12125=CARTESIAN_POINT('Ctrl Pts',(-1.46257878807563,2.28913945229282,2.61792630279671));
#12126=CARTESIAN_POINT('Ctrl Pts',(-2.71645165882843,0.0136569319563776,
2.7448965100506));
#12127=CARTESIAN_POINT('Ctrl Pts',(-1.48552152633178,-2.27431790049286,
2.87186671730448));
#12128=CARTESIAN_POINT('Ctrl Pts',(1.10425051067844,-2.48192001020248,2.99883692455838));
#12129=CARTESIAN_POINT('Ctrl Pts',(2.68393831757051,-0.419250798182282,
3.12580713181225));
#12130=CARTESIAN_POINT('Ctrl Pts',(1.80856384979101,2.02691709860416,3.25277733906614));
#12131=CARTESIAN_POINT('Ctrl Pts',(-0.721147026982028,2.61901567200914,
3.37974754632003));
#12132=CARTESIAN_POINT('Ctrl Pts',(-2.59120755019672,0.815438260096795,
3.50671775357391));
#12133=CARTESIAN_POINT('Ctrl Pts',(-2.09102883944623,-1.73403994093382,
3.6336879608278));
#12134=CARTESIAN_POINT('Ctrl Pts',(0.321863730957119,-2.69735052654142,
3.76065816808169));
#12135=CARTESIAN_POINT('Ctrl Pts',(2.44033988419076,-1.19333037080265,3.88762837533557));
#12136=CARTESIAN_POINT('Ctrl Pts',(2.32657904922396,1.40225748418809,4.01459858258946));
#12137=CARTESIAN_POINT('Ctrl Pts',(0.084640970063364,2.71516703546239,4.14156878984334));
#12138=CARTESIAN_POINT('Ctrl Pts',(-2.23472021942679,1.54444866057315,4.26853899709723));
#12139=CARTESIAN_POINT('Ctrl Pts',(-2.50992962317935,-1.03901367216639,
4.39550920435112));
#12140=CARTESIAN_POINT('Ctrl Pts',(-0.489246647790451,-2.6720654636238,
4.522479411605));
#12141=CARTESIAN_POINT('Ctrl Pts',(1.97896188361798,-1.86091536278529,4.64944961885889));
#12142=CARTESIAN_POINT('Ctrl Pts',(2.63696686778288,0.652458322407474,4.77641982611277));
#12143=CARTESIAN_POINT('Ctrl Pts',(0.882875480845896,2.56901284729855,4.90339003336666));
#12144=CARTESIAN_POINT('Ctrl Pts',(-1.67880312665934,2.13563016137682,5.03036024062055));
#12145=CARTESIAN_POINT('Ctrl Pts',(-2.70484054766217,-0.251264275188861,
5.15733044787444));
#12146=CARTESIAN_POINT('Ctrl Pts',(-1.25669592673788,-2.40832129749834,
5.28430065512832));
#12147=CARTESIAN_POINT('Ctrl Pts',(1.34097837599531,-2.36242949511231,5.41127086238221));
#12148=CARTESIAN_POINT('Ctrl Pts',(2.71202783410766,-0.155567192199782,
5.5382410696361));
#12149=CARTESIAN_POINT('Ctrl Pts',(1.60232086827652,2.19359612493941,5.66521127688997));
#12150=CARTESIAN_POINT('Ctrl Pts',(-0.97306714153387,2.53622484459299,5.79218148414387));
#12151=CARTESIAN_POINT('Ctrl Pts',(-2.65836747159051,0.558908320078628,
5.91915169139774));
#12152=CARTESIAN_POINT('Ctrl Pts',(-1.91199578876737,-1.92965495050268,
6.04612189865165));
#12153=CARTESIAN_POINT('Ctrl Pts',(0.583323960106212,-2.65311689939015,
6.17309210590551));
#12154=CARTESIAN_POINT('Ctrl Pts',(2.54506339572692,-0.949709658787648,
6.30006231315942));
#12155=CARTESIAN_POINT('Ctrl Pts',(2.1787727540419,1.62241961603905,6.42703252041328));
#12156=CARTESIAN_POINT('Ctrl Pts',(-0.180493194875146,2.71048304382584,
6.55400272766719));
#12157=CARTESIAN_POINT('Ctrl Pts',(-2.3746577215157,1.31920310411608,6.68097293492105));
#12158=CARTESIAN_POINT('Ctrl Pts',(-2.39666629782642,-1.27878332063201,
6.80794314217497));
#12159=CARTESIAN_POINT('Ctrl Pts',(-0.226387155107136,-2.70703619855112,
6.93491334942882));
#12160=CARTESIAN_POINT('Ctrl Pts',(2.15097370789069,-1.65909862040404,7.06188355668274));
#12161=CARTESIAN_POINT('Ctrl Pts',(2.560787712971,0.906455963276967,7.18885376393661));
#12162=CARTESIAN_POINT('Ctrl Pts',(0.628188233420324,2.6428536977396,7.3158239711905));
#12163=CARTESIAN_POINT('Ctrl Pts',(-1.87902997824817,1.96177023759366,7.44279417844438));
#12164=CARTESIAN_POINT('Ctrl Pts',(-2.66745473555108,-0.51379116190309,
7.56976438569826));
#12165=CARTESIAN_POINT('Ctrl Pts',(-1.01589514329288,-2.51937555400095,
7.69673459295215));
#12166=CARTESIAN_POINT('Ctrl Pts',(1.56492792151594,-2.22042714915924,7.82370480020605));
#12167=CARTESIAN_POINT('Ctrl Pts',(2.71427416094528,0.109598829776655,7.95067500745992));
#12168=CARTESIAN_POINT('Ctrl Pts',(1.38080920779542,2.33937214994344,8.07764521471382));
#12169=CARTESIAN_POINT('Ctrl Pts',(-1.21571480005839,2.42926607212603,8.20461542196769));
#12170=CARTESIAN_POINT('Ctrl Pts',(-2.70019553829717,0.297052485637893,
8.33158562922158));
#12171=CARTESIAN_POINT('Ctrl Pts',(-1.71474313525672,-2.10688208126453,
8.45855583647548));
#12172=CARTESIAN_POINT('Ctrl Pts',(0.839225635758536,-2.58360145079486,
8.58552604372935));
#12173=CARTESIAN_POINT('Ctrl Pts',(2.62553473866015,-0.697039066589821,
8.71249625098326));
#12174=CARTESIAN_POINT('Ctrl Pts',(2.01020471112819,1.82712154593548,8.83946645823712));
#12175=CARTESIAN_POINT('Ctrl Pts',(-0.443907421755409,2.67997058289342,
8.96643666549102));
#12176=CARTESIAN_POINT('Ctrl Pts',(-2.49196686804545,1.08138672676678,9.0934068727449));
#12177=CARTESIAN_POINT('Ctrl Pts',(-2.26056489494628,-1.50636731244413,
9.22037707999879));
#12178=CARTESIAN_POINT('Ctrl Pts',(0.0386296038606172,-2.71621130952089,
9.34734728725266));
#12179=CARTESIAN_POINT('Ctrl Pts',(2.30248868437777,-1.44147215809947,9.47431749450658));
#12180=CARTESIAN_POINT('Ctrl Pts',(2.46020655093251,1.15181589284589,9.60128770176043));
#12181=CARTESIAN_POINT('Ctrl Pts',(0.367514916265517,2.69151052581742,9.72825790901435));
#12182=CARTESIAN_POINT('Ctrl Pts',(-2.06135136157977,1.76921640518531,9.8552281162682));
#12183=CARTESIAN_POINT('Ctrl Pts',(-2.60465047527895,-0.771422080247088,
9.98219832352212));
#12184=CARTESIAN_POINT('Ctrl Pts',(-0.765413791442057,-2.60642242396238,
10.109168530776));
#12185=CARTESIAN_POINT('Ctrl Pts',(1.77396510930522,-2.05726612649684,10.2361387380299));
#12186=CARTESIAN_POINT('Ctrl Pts',(2.69065589254337,0.373720473328978,10.3631089452838));
#12187=CARTESIAN_POINT('Ctrl Pts',(1.14613967557957,2.46285605919753,10.4900791525376));
#12188=CARTESIAN_POINT('Ctrl Pts',(-1.44677778829329,2.29915857555863,10.6170493597916));
#12189=CARTESIAN_POINT('Ctrl Pts',(-2.71629316639506,0.0323660077726636,
10.7440195670454));
#12190=CARTESIAN_POINT('Ctrl Pts',(-1.50115051956711,-2.26403251784665,
10.8709897742993));
#12191=CARTESIAN_POINT('Ctrl Pts',(1.08713024475642,-2.48946660053905,10.9979599815532));
#12192=CARTESIAN_POINT('Ctrl Pts',(2.68098709335709,-0.437726318053145,
11.1249301888071));
#12193=CARTESIAN_POINT('Ctrl Pts',(1.82248122255242,2.01441264831897,11.251900396061));
#12194=CARTESIAN_POINT('Ctrl Pts',(-0.703091609550923,2.62392040901448,
11.3788706033149));
#12195=CARTESIAN_POINT('Ctrl Pts',(-2.58552980819719,0.833265705034965,
11.5058408105687));
#12196=CARTESIAN_POINT('Ctrl Pts',(-2.10292233868461,-1.71959697653983,
11.6328110178226));
#12197=CARTESIAN_POINT('Ctrl Pts',(0.303278257394332,-2.69950336596484,
11.7597812250765));
#12198=CARTESIAN_POINT('Ctrl Pts',(2.43206301141908,-1.21010976062125,11.8867514323304));
#12199=CARTESIAN_POINT('Ctrl Pts',(2.33618182981621,1.38620005132744,12.0137216395843));
#12200=CARTESIAN_POINT('Ctrl Pts',(0.103339512000114,2.71451967565594,12.1406918468382));
#12201=CARTESIAN_POINT('Ctrl Pts',(-2.224029917602,1.55980352925453,12.267662054092));
#12202=CARTESIAN_POINT('Ctrl Pts',(-2.51702623504576,-1.02170203893063,
12.394632261346));
#12203=CARTESIAN_POINT('Ctrl Pts',(-0.507638733527514,-2.66863242888303,
12.5216024685998));
#12204=CARTESIAN_POINT('Ctrl Pts',(1.96609800268626,-1.87450120514677,12.6485726758537));
#12205=CARTESIAN_POINT('Ctrl Pts',(2.64139808978978,0.634280896384674,12.7755428831076));
#12206=CARTESIAN_POINT('Ctrl Pts',(0.900548461529443,2.56287116193939,12.9025130903615));
#12207=CARTESIAN_POINT('Ctrl Pts',(-1.66405428346344,2.14714216249195,13.0294832976154));
#12208=CARTESIAN_POINT('Ctrl Pts',(-2.70650695994461,-0.232628889080822,
13.1564535048693));
#12209=CARTESIAN_POINT('Ctrl Pts',(-1.27325328751233,-2.39960875771503,
13.2834237121231));
#12210=CARTESIAN_POINT('Ctrl Pts',(1.32467547880323,-2.37160936920924,13.410393919377));
#12211=CARTESIAN_POINT('Ctrl Pts',(2.71089204867564,-0.174242430799153,
13.5373641266309));
#12212=CARTESIAN_POINT('Ctrl Pts',(1.61739112457839,2.18250820717785,13.6643343338848));
#12213=CARTESIAN_POINT('Ctrl Pts',(-0.955575965708573,2.54286663001105,
13.7913045411387));
#12214=CARTESIAN_POINT('Ctrl Pts',(-2.65445497117411,0.577204409436265,
13.9182747483926));
#12215=CARTESIAN_POINT('Ctrl Pts',(-1.92524082103397,-1.91644042570806,
14.0452449556465));
#12216=CARTESIAN_POINT('Ctrl Pts',(0.565036941489686,-2.65707157958072,
14.1722151629003));
#12217=CARTESIAN_POINT('Ctrl Pts',(2.53846196204024,-0.967216103845703,
14.2991853701542));
#12218=CARTESIAN_POINT('Ctrl Pts',(2.18989539383575,1.60737496817656,14.4261555774081));
#12219=CARTESIAN_POINT('Ctrl Pts',(-0.161820625012098,2.71166189072021,
14.553125784662));
#12220=CARTESIAN_POINT('Ctrl Pts',(-2.36551546576707,1.33552712644875,14.6800959919159));
#12221=CARTESIAN_POINT('Ctrl Pts',(-2.40541699517125,-1.26224609470774,
14.8070661991698));
#12222=CARTESIAN_POINT('Ctrl Pts',(-0.245026334360027,-2.70541276328283,
14.9340364064237));
#12223=CARTESIAN_POINT('Ctrl Pts',(2.13949574772732,-1.6738739706801,15.0610066136776));
#12224=CARTESIAN_POINT('Ctrl Pts',(2.56697013530948,0.888797192104508,15.1879768209314));
#12225=CARTESIAN_POINT('Ctrl Pts',(0.646375829365357,2.638464404057,15.3149470281853));
#12226=CARTESIAN_POINT('Ctrl Pts',(-1.86547383569181,1.97466541282641,15.4419172354392));
#12227=CARTESIAN_POINT('Ctrl Pts',(-2.67093017270497,-0.495407041530328,
15.5688874426931));
#12228=CARTESIAN_POINT('Ctrl Pts',(-1.0332230950541,-2.512318881056,15.695857649947));
#12229=CARTESIAN_POINT('Ctrl Pts',(1.54959774514251,-2.23115283038005,15.8228278572008));
#12230=CARTESIAN_POINT('Ctrl Pts',(2.71496463724735,0.0909018303444614,
15.9497980644548));
#12231=CARTESIAN_POINT('Ctrl Pts',(1.39688874166162,2.32980642279196,16.0767682717086));
#12232=CARTESIAN_POINT('Ctrl Pts',(-1.19895454105405,2.43758161560788,16.2037384789625));
#12233=CARTESIAN_POINT('Ctrl Pts',(-2.69808556207027,0.315642874165645,
16.3307086862164));
#12234=CARTESIAN_POINT('Ctrl Pts',(-1.72921348729331,-2.09502191865062,
16.4576788934703));
#12235=CARTESIAN_POINT('Ctrl Pts',(0.821411330955809,-2.58932028718755,
16.5846491007242));
#12236=CARTESIAN_POINT('Ctrl Pts',(2.62067164979186,-0.715105746194832,
16.7116193079781));
#12237=CARTESIAN_POINT('Ctrl Pts',(2.02274122135563,1.81323304505856,16.838589515232));
#12238=CARTESIAN_POINT('Ctrl Pts',(-0.425438756788597,2.6829644031343,16.9655597224858));
#12239=CARTESIAN_POINT('Ctrl Pts',(-2.48445977586001,1.09852434947853,17.0925299297397));
#12240=CARTESIAN_POINT('Ctrl Pts',(-2.27088629148237,-1.49076207874399,
17.2195001369936));
#12241=CARTESIAN_POINT('Ctrl Pts',(0.0199209457316412,-2.716412943605,17.3464703442475));
#12242=CARTESIAN_POINT('Ctrl Pts',(2.29250601963548,-1.45729622047088,17.4734405515014));
#12243=CARTESIAN_POINT('Ctrl Pts',(2.46808126066971,1.134844048755,17.6004107587553));
#12244=CARTESIAN_POINT('Ctrl Pts',(0.386043816015746,2.68891544983839,17.7273809660092));
#12245=CARTESIAN_POINT('Ctrl Pts',(-2.04911709752763,1.78337187509604,17.854351173263));
#12246=CARTESIAN_POINT('Ctrl Pts',(-2.60990181950929,-0.753464409767162,
17.9813213805169));
#12247=CARTESIAN_POINT('Ctrl Pts',(-0.783347214370861,-2.60108886161181,
18.1082915877708));
#12248=CARTESIAN_POINT('Ctrl Pts',(1.75975373656424,-2.06943540873153,18.2352617950247));
#12249=CARTESIAN_POINT('Ctrl Pts',(2.69316605096044,0.355179878678,18.3622320022786));
#12250=CARTESIAN_POINT('Ctrl Pts',(1.16307526349234,2.45490367544551,18.4892022095325));
#12251=CARTESIAN_POINT('Ctrl Pts',(-1.43090815632692,2.30906863744254,18.6161724167864));
#12252=CARTESIAN_POINT('Ctrl Pts',(-2.71600582053626,0.0510735457626923,
18.7431426240402));
#12253=CARTESIAN_POINT('Ctrl Pts',(-1.51670830191366,-2.25363973411232,
18.8701128312942));
#12254=CARTESIAN_POINT('Ctrl Pts',(1.0699584080944,-2.49689509775876,18.997083038548));
#12255=CARTESIAN_POINT('Ctrl Pts',(2.67790869017686,-0.456181072972995,
19.1240532458019));
#12256=CARTESIAN_POINT('Ctrl Pts',(1.83631214152924,2.00181263936867,19.2510234530558));
#12257=CARTESIAN_POINT('Ctrl Pts',(-0.685002839272038,2.62870067418348,
19.3779936603097));
#12258=CARTESIAN_POINT('Ctrl Pts',(-2.57972941542172,0.85105362197164,19.5049638675636));
#12259=CARTESIAN_POINT('Ctrl Pts',(-2.11471608077217,-1.70507243892711,
19.6319340748175));
#12260=CARTESIAN_POINT('Ctrl Pts',(0.284678397100628,-2.70152814800923,
19.7589042820713));
#12261=CARTESIAN_POINT('Ctrl Pts',(2.4236707679272,-1.22683174598488,19.8858744893252));
#12262=CARTESIAN_POINT('Ctrl Pts',(2.34567378804177,1.37007686075223,20.0128446965791));
#12263=CARTESIAN_POINT('Ctrl Pts',(0.122033151777428,2.71374354612161,20.139814903833));
#12264=CARTESIAN_POINT('Ctrl Pts',(-2.21323411359773,1.57508440493182,20.2667851110869));
#12265=CARTESIAN_POINT('Ctrl Pts',(-2.52400344576924,-1.00434193882558,
20.3937553183407));
#12266=CARTESIAN_POINT('Ctrl Pts',(-0.526006738186656,-2.6650728011692,
20.5207255255947));
#12267=CARTESIAN_POINT('Ctrl Pts',(1.95314085515653,-1.88799812609669,20.6476957328485));
#12268=CARTESIAN_POINT('Ctrl Pts',(2.64570401084464,0.616073381793945,20.7746659401024));
#12269=CARTESIAN_POINT('Ctrl Pts',(0.918178722395619,2.55660790054414,20.9016361473563));
#12270=CARTESIAN_POINT('Ctrl Pts',(-1.64922650159215,2.1585523090131,21.0286063546102));
#12271=CARTESIAN_POINT('Ctrl Pts',(-2.70804498314286,-0.213982468094741,
21.1555765618641));
#12272=CARTESIAN_POINT('Ctrl Pts',(-1.28975024744425,-2.39078238593873,
21.282546769118));
#12273=CARTESIAN_POINT('Ctrl Pts',(1.30830974050215,-2.38067674190542,21.4095169763718));
#12274=CARTESIAN_POINT('Ctrl Pts',(2.7096276693385,-0.192909400827225,21.5364871836258));
#12275=CARTESIAN_POINT('Ctrl Pts',(1.63238464894961,2.17131675127667,21.6634573908796));
#12276=CARTESIAN_POINT('Ctrl Pts',(-0.938039446297698,2.54938779923009,
21.7904275981335));
#12277=CARTESIAN_POINT('Ctrl Pts',(-2.65041657616178,0.595473097237805,
21.9173978053874));
#12278=CARTESIAN_POINT('Ctrl Pts',(-1.93839447572803,-1.90313495096593,
22.0443680126413));
#12279=CARTESIAN_POINT('Ctrl Pts',(0.546723025340935,-2.66090028954102,
22.1713382198951));
#12280=CARTESIAN_POINT('Ctrl Pts',(2.5317402887165,-0.984676525168914,22.2983084271491));
#12281=CARTESIAN_POINT('Ctrl Pts',(2.20091381098623,1.59225380109178,22.4252786344029));
#12282=CARTESIAN_POINT('Ctrl Pts',(-0.143139731775406,2.71271261682962,
22.5522488416569));
#12283=CARTESIAN_POINT('Ctrl Pts',(-2.3562622284463,1.35178681709819,22.6792190489107));
#12284=CARTESIAN_POINT('Ctrl Pts',(-2.41405123879661,-1.24564712890483,
22.8061892561647));
#12285=CARTESIAN_POINT('Ctrl Pts',(-0.263658360263974,-2.7036645370246,
22.9331594634184));
#12286=CARTESIAN_POINT('Ctrl Pts',(2.12792480902252,-1.68856316174379,23.0601296706724));
#12287=CARTESIAN_POINT('Ctrl Pts',(2.57301457260841,0.871083393326757,23.1870998779262));
#12288=CARTESIAN_POINT('Ctrl Pts',(0.664563645007867,2.63397445159584,23.3140700851802));
#12289=CARTESIAN_POINT('Ctrl Pts',(-1.85188801762549,1.98742024690464,23.441040292434));
#12290=CARTESIAN_POINT('Ctrl Pts',(-2.67416688047444,-0.476910534840453,
23.5680104996879));
#12291=CARTESIAN_POINT('Ctrl Pts',(-1.05071544021771,-2.50531234164241,
23.6949807069418));
#12292=CARTESIAN_POINT('Ctrl Pts',(1.53460087730742,-2.24145001013409,23.8219509141957));
#12293=CARTESIAN_POINT('Ctrl Pts',(2.71474831193969,0.0715842898877685,
23.9489211214496));
#12294=CARTESIAN_POINT('Ctrl Pts',(1.4144115015539,2.3213185430733,24.0758913287035));
#12295=CARTESIAN_POINT('Ctrl Pts',(-1.18525106712396,2.44339045977451,24.2028615359573));
#12296=CARTESIAN_POINT('Ctrl Pts',(-2.18711439872577,1.04106308798187,24.2875083407933));
#12297=CARTESIAN_POINT('Ctrl Pts',(-2.28111993934175,0.282802338419006,
24.3298317432112));
#12298=CARTESIAN_POINT('Ctrl Pts',(1.24871913126432,-1.7461037509244,-0.0877091283943906));
#12299=CARTESIAN_POINT('Ctrl Pts',(1.82913663415658,-1.33102048934929,-0.0453857259764285));
#12300=CARTESIAN_POINT('Ctrl Pts',(2.53354408385517,0.116190684323019,0.0392610788594953));
#12301=CARTESIAN_POINT('Ctrl Pts',(1.27477413639151,2.19535803865958,0.166231286113382));
#12302=CARTESIAN_POINT('Ctrl Pts',(-1.15112416905651,2.25992566216479,0.293201493367268));
#12303=CARTESIAN_POINT('Ctrl Pts',(-2.52350313926065,0.260522656942532,
0.420171700621154));
#12304=CARTESIAN_POINT('Ctrl Pts',(-1.58786719865054,-1.97886879483645,
0.54714190787504));
#12305=CARTESIAN_POINT('Ctrl Pts',(0.800382785444057,-2.40726064333533,
0.674112115128925));
#12306=CARTESIAN_POINT('Ctrl Pts',(2.45642266052488,-0.634136319309549,
0.801082322382812));
#12307=CARTESIAN_POINT('Ctrl Pts',(1.86555673694162,1.71929037441,0.928052529636697));
#12308=CARTESIAN_POINT('Ctrl Pts',(-0.431800654848601,2.49991376216546,
1.05502273689058));
#12309=CARTESIAN_POINT('Ctrl Pts',(-2.33416799486367,0.993873445412137,
1.18199294414447));
#12310=CARTESIAN_POINT('Ctrl Pts',(-2.10142245142702,-1.42132171331109,
1.30896315139835));
#12311=CARTESIAN_POINT('Ctrl Pts',(0.0535474650605221,-2.53638161334886,
1.43593335865224));
#12312=CARTESIAN_POINT('Ctrl Pts',(2.15953454504651,-1.33136255670197,1.56290356590613));
#12313=CARTESIAN_POINT('Ctrl Pts',(2.29014485575358,1.09149061223455,1.68987377316002));
#12314=CARTESIAN_POINT('Ctrl Pts',(0.325904679009007,2.51592866283334,1.8168439804139));
#12315=CARTESIAN_POINT('Ctrl Pts',(-1.9364480208908,1.63898827214785,1.94381418766779));
#12316=CARTESIAN_POINT('Ctrl Pts',(-2.42748574474482,-0.737174446015656,
2.07078439492167));
#12317=CARTESIAN_POINT('Ctrl Pts',(-0.698044400113263,-2.43902576224114,
2.19775460217556));
#12318=CARTESIAN_POINT('Ctrl Pts',(1.66991473982413,-1.90984235187298,2.32472480942945));
#12319=CARTESIAN_POINT('Ctrl Pts',(2.51036313095016,0.36631943112233,2.45169501668333));
#12320=CARTESIAN_POINT('Ctrl Pts',(1.05452259326343,2.3074000537054,2.57866522393722));
#12321=CARTESIAN_POINT('Ctrl Pts',(-1.36591485990746,2.13784694525844,2.7056354311911));
#12322=CARTESIAN_POINT('Ctrl Pts',(-2.53691747567054,0.012754325751266,
2.832605638445));
#12323=CARTESIAN_POINT('Ctrl Pts',(-1.38734127971241,-2.1240049710581,2.95957584569887));
#12324=CARTESIAN_POINT('Ctrl Pts',(1.03126901189414,-2.31788635981642,3.08654605295276));
#12325=CARTESIAN_POINT('Ctrl Pts',(2.50655298773216,-0.391541912089928,
3.21351626020665));
#12326=CARTESIAN_POINT('Ctrl Pts',(1.68903327305286,1.89295524272351,3.34048646746053));
#12327=CARTESIAN_POINT('Ctrl Pts',(-0.673485386471964,2.44592117285849,
3.46745667471442));
#12328=CARTESIAN_POINT('Ctrl Pts',(-2.41995092966926,0.761544776858728,
3.5944268819683));
#12329=CARTESIAN_POINT('Ctrl Pts',(-1.95282974673297,-1.61943475613438,
3.7213970892222));
#12330=CARTESIAN_POINT('Ctrl Pts',(0.300591295705853,-2.51907876459076,
3.84836729647607));
#12331=CARTESIAN_POINT('Ctrl Pts',(2.27905432392247,-1.11446145639985,3.97533750372997));
#12332=CARTESIAN_POINT('Ctrl Pts',(2.17281210557263,1.30958027744207,4.10230771098385));
#12333=CARTESIAN_POINT('Ctrl Pts',(0.0790469270504698,2.53571775490379,
4.22927791823773));
#12334=CARTESIAN_POINT('Ctrl Pts',(-2.08702435748228,1.44237383520157,4.35624812549163));
#12335=CARTESIAN_POINT('Ctrl Pts',(-2.34404477733026,-0.970343769532158,
4.4832183327455));
#12336=CARTESIAN_POINT('Ctrl Pts',(-0.456911635684403,-2.49546482771812,
4.6101885399994));
#12337=CARTESIAN_POINT('Ctrl Pts',(1.84816945662178,-1.73792479952687,4.73715874725328));
#12338=CARTESIAN_POINT('Ctrl Pts',(2.46268594837716,0.609336416822525,4.86412895450717));
#12339=CARTESIAN_POINT('Ctrl Pts',(0.824524975042275,2.39922310649351,4.99109916176105));
#12340=CARTESIAN_POINT('Ctrl Pts',(-1.56784862207678,1.99448330337771,5.11806936901495));
#12341=CARTESIAN_POINT('Ctrl Pts',(-2.52607375948148,-0.234657859147452,
5.24503957626882));
#12342=CARTESIAN_POINT('Ctrl Pts',(-1.1736390919323,-2.24915189151133,5.37200978352272));
#12343=CARTESIAN_POINT('Ctrl Pts',(1.25235119333062,-2.20629314411389,5.49897999077659));
#12344=CARTESIAN_POINT('Ctrl Pts',(2.53278602786547,-0.145285533519461,
5.62595019803048));
#12345=CARTESIAN_POINT('Ctrl Pts',(1.49642118575949,2.0486182133357,5.75292040528437));
#12346=CARTESIAN_POINT('Ctrl Pts',(-0.908755739619028,2.36860210987622,
5.87989061253825));
#12347=CARTESIAN_POINT('Ctrl Pts',(-2.4826721556093,0.521969268216885,6.00686081979214));
#12348=CARTESIAN_POINT('Ctrl Pts',(-1.78562924695095,-1.80212128937927,
6.13383102704603));
#12349=CARTESIAN_POINT('Ctrl Pts',(0.544771243604218,-2.47776860125043,
6.26080123429992));
#12350=CARTESIAN_POINT('Ctrl Pts',(2.3768565084989,-0.886941986381852,6.3877714415538));
#12351=CARTESIAN_POINT('Ctrl Pts',(2.03477454026465,1.51519157847824,6.51474164880769));
#12352=CARTESIAN_POINT('Ctrl Pts',(-0.168564140955765,2.53134333498726,
6.64171185606157));
#12353=CARTESIAN_POINT('Ctrl Pts',(-2.21771318950963,1.23201508037672,6.76868206331545));
#12354=CARTESIAN_POINT('Ctrl Pts',(-2.23826718747087,-1.19426669830983,
6.89565227056935));
#12355=CARTESIAN_POINT('Ctrl Pts',(-0.211424903584118,-2.52812429665652,
7.02262247782322));
#12356=CARTESIAN_POINT('Ctrl Pts',(2.00881277291316,-1.54944641487905,7.14959268507712));
#12357=CARTESIAN_POINT('Ctrl Pts',(2.39154158308137,0.846546989595545,7.276562892331));
#12358=CARTESIAN_POINT('Ctrl Pts',(0.586670372798765,2.46818370930543,7.40353309958489));
#12359=CARTESIAN_POINT('Ctrl Pts',(-1.75484219409317,1.83211403112111,7.53050330683878));
#12360=CARTESIAN_POINT('Ctrl Pts',(-2.49115882927151,-0.479833967683821,
7.65747351409266));
#12361=CARTESIAN_POINT('Ctrl Pts',(-0.94875317736379,-2.35286641304659,
7.78444372134655));
#12362=CARTESIAN_POINT('Ctrl Pts',(1.46149959243917,-2.07367593671256,7.91141392860043));
#12363=CARTESIAN_POINT('Ctrl Pts',(2.53488389174312,0.102355286047412,8.03838413585432));
#12364=CARTESIAN_POINT('Ctrl Pts',(1.28954954837439,2.18475969193136,8.16535434310821));
#12365=CARTESIAN_POINT('Ctrl Pts',(-1.13536646664624,2.26871239596733,8.29232455036209));
#12366=CARTESIAN_POINT('Ctrl Pts',(-2.52173574544231,0.277419861147555,
8.41929475761597));
#12367=CARTESIAN_POINT('Ctrl Pts',(-1.60141330399934,-1.96763522507972,
8.54626496486987));
#12368=CARTESIAN_POINT('Ctrl Pts',(0.783760010772541,-2.41284752827741,
8.67323517212374));
#12369=CARTESIAN_POINT('Ctrl Pts',(2.45200938505186,-0.65097075573196,8.80020537937764));
#12370=CARTESIAN_POINT('Ctrl Pts',(1.87734740088688,1.70636446446352,8.92717558663151));
#12371=CARTESIAN_POINT('Ctrl Pts',(-0.414568944074917,2.50284748632617,
9.05414579388541));
#12372=CARTESIAN_POINT('Ctrl Pts',(-2.32726920642608,1.00991632822801,9.18111600113929));
#12373=CARTESIAN_POINT('Ctrl Pts',(-2.11116092135796,-1.40680933794583,
9.30808620839318));
#12374=CARTESIAN_POINT('Ctrl Pts',(0.0360765179802292,-2.53669301139319,
9.43505641564706));
#12375=CARTESIAN_POINT('Ctrl Pts',(2.15031390746369,-1.34620319735501,9.56202662290096));
#12376=CARTESIAN_POINT('Ctrl Pts',(2.2976079741878,1.0756907297868,9.68899683015483));
#12377=CARTESIAN_POINT('Ctrl Pts',(0.343225328753236,2.51362473788409,9.81596703740874));
#12378=CARTESIAN_POINT('Ctrl Pts',(-1.92511369591032,1.65228635745112,9.94293724466261));
#12379=CARTESIAN_POINT('Ctrl Pts',(-2.43250539256738,-0.720437689416097,
10.0699074519165));
#12380=CARTESIAN_POINT('Ctrl Pts',(-0.714826497028901,-2.43416023062287,
10.1968776591704));
#12381=CARTESIAN_POINT('Ctrl Pts',(1.65672121291019,-1.92129845986873,10.3238478664243));
#12382=CARTESIAN_POINT('Ctrl Pts',(2.51282658854792,0.34902075165695,10.4508180736782));
#12383=CARTESIAN_POINT('Ctrl Pts',(1.07038966185442,2.30008237265446,10.577788280932));
#12384=CARTESIAN_POINT('Ctrl Pts',(-1.35115817084561,2.14720389030891,10.7047584881859));
#12385=CARTESIAN_POINT('Ctrl Pts',(-2.53676945822922,0.0302268919343324,
10.8317286954398));
#12386=CARTESIAN_POINT('Ctrl Pts',(-1.40193733038645,-2.11439936409126,
10.9586989026937));
#12387=CARTESIAN_POINT('Ctrl Pts',(1.01528024888245,-2.3249341851824,11.0856691099476));
#12388=CARTESIAN_POINT('Ctrl Pts',(2.50379681415649,-0.40879635837472,11.2126393172015));
#12389=CARTESIAN_POINT('Ctrl Pts',(1.70203082670308,1.88127722947816,11.3396095244553));
#12390=CARTESIAN_POINT('Ctrl Pts',(-0.656623277454625,2.45050174876602,
11.4665797317093));
#12391=CARTESIAN_POINT('Ctrl Pts',(-2.41464843777542,0.778193980411903,
11.5935499389631));
#12392=CARTESIAN_POINT('Ctrl Pts',(-1.96393718756176,-1.60594634795581,
11.720520146217));
#12393=CARTESIAN_POINT('Ctrl Pts',(0.283234162726211,-2.52108931977139,
11.8474903534709));
#12394=CARTESIAN_POINT('Ctrl Pts',(2.2713244815341,-1.1301318722983,11.9744605607248));
#12395=CARTESIAN_POINT('Ctrl Pts',(2.18178022463351,1.29458410333155,12.1014307679787));
#12396=CARTESIAN_POINT('Ctrl Pts',(0.0965096555531949,2.53511318003469,
12.2284009752326));
#12397=CARTESIAN_POINT('Ctrl Pts',(-2.07704059302567,1.45671387860629,12.3553711824864));
#12398=CARTESIAN_POINT('Ctrl Pts',(-2.35067236394805,-0.954176286946753,
12.4823413897403));
#12399=CARTESIAN_POINT('Ctrl Pts',(-0.474088162116868,-2.49225868716336,
12.6093115969942));
#12400=CARTESIAN_POINT('Ctrl Pts',(1.83615576801644,-1.75061273409641,12.7362818042481));
#12401=CARTESIAN_POINT('Ctrl Pts',(2.46682430457111,0.59236036293617,12.863252011502));
#12402=CARTESIAN_POINT('Ctrl Pts',(0.841029923104784,2.39348733392156,12.9902222187559));
#12403=CARTESIAN_POINT('Ctrl Pts',(-1.55407455106469,2.00523445984096,13.1171924260098));
#12404=CARTESIAN_POINT('Ctrl Pts',(-2.52763003618799,-0.217254112414209,
13.2441626332636));
#12405=CARTESIAN_POINT('Ctrl Pts',(-1.18910215300433,-2.24101517596849,
13.3711328405175));
#12406=CARTESIAN_POINT('Ctrl Pts',(1.23712577797812,-2.21486630717581,13.4981030477714));
#12407=CARTESIAN_POINT('Ctrl Pts',(2.53172530812039,-0.16272649883577,13.6250732550253));
#12408=CARTESIAN_POINT('Ctrl Pts',(1.51049542722474,2.03826311194943,13.7520434622792));
#12409=CARTESIAN_POINT('Ctrl Pts',(-0.892420580671138,2.37480493017746,
13.8790136695331));
#12410=CARTESIAN_POINT('Ctrl Pts',(-2.47901823795254,0.539056142808217,
14.0059838767869));
#12411=CARTESIAN_POINT('Ctrl Pts',(-1.79799889605321,-1.78978013146645,
14.1329540840409));
#12412=CARTESIAN_POINT('Ctrl Pts',(0.527692840255718,-2.48146191095963,
14.2599242912947));
#12413=CARTESIAN_POINT('Ctrl Pts',(2.37069137302528,-0.903291405397025,
14.3868944985486));
#12414=CARTESIAN_POINT('Ctrl Pts',(2.04516206885435,1.5011412529539,14.5138647058025));
#12415=CARTESIAN_POINT('Ctrl Pts',(-0.151125667995169,2.53244427020094,
14.6408349130564));
#12416=CARTESIAN_POINT('Ctrl Pts',(-2.20917515854546,1.24726022467899,14.7678051203103));
#12417=CARTESIAN_POINT('Ctrl Pts',(-2.2464395386873,-1.17882244134687,14.8947753275642));
#12418=CARTESIAN_POINT('Ctrl Pts',(-0.228832192767835,-2.5266081565517,
15.0217455348181));
#12419=CARTESIAN_POINT('Ctrl Pts',(1.99809340758638,-1.56324524108038,15.1487157420719));
#12420=CARTESIAN_POINT('Ctrl Pts',(2.39731540026729,0.830055311917173,15.2756859493258));
#12421=CARTESIAN_POINT('Ctrl Pts',(0.603655924462618,2.46408451033275,15.4026561565797));
#12422=CARTESIAN_POINT('Ctrl Pts',(-1.74218199642607,1.84415694574227,15.5296263638336));
#12423=CARTESIAN_POINT('Ctrl Pts',(-2.49440456980315,-0.462664880173312,
15.6565965710875));
#12424=CARTESIAN_POINT('Ctrl Pts',(-0.964935899959919,-2.34627612572969,
15.7835667783414));
#12425=CARTESIAN_POINT('Ctrl Pts',(1.44718260939238,-2.0836927422902,15.9105369855953));
#12426=CARTESIAN_POINT('Ctrl Pts',(2.53552873347685,0.0848939981029082,
16.0375071928491));
#12427=CARTESIAN_POINT('Ctrl Pts',(1.30456636280332,2.17582617739623,16.164477400103));
#12428=CARTESIAN_POINT('Ctrl Pts',(-1.11971391717911,2.27647835326322,16.2914476073569));
#12429=CARTESIAN_POINT('Ctrl Pts',(-2.51976522056811,0.294781584255081,
16.4184178146108));
#12430=CARTESIAN_POINT('Ctrl Pts',(-1.61492728973195,-1.95655891761011,
16.5453880218647));
#12431=CARTESIAN_POINT('Ctrl Pts',(0.767123078904428,-2.41818839857708,
16.6723582291185));
#12432=CARTESIAN_POINT('Ctrl Pts',(2.4474677046963,-0.667843382589994,16.7993284363725));
#12433=CARTESIAN_POINT('Ctrl Pts',(1.88905535518695,1.69339387451358,16.9262986436263));
#12434=CARTESIAN_POINT('Ctrl Pts',(-0.397320899643744,2.5056434406968,17.0532688508803));
#12435=CARTESIAN_POINT('Ctrl Pts',(-2.32025826872181,1.02592130089431,17.1802390581341));
#12436=CARTESIAN_POINT('Ctrl Pts',(-2.12080016200509,-1.39223547650525,
17.307209265388));
#12437=CARTESIAN_POINT('Ctrl Pts',(0.0186043418789166,-2.53688131919171,
17.4341794726419));
#12438=CARTESIAN_POINT('Ctrl Pts',(2.14099101134067,-1.36098142476636,17.5611496798958));
#12439=CARTESIAN_POINT('Ctrl Pts',(2.30496223307299,1.05984057919471,17.6881198871497));
#12440=CARTESIAN_POINT('Ctrl Pts',(0.360529626964672,2.51120117419559,17.8150900944035));
#12441=CARTESIAN_POINT('Ctrl Pts',(-1.91368801190267,1.66550627206883,17.9420603016574));
#12442=CARTESIAN_POINT('Ctrl Pts',(-2.43740966793167,-0.703666867113844,
18.0690305089113));
#12443=CARTESIAN_POINT('Ctrl Pts',(-0.731574674335433,-2.42917917105174,
18.1960007161652));
#12444=CARTESIAN_POINT('Ctrl Pts',(1.64344909016039,-1.93266345680038,18.3229709234191));
#12445=CARTESIAN_POINT('Ctrl Pts',(2.51517084699783,0.33170553147752,18.449941130673));
#12446=CARTESIAN_POINT('Ctrl Pts',(1.08620595249116,2.2926555733414,18.5769113379269));
#12447=CARTESIAN_POINT('Ctrl Pts',(-1.33633738559912,2.15645898200052,18.7038815451807));
#12448=CARTESIAN_POINT('Ctrl Pts',(-2.53650110347004,0.0476980219282782,
18.8308517524346));
#12449=CARTESIAN_POINT('Ctrl Pts',(-1.41646687660141,-2.10469345432813,
18.9578219596885));
#12450=CARTESIAN_POINT('Ctrl Pts',(0.999243323514884,-2.33187172237487,
19.0847921669424));
#12451=CARTESIAN_POINT('Ctrl Pts',(2.50092186705419,-0.426031412093869,
19.2117623741963));
#12452=CARTESIAN_POINT('Ctrl Pts',(1.71494764042323,1.86950997317682,19.3387325814502));
#12453=CARTESIAN_POINT('Ctrl Pts',(-0.639730019927018,2.45496607935927,
19.4657027887041));
#12454=CARTESIAN_POINT('Ctrl Pts',(-2.40923140127119,0.794806268425853,
19.592672995958));
#12455=CARTESIAN_POINT('Ctrl Pts',(-1.97495146433281,-1.59238175784946,
19.7196432032118));
#12456=CARTESIAN_POINT('Ctrl Pts',(0.265863593855321,-2.52298028106869,
19.8466134104657));
#12457=CARTESIAN_POINT('Ctrl Pts',(2.26348689344177,-1.14574867768449,19.9735836177196));
#12458=CARTESIAN_POINT('Ctrl Pts',(2.19064484573673,1.27952651752807,20.1005538249735));
#12459=CARTESIAN_POINT('Ctrl Pts',(0.113967805887229,2.53438834601358,20.2275240322274));
#12460=CARTESIAN_POINT('Ctrl Pts',(-2.06695829917982,1.47098481931061,20.3544942394812));
#12461=CARTESIAN_POINT('Ctrl Pts',(-2.35718844081557,-0.93796354073691,
20.4814644467352));
#12462=CARTESIAN_POINT('Ctrl Pts',(-0.491242199024368,-2.48893432034654,
20.608434653989));
#12463=CARTESIAN_POINT('Ctrl Pts',(1.82405497693622,-1.76321762419793,20.7354048612429));
#12464=CARTESIAN_POINT('Ctrl Pts',(2.47084564113251,0.575356209078461,20.8623750684968));
#12465=CARTESIAN_POINT('Ctrl Pts',(0.857494974763876,2.38763802044798,20.9893452757507));
#12466=CARTESIAN_POINT('Ctrl Pts',(-1.5402267585474,2.01589049342632,21.1163154830046));
#12467=CARTESIAN_POINT('Ctrl Pts',(-2.52906640922887,-0.199840060113828,
21.2432856902585));
#12468=CARTESIAN_POINT('Ctrl Pts',(-1.20450880521207,-2.23277215175221,
21.3702558975124));
#12469=CARTESIAN_POINT('Ctrl Pts',(1.22184167477557,-2.22333440421579,21.4972261047662));
#12470=CARTESIAN_POINT('Ctrl Pts',(2.53054449342564,-0.180159742062507,
21.6241963120202));
#12471=CARTESIAN_POINT('Ctrl Pts',(1.52449800808261,2.02781131540755,21.751166519274));
#12472=CARTESIAN_POINT('Ctrl Pts',(-0.876043074960227,2.38089510597715,
21.8781367265279));
#12473=CARTESIAN_POINT('Ctrl Pts',(-2.47524674625411,0.556117426851564,
22.0051069337818));
#12474=CARTESIAN_POINT('Ctrl Pts',(-1.81028320685765,-1.77735403461849,
22.1320771410357));
#12475=CARTESIAN_POINT('Ctrl Pts',(0.510589317071444,-2.48503757599162,
22.2590473482895));
#12476=CARTESIAN_POINT('Ctrl Pts',(2.36441394472454,-0.919597842451947,
22.3860175555435));
#12477=CARTESIAN_POINT('Ctrl Pts',(2.05545226302454,1.48701946547234,22.5129877627973));
#12478=CARTESIAN_POINT('Ctrl Pts',(-0.133679421764624,2.53342555231595,
22.6399579700512));
#12479=CARTESIAN_POINT('Ctrl Pts',(-2.2005334809403,1.26244528907117,22.7669281773051));
#12480=CARTESIAN_POINT('Ctrl Pts',(-2.25450313277747,-1.16332052498233,
22.893898384559));
#12481=CARTESIAN_POINT('Ctrl Pts',(-0.24623280137769,-2.52497547307231,
23.0208685918128));
#12482=CARTESIAN_POINT('Ctrl Pts',(1.98728720880323,-1.57696360245516,23.1478387990668));
#12483=CARTESIAN_POINT('Ctrl Pts',(2.40296035204267,0.813512243486801,23.2748090063206));
#12484=CARTESIAN_POINT('Ctrl Pts',(0.620641681303831,2.45989130526442,23.4017792135745));
#12485=CARTESIAN_POINT('Ctrl Pts',(-1.72949408454599,1.85606879455694,23.5287494208284));
#12486=CARTESIAN_POINT('Ctrl Pts',(-2.49742735891751,-0.445390834118454,
23.6557196280823));
#12487=CARTESIAN_POINT('Ctrl Pts',(-0.981272150962877,-2.33973265854723,
23.7826898353362));
#12488=CARTESIAN_POINT('Ctrl Pts',(1.43317690604497,-2.0933093666771,23.9096600425901));
#12489=CARTESIAN_POINT('Ctrl Pts',(2.53532670541879,0.0668531815795256,
24.036630249844));
#12490=CARTESIAN_POINT('Ctrl Pts',(1.32093101838195,2.16789927381241,24.1636004570979));
#12491=CARTESIAN_POINT('Ctrl Pts',(-1.10691612547992,2.28190328259405,24.2905706643517));
#12492=CARTESIAN_POINT('Ctrl Pts',(-2.04256487369668,0.972257736519369,
24.3752174691877));
#12493=CARTESIAN_POINT('Ctrl Pts',(-2.13035745341128,0.264111526580659,
24.4175408716056));
#12494=CARTESIAN_POINT('Ctrl Pts',(1.160348984669,-1.62253437445178,0.));
#12495=CARTESIAN_POINT('Ctrl Pts',(1.69969113399867,-1.23682598810383,0.0423234024179621));
#12496=CARTESIAN_POINT('Ctrl Pts',(2.35424863102644,0.107968028363325,0.126970207253886));
#12497=CARTESIAN_POINT('Ctrl Pts',(1.18456011268651,2.03999555013175,0.253940414507772));
#12498=CARTESIAN_POINT('Ctrl Pts',(-1.06966068457706,2.09999381115058,0.380910621761658));
#12499=CARTESIAN_POINT('Ctrl Pts',(-2.34491827036033,0.242085824504435,
0.507880829015544));
#12500=CARTESIAN_POINT('Ctrl Pts',(-1.47549600675849,-1.83882695427017,
0.634851036269431));
#12501=CARTESIAN_POINT('Ctrl Pts',(0.743740789408913,-2.23690209703098,
0.761821243523316));
#12502=CARTESIAN_POINT('Ctrl Pts',(2.28258498544192,-0.589259358513722,
0.888791450777202));
#12503=CARTESIAN_POINT('Ctrl Pts',(1.73353383587625,1.59761854395386,1.01576165803109));
#12504=CARTESIAN_POINT('Ctrl Pts',(-0.401242712543095,2.32299828124824,
1.14273186528497));
#12505=CARTESIAN_POINT('Ctrl Pts',(-2.16898211541349,0.923538379768288,
1.26970207253886));
#12506=CARTESIAN_POINT('Ctrl Pts',(-1.95270765604849,-1.32073671783877,
1.39667227979275));
#12507=CARTESIAN_POINT('Ctrl Pts',(0.0497579841286025,-2.35688535243524,
1.52364248704663));
#12508=CARTESIAN_POINT('Ctrl Pts',(2.00670723621032,-1.23714384781738,1.65061269430052));
#12509=CARTESIAN_POINT('Ctrl Pts',(2.1280744337024,1.01424731308453,1.77758290155441));
#12510=CARTESIAN_POINT('Ctrl Pts',(0.302840850211159,2.33787982927957,1.90455310880829));
#12511=CARTESIAN_POINT('Ctrl Pts',(-1.79940824053038,1.52299931173928,2.03152331606218));
#12512=CARTESIAN_POINT('Ctrl Pts',(-2.25569589565051,-0.685005617790214,
2.15849352331606));
#12513=CARTESIAN_POINT('Ctrl Pts',(-0.648644751766769,-2.26641924187756,
2.28546373056995));
#12514=CARTESIAN_POINT('Ctrl Pts',(1.55173715555782,-1.77468541835342,2.41243393782384));
#12515=CARTESIAN_POINT('Ctrl Pts',(2.33270816248269,0.340395505542482,2.53940414507772));
#12516=CARTESIAN_POINT('Ctrl Pts',(0.979895470300759,2.14410850487368,2.66637435233161));
#12517=CARTESIAN_POINT('Ctrl Pts',(-1.2692509317393,1.98655443822406,2.7933445595855));
#12518=CARTESIAN_POINT('Ctrl Pts',(-2.35738329251264,0.0118517195461532,
2.92031476683938));
#12519=CARTESIAN_POINT('Ctrl Pts',(-1.28916103309304,-1.97369204162334,
3.04728497409327));
#12520=CARTESIAN_POINT('Ctrl Pts',(0.958287513109827,-2.15385270943036,
3.17425518134715));
#12521=CARTESIAN_POINT('Ctrl Pts',(2.32916765789381,-0.363833025997572,
3.30122538860104));
#12522=CARTESIAN_POINT('Ctrl Pts',(1.56950269631471,1.75899338684286,3.42819559585493));
#12523=CARTESIAN_POINT('Ctrl Pts',(-0.6258237459619,2.27282667370784,3.55516580310881));
#12524=CARTESIAN_POINT('Ctrl Pts',(-2.24869430914181,0.70765129362066,3.68213601036269));
#12525=CARTESIAN_POINT('Ctrl Pts',(-1.8146306540197,-1.50482957133494,3.80910621761659));
#12526=CARTESIAN_POINT('Ctrl Pts',(0.279318860454586,-2.34080700264011,
3.93607642487046));
#12527=CARTESIAN_POINT('Ctrl Pts',(2.11776876365419,-1.03559254199705,4.06304663212436));
#12528=CARTESIAN_POINT('Ctrl Pts',(2.01904516192129,1.21690307069604,4.19001683937824));
#12529=CARTESIAN_POINT('Ctrl Pts',(0.0734528840375746,2.35626847434518,
4.31698704663213));
#12530=CARTESIAN_POINT('Ctrl Pts',(-1.93932849553776,1.34029900983,4.44395725388601));
#12531=CARTESIAN_POINT('Ctrl Pts',(-2.17815993148116,-0.901673866897921,
4.5709274611399));
#12532=CARTESIAN_POINT('Ctrl Pts',(-0.424576623578355,-2.31886419181245,
4.69789766839378));
#12533=CARTESIAN_POINT('Ctrl Pts',(1.71737702962559,-1.61493423626845,4.82486787564767));
#12534=CARTESIAN_POINT('Ctrl Pts',(2.28840502897144,0.566214511237573,4.95183808290156));
#12535=CARTESIAN_POINT('Ctrl Pts',(0.766174469238656,2.22943336568846,5.07880829015544));
#12536=CARTESIAN_POINT('Ctrl Pts',(-1.45689411749422,1.8533364453786,5.20577849740933));
#12537=CARTESIAN_POINT('Ctrl Pts',(-2.34730697130079,-0.218051443106043,
5.33274870466322));
#12538=CARTESIAN_POINT('Ctrl Pts',(-1.09058225712671,-2.08998248552431,
5.4597189119171));
#12539=CARTESIAN_POINT('Ctrl Pts',(1.16372401066593,-2.05015679311548,5.58668911917098));
#12540=CARTESIAN_POINT('Ctrl Pts',(2.35354422162328,-0.13500387483914,5.71365932642487));
#12541=CARTESIAN_POINT('Ctrl Pts',(1.39052150324245,1.903640301732,5.84062953367876));
#12542=CARTESIAN_POINT('Ctrl Pts',(-0.844444337704187,2.20097937515945,
5.96759974093265));
#12543=CARTESIAN_POINT('Ctrl Pts',(-2.30697683962809,0.485030216355141,
6.09456994818653));
#12544=CARTESIAN_POINT('Ctrl Pts',(-1.65926270513453,-1.67458762825586,
6.22154015544043));
#12545=CARTESIAN_POINT('Ctrl Pts',(0.506218527102226,-2.3024203031107,6.3485103626943));
#12546=CARTESIAN_POINT('Ctrl Pts',(2.20864962127088,-0.824174313976057,
6.4754805699482));
#12547=CARTESIAN_POINT('Ctrl Pts',(1.8907763264874,1.40796354091743,6.60245077720207));
#12548=CARTESIAN_POINT('Ctrl Pts',(-0.156635087036384,2.35220362614869,
6.72942098445597));
#12549=CARTESIAN_POINT('Ctrl Pts',(-2.06076865750355,1.14482705663735,6.85639119170984));
#12550=CARTESIAN_POINT('Ctrl Pts',(-2.07986807711532,-1.10975007598764,
6.98336139896374));
#12551=CARTESIAN_POINT('Ctrl Pts',(-0.1964626520611,-2.34921239476192,7.11033160621761));
#12552=CARTESIAN_POINT('Ctrl Pts',(1.86665183793563,-1.43979420935406,7.23730181347151));
#12553=CARTESIAN_POINT('Ctrl Pts',(2.22229545319173,0.786638015914119,7.36427202072539));
#12554=CARTESIAN_POINT('Ctrl Pts',(0.54515251217721,2.29351372087127,7.49124222797928));
#12555=CARTESIAN_POINT('Ctrl Pts',(-1.63065440993819,1.70245782464854,7.61821243523317));
#12556=CARTESIAN_POINT('Ctrl Pts',(-2.31486292299194,-0.445876773464548,
7.74518264248704));
#12557=CARTESIAN_POINT('Ctrl Pts',(-0.8816112114347,-2.18635727209223,7.87215284974095));
#12558=CARTESIAN_POINT('Ctrl Pts',(1.35807126336241,-1.92692472426588,7.99912305699481));
#12559=CARTESIAN_POINT('Ctrl Pts',(2.35549362254096,0.0951117423181714,
8.12609326424872));
#12560=CARTESIAN_POINT('Ctrl Pts',(1.19828988895336,2.03014723391927,8.25306347150259));
#12561=CARTESIAN_POINT('Ctrl Pts',(-1.05501813323409,2.10815871980864,8.38003367875648));
#12562=CARTESIAN_POINT('Ctrl Pts',(-2.34327595258744,0.257787236657217,
8.50700388601036));
#12563=CARTESIAN_POINT('Ctrl Pts',(-1.48808347274196,-1.8283883688949,8.63397409326426));
#12564=CARTESIAN_POINT('Ctrl Pts',(0.72829438578655,-2.24209360575996,8.76094430051814));
#12565=CARTESIAN_POINT('Ctrl Pts',(2.27848403144356,-0.604902444874099,
8.88791450777203));
#12566=CARTESIAN_POINT('Ctrl Pts',(1.74449009064557,1.58560738299156,9.01488471502591));
#12567=CARTESIAN_POINT('Ctrl Pts',(-0.385230466394427,2.32572438975891,
9.1418549222798));
#12568=CARTESIAN_POINT('Ctrl Pts',(-2.1625715448067,0.938445929689231,9.26882512953368));
#12569=CARTESIAN_POINT('Ctrl Pts',(-1.96175694776964,-1.30725136344754,
9.39579533678757));
#12570=CARTESIAN_POINT('Ctrl Pts',(0.0335234320998379,-2.35717471326548,
9.52276554404145));
#12571=CARTESIAN_POINT('Ctrl Pts',(1.99813913054961,-1.25093423661054,9.64973575129535));
#12572=CARTESIAN_POINT('Ctrl Pts',(2.13500939744307,0.999565566727712,9.77670595854921));
#12573=CARTESIAN_POINT('Ctrl Pts',(0.318935741240959,2.33573894995075,9.90367616580313));
#12574=CARTESIAN_POINT('Ctrl Pts',(-1.78887603024087,1.53535630971693,10.030646373057));
#12575=CARTESIAN_POINT('Ctrl Pts',(-2.26036030985581,-0.669453298585103,
10.1576165803109));
#12576=CARTESIAN_POINT('Ctrl Pts',(-0.664239202615746,-2.26189803728336,
10.2845867875648));
#12577=CARTESIAN_POINT('Ctrl Pts',(1.53947731651516,-1.78533079324062,10.4115569948187));
#12578=CARTESIAN_POINT('Ctrl Pts',(2.33499728455247,0.32432102998492,10.5385272020725));
#12579=CARTESIAN_POINT('Ctrl Pts',(0.994639648129273,2.13730868611139,10.6654974093264));
#12580=CARTESIAN_POINT('Ctrl Pts',(-1.25553855339793,1.9952492050592,10.7924676165803));
#12581=CARTESIAN_POINT('Ctrl Pts',(-2.35724575006339,0.028087776096,10.9194378238342));
#12582=CARTESIAN_POINT('Ctrl Pts',(-1.30272414120579,-1.96476621033587,
11.0464080310881));
#12583=CARTESIAN_POINT('Ctrl Pts',(0.943430253008483,-2.16040176982576,
11.173378238342));
#12584=CARTESIAN_POINT('Ctrl Pts',(2.32660653495589,-0.379866398696293,
11.3003484455959));
#12585=CARTESIAN_POINT('Ctrl Pts',(1.58158043085374,1.74814181063735,11.4273186528497));
#12586=CARTESIAN_POINT('Ctrl Pts',(-0.610154945358331,2.27708308851757,
11.5542888601037));
#12587=CARTESIAN_POINT('Ctrl Pts',(-2.24376706735364,0.723122255788841,
11.6812590673575));
#12588=CARTESIAN_POINT('Ctrl Pts',(-1.82495203643891,-1.4922957193718,11.8082292746114));
#12589=CARTESIAN_POINT('Ctrl Pts',(0.263190068058092,-2.34267527357795,
11.9351994818653));
#12590=CARTESIAN_POINT('Ctrl Pts',(2.11058595164912,-1.05015398397536,12.0621696891192));
#12591=CARTESIAN_POINT('Ctrl Pts',(2.0273786194508,1.20296815533566,12.1891398963731));
#12592=CARTESIAN_POINT('Ctrl Pts',(0.0896797991062791,2.35570668441345,
12.316110103627));
#12593=CARTESIAN_POINT('Ctrl Pts',(-1.93005126844934,1.35362422795805,12.4430803108808));
#12594=CARTESIAN_POINT('Ctrl Pts',(-2.18431849285034,-0.886650534962871,
12.5700505181347));
#12595=CARTESIAN_POINT('Ctrl Pts',(-0.440537590706227,-2.31588494544368,
12.6970207253886));
#12596=CARTESIAN_POINT('Ctrl Pts',(1.70621353334662,-1.62672426304606,12.8239909326425));
#12597=CARTESIAN_POINT('Ctrl Pts',(2.29225051935244,0.550439829487665,12.9509611398964));
#12598=CARTESIAN_POINT('Ctrl Pts',(0.781511384680127,2.22410350590373,13.0779313471503));
#12599=CARTESIAN_POINT('Ctrl Pts',(-1.44409481866595,1.86332675718997,13.2049015544042));
#12600=CARTESIAN_POINT('Ctrl Pts',(-2.34875311243137,-0.201879335747595,
13.331871761658));
#12601=CARTESIAN_POINT('Ctrl Pts',(-1.10495101849633,-2.08242159422195,
13.4588419689119));
#12602=CARTESIAN_POINT('Ctrl Pts',(1.14957607715301,-2.05812324514239,13.5858121761658));
#12603=CARTESIAN_POINT('Ctrl Pts',(2.35255856756512,-0.151210566872388,
13.7127823834197));
#12604=CARTESIAN_POINT('Ctrl Pts',(1.40359972987109,1.894018016721,13.8397525906736));
#12605=CARTESIAN_POINT('Ctrl Pts',(-0.829265195633706,2.20674323034388,
13.9667227979275));
#12606=CARTESIAN_POINT('Ctrl Pts',(-2.30358150473097,0.500907876180168,
14.0936930051813));
#12607=CARTESIAN_POINT('Ctrl Pts',(-1.67075697107245,-1.66311983722483,
14.2206632124353));
#12608=CARTESIAN_POINT('Ctrl Pts',(0.490348739021751,-2.30585224233855,
14.3476334196891));
#12609=CARTESIAN_POINT('Ctrl Pts',(2.20292078401032,-0.839366706948347,
14.474603626943));
#12610=CARTESIAN_POINT('Ctrl Pts',(1.90042874387294,1.39490753773124,14.6015738341969));
#12611=CARTESIAN_POINT('Ctrl Pts',(-0.140430710978244,2.35322664968167,
14.7285440414508));
#12612=CARTESIAN_POINT('Ctrl Pts',(-2.05283485132384,1.15899332290923,14.8555142487047));
#12613=CARTESIAN_POINT('Ctrl Pts',(-2.08746208220335,-1.095398787986,14.9824844559586));
#12614=CARTESIAN_POINT('Ctrl Pts',(-0.21263805117564,-2.34780354982058,
15.1094546632124));
#12615=CARTESIAN_POINT('Ctrl Pts',(1.85669106744545,-1.45261651148066,15.2364248704663));
#12616=CARTESIAN_POINT('Ctrl Pts',(2.22766066522509,0.771313431729834,15.3633950777202));
#12617=CARTESIAN_POINT('Ctrl Pts',(0.560936019559882,2.28970461660849,15.4903652849741));
#12618=CARTESIAN_POINT('Ctrl Pts',(-1.61889015716034,1.71364847865813,15.617335492228));
#12619=CARTESIAN_POINT('Ctrl Pts',(-2.31787896690132,-0.429922718816292,
15.7443056994818));
#12620=CARTESIAN_POINT('Ctrl Pts',(-0.896648704865739,-2.18023337040339,
15.8712759067358));
#12621=CARTESIAN_POINT('Ctrl Pts',(1.34476747364227,-1.93623265420035,15.9982461139896));
#12622=CARTESIAN_POINT('Ctrl Pts',(2.35609282970634,0.0788861658613507,
16.1252163212435));
#12623=CARTESIAN_POINT('Ctrl Pts',(1.21224398394502,2.02184593200051,16.2521865284974));
#12624=CARTESIAN_POINT('Ctrl Pts',(-1.04047329330418,2.11537509091856,16.3791567357513));
#12625=CARTESIAN_POINT('Ctrl Pts',(-2.34144487906595,0.273920294344516,
16.5061269430052));
#12626=CARTESIAN_POINT('Ctrl Pts',(-1.50064109217059,-1.81809591656959,
16.6330971502591));
#12627=CARTESIAN_POINT('Ctrl Pts',(0.712834826853045,-2.24705650996661,
16.760067357513));
#12628=CARTESIAN_POINT('Ctrl Pts',(2.27426375960074,-0.620581018985151,
16.8870375647669));
#12629=CARTESIAN_POINT('Ctrl Pts',(1.75536948901827,1.57355470396859,17.0140077720207));
#12630=CARTESIAN_POINT('Ctrl Pts',(-0.36920304249889,2.32832247825929,17.1409779792746));
#12631=CARTESIAN_POINT('Ctrl Pts',(-2.1560567615836,0.953318252310089,17.2679481865285));
#12632=CARTESIAN_POINT('Ctrl Pts',(-1.9707140325278,-1.29370887426652,17.3949183937824));
#12633=CARTESIAN_POINT('Ctrl Pts',(0.0172877380261932,-2.35734969477841,
17.5218886010363));
#12634=CARTESIAN_POINT('Ctrl Pts',(1.98947600304585,-1.26466662906185,17.6488588082902));
#12635=CARTESIAN_POINT('Ctrl Pts',(2.14184320547626,0.984837109634436,17.775829015544));
#12636=CARTESIAN_POINT('Ctrl Pts',(0.335015437913597,2.33348689855279,17.902799222798));
#12637=CARTESIAN_POINT('Ctrl Pts',(-1.7782589262777,1.54764066904162,18.0297694300518));
#12638=CARTESIAN_POINT('Ctrl Pts',(-2.26491751635406,-0.653869324460531,
18.1567396373057));
#12639=CARTESIAN_POINT('Ctrl Pts',(-0.679802134300005,-2.25726948049166,
18.2837098445596));
#12640=CARTESIAN_POINT('Ctrl Pts',(1.52714444375655,-1.79589150486922,18.4106800518135));
#12641=CARTESIAN_POINT('Ctrl Pts',(2.33717564303521,0.30823118427704,18.5376502590674));
#12642=CARTESIAN_POINT('Ctrl Pts',(1.00933664148997,2.13040747123729,18.6646204663213));
#12643=CARTESIAN_POINT('Ctrl Pts',(-1.24176661487133,2.00384932655849,18.7915906735751));
#12644=CARTESIAN_POINT('Ctrl Pts',(-2.35699638640381,0.0443224980938706,
18.918560880829));
#12645=CARTESIAN_POINT('Ctrl Pts',(-1.31622545128915,-1.95574717454394,
19.0455310880829));
#12646=CARTESIAN_POINT('Ctrl Pts',(0.928528238935361,-2.16684834699098,
19.1725012953368));
#12647=CARTESIAN_POINT('Ctrl Pts',(2.32393504393153,-0.395881751214744,
19.2994715025907));
#12648=CARTESIAN_POINT('Ctrl Pts',(1.59358313931722,1.73720730698498,19.4264417098446));
#12649=CARTESIAN_POINT('Ctrl Pts',(-0.594457200581991,2.28123148453506,
19.5534119170984));
#12650=CARTESIAN_POINT('Ctrl Pts',(-2.23873338712067,0.738558914880064,
19.6803821243523));
#12651=CARTESIAN_POINT('Ctrl Pts',(-1.83518684789343,-1.47969107677181,
19.8073523316062));
#12652=CARTESIAN_POINT('Ctrl Pts',(0.247048790610012,-2.34443241412816,
19.9343225388601));
#12653=CARTESIAN_POINT('Ctrl Pts',(2.10330301895634,-1.0646656093841,20.061292746114));
#12654=CARTESIAN_POINT('Ctrl Pts',(2.0356159034317,1.18897617430391,20.1882629533679));
#12655=CARTESIAN_POINT('Ctrl Pts',(0.10590245999703,2.35503314590555,20.3152331606218));
#12656=CARTESIAN_POINT('Ctrl Pts',(-1.92068248476191,1.36688523368939,20.4422033678757));
#12657=CARTESIAN_POINT('Ctrl Pts',(-2.1903734358619,-0.871585142648238,
20.5691735751295));
#12658=CARTESIAN_POINT('Ctrl Pts',(-0.456477659862079,-2.31279583952387,
20.6961437823834));
#12659=CARTESIAN_POINT('Ctrl Pts',(1.6949690987159,-1.63843712229916,20.8231139896373));
#12660=CARTESIAN_POINT('Ctrl Pts',(2.29598727142038,0.534639036362976,20.9500841968912));
#12661=CARTESIAN_POINT('Ctrl Pts',(0.796811227132131,2.21866814035183,21.0770544041451));
#12662=CARTESIAN_POINT('Ctrl Pts',(-1.43122701550266,1.87322867783953,21.204024611399));
#12663=CARTESIAN_POINT('Ctrl Pts',(-2.35008783531489,-0.185697652132911,
21.3309948186529));
#12664=CARTESIAN_POINT('Ctrl Pts',(-1.1192673629799,-2.07476191756569,21.4579650259067));
#12665=CARTESIAN_POINT('Ctrl Pts',(1.13537360904899,-2.06599206652615,21.5849352331606));
#12666=CARTESIAN_POINT('Ctrl Pts',(2.3514613175128,-0.167410083297791,21.7119054404145));
#12667=CARTESIAN_POINT('Ctrl Pts',(1.41661136721561,1.88430587953843,21.8388756476684));
#12668=CARTESIAN_POINT('Ctrl Pts',(-0.814046703622753,2.21240241272419,
21.9658458549223));
#12669=CARTESIAN_POINT('Ctrl Pts',(-2.30007691634645,0.516761756465324,
22.0928160621762));
#12670=CARTESIAN_POINT('Ctrl Pts',(-1.68217193798728,-1.65157311827105,
22.2197862694301));
#12671=CARTESIAN_POINT('Ctrl Pts',(0.474455608801953,-2.30917486244222,
22.3467564766839));
#12672=CARTESIAN_POINT('Ctrl Pts',(2.19708760073256,-0.854519159734979,
22.4737266839378));
#12673=CARTESIAN_POINT('Ctrl Pts',(1.90999071506285,1.3817851298529,22.6006968911917));
#12674=CARTESIAN_POINT('Ctrl Pts',(-0.124219111753841,2.35413848780229,
22.7276670984456));
#12675=CARTESIAN_POINT('Ctrl Pts',(-2.0448047334343,1.17310376104416,22.8546373056995));
#12676=CARTESIAN_POINT('Ctrl Pts',(-2.09495502675834,-1.08099392105983,
22.9816075129534));
#12677=CARTESIAN_POINT('Ctrl Pts',(-0.228807242491405,-2.34628640912002,
23.1085777202073));
#12678=CARTESIAN_POINT('Ctrl Pts',(1.84664960858395,-1.46536404316653,23.2355479274611));
#12679=CARTESIAN_POINT('Ctrl Pts',(2.23290613147693,0.755941093646845,23.3625181347151));
#12680=CARTESIAN_POINT('Ctrl Pts',(0.576719717599789,2.28580815893301,23.4894883419689));
#12681=CARTESIAN_POINT('Ctrl Pts',(-1.60710015146648,1.72471734220924,23.6164585492229));
#12682=CARTESIAN_POINT('Ctrl Pts',(-2.32068783736058,-0.413871133396448,
23.7434287564766));
#12683=CARTESIAN_POINT('Ctrl Pts',(-0.911828861708041,-2.17415297545205,
23.8703989637307));
#12684=CARTESIAN_POINT('Ctrl Pts',(1.33175293478252,-1.94516872322012,23.9973691709844));
#12685=CARTESIAN_POINT('Ctrl Pts',(2.35590509889789,0.0621220732712832,
24.1243393782384));
#12686=CARTESIAN_POINT('Ctrl Pts',(1.22745053520999,2.01448000455152,24.2513095854922));
#12687=CARTESIAN_POINT('Ctrl Pts',(-1.02858118383587,2.12041610541359,24.3782797927461));
#12688=CARTESIAN_POINT('Ctrl Pts',(-1.89801534866759,0.903452385056865,
24.4629265975821));
#12689=CARTESIAN_POINT('Ctrl Pts',(-1.97959496748082,0.245420714742313,
24.50525));
#12690=CARTESIAN_POINT('',(1.16034898466906,-1.62253437445173,0.));
#12691=CARTESIAN_POINT('Ctrl Pts',(1.160348984669,-1.62253437445178,0.));
#12692=CARTESIAN_POINT('Ctrl Pts',(1.69969113399867,-1.23682598810383,0.0423234024179621));
#12693=CARTESIAN_POINT('Ctrl Pts',(2.35424863102644,0.107968028363325,0.126970207253886));
#12694=CARTESIAN_POINT('Ctrl Pts',(1.18456011268651,2.03999555013175,0.253940414507772));
#12695=CARTESIAN_POINT('Ctrl Pts',(-1.06966068457706,2.09999381115058,0.380910621761658));
#12696=CARTESIAN_POINT('Ctrl Pts',(-1.9636032657455,0.797619232342793,0.469915444057474));
#12697=CARTESIAN_POINT('Ctrl Pts',(-1.99761127318624,0.0693315477139227,
0.516596863935328));
#12698=CARTESIAN_POINT('Ctrl Pts',(-1.99714087507904,0.00129381383500625,
0.52095488139522));
#12699=CARTESIAN_POINT('Ctrl Pts',(1.07765127757231,2.20530172674001,7.97972798949331E-17));
#12700=CARTESIAN_POINT('Ctrl Pts',(1.12809639271741,2.17510065728148,6.86960599404408E-17));
#12701=CARTESIAN_POINT('Ctrl Pts',(1.17730025765894,2.14300509491081,1.10309490283818E-16));
#12702=CARTESIAN_POINT('Ctrl Pts',(1.22514132390505,2.1090085670223,1.26634813746307E-16));
#12703=CARTESIAN_POINT('Ctrl Pts',(1.29462421705668,2.05963305555998,1.57121996985627E-16));
#12704=CARTESIAN_POINT('Ctrl Pts',(1.36123441505861,2.00624872602741,1.84001859055496E-16));
#12705=CARTESIAN_POINT('Ctrl Pts',(1.42480302814056,1.94921747509588,1.31838984174237E-16));
#12706=CARTESIAN_POINT('Ctrl Pts',(1.45690053415869,1.92042085941958,1.05500542776029E-16));
#12707=CARTESIAN_POINT('Ctrl Pts',(1.48822193239482,1.89069393167789,-1.71410280842816E-16));
#12708=CARTESIAN_POINT('Ctrl Pts',(1.51874122959272,1.86008072957315,-2.1163626406917E-16));
#12709=CARTESIAN_POINT('Ctrl Pts',(1.53250999529149,1.84626959872253,-2.29784196325102E-16));
#12710=CARTESIAN_POINT('Ctrl Pts',(1.54611546415791,1.83227806106527,-6.87915904046554E-17));
#12711=CARTESIAN_POINT('Ctrl Pts',(1.55955504465434,1.81811008308972,-8.32667268468867E-17));
#12712=CARTESIAN_POINT('Ctrl Pts',(1.57081510549093,1.80623975023383,-9.53944057577452E-17));
#12713=CARTESIAN_POINT('Ctrl Pts',(1.5819588119139,1.79424531325038,-9.69640209386679E-17));
#12714=CARTESIAN_POINT('Ctrl Pts',(1.59297464935461,1.7821404241451,-1.17961196366423E-16));
#12715=CARTESIAN_POINT('Ctrl Pts',(1.65014233615335,1.7193210050289,-2.26927941289128E-16));
#12716=CARTESIAN_POINT('Ctrl Pts',(1.70393951009346,1.65345682333213,-6.05899575447923E-16));
#12717=CARTESIAN_POINT('Ctrl Pts',(1.75419867452451,1.58490693773027,-5.20417042793042E-16));
#12718=CARTESIAN_POINT('Ctrl Pts',(1.79330135022385,1.53157370037424,-4.53909853702211E-16));
#12719=CARTESIAN_POINT('Ctrl Pts',(1.83026160943548,1.47661394117244,-5.4299838061594E-16));
#12720=CARTESIAN_POINT('Ctrl Pts',(1.86498033301496,1.42018860836785,-6.45317133063372E-16));
#12721=CARTESIAN_POINT('Ctrl Pts',(1.88104710033835,1.39407668373901,-6.92667133838316E-16));
#12722=CARTESIAN_POINT('Ctrl Pts',(1.89663356986419,1.3676508303538,-1.30333522663486E-16));
#12723=CARTESIAN_POINT('Ctrl Pts',(1.91172852635572,1.34092677154389,-1.52655665885959E-16));
#12724=CARTESIAN_POINT('Ctrl Pts',(1.9192190540249,1.32766556724293,-1.63732520035034E-16));
#12725=CARTESIAN_POINT('Ctrl Pts',(1.92658853680698,1.31433093124829,-4.1258915407781E-16));
#12726=CARTESIAN_POINT('Ctrl Pts',(1.93383552001789,1.30092478157845,-4.30211422042248E-16));
#12727=CARTESIAN_POINT('Ctrl Pts',(1.9407073591395,1.28821260865211,-4.46921463570597E-16));
#12728=CARTESIAN_POINT('Ctrl Pts',(1.94746478045741,1.27544399500121,-6.09762297626216E-16));
#12729=CARTESIAN_POINT('Ctrl Pts',(1.95410541003034,1.26262383458428,-5.82867087928207E-16));
#12730=CARTESIAN_POINT('Ctrl Pts',(1.99234448003475,1.18880086248997,-4.27995054315904E-16));
#12731=CARTESIAN_POINT('Ctrl Pts',(2.0267328516625,1.11323685926757,-3.04131430563134E-16));
#12732=CARTESIAN_POINT('Ctrl Pts',(2.05710895345793,1.03626323191291,-2.77555756156289E-16));
#12733=CARTESIAN_POINT('Ctrl Pts',(2.08682191459507,0.960970015766318,-2.51560255279913E-16));
#12734=CARTESIAN_POINT('Ctrl Pts',(2.11269600419783,0.884327115080494,-2.74271135208625E-16));
#12735=CARTESIAN_POINT('Ctrl Pts',(2.13453193486002,0.806636355014066,-4.02455846426619E-16));
#12736=CARTESIAN_POINT('Ctrl Pts',(2.15588460824072,0.730664991573634,-5.27803664817409E-16));
#12737=CARTESIAN_POINT('Ctrl Pts',(2.17337597523708,0.65369086607791,1.83917474183848E-16));
#12738=CARTESIAN_POINT('Ctrl Pts',(2.18677163924531,0.576000526431045,1.80411241501588E-16));
#12739=CARTESIAN_POINT('Ctrl Pts',(2.19271177554795,0.541549736487604,1.78856447351139E-16));
#12740=CARTESIAN_POINT('Ctrl Pts',(2.19784589713018,0.506958238696871,2.58667507258439E-16));
#12741=CARTESIAN_POINT('Ctrl Pts',(2.20215036681449,0.472251887192273,3.05311331771918E-16));
#12742=CARTESIAN_POINT('Ctrl Pts',(2.20384086463367,0.45862163402915,3.23629798250044E-16));
#12743=CARTESIAN_POINT('Ctrl Pts',(2.2054034189863,0.444972429750506,-2.67189007756782E-16));
#12744=CARTESIAN_POINT('Ctrl Pts',(2.20683493494602,0.431323439258898,-2.63677968348475E-16));
#12745=CARTESIAN_POINT('Ctrl Pts',(2.21498668224708,0.353599456758773,-2.43684404304575E-16));
#12746=CARTESIAN_POINT('Ctrl Pts',(2.21891062752072,0.275752097207065,-3.64361181543216E-16));
#12747=CARTESIAN_POINT('Ctrl Pts',(2.21842976595528,0.198061284129886,-3.33066907387547E-16));
#12748=CARTESIAN_POINT('Ctrl Pts',(2.21823573988328,0.166713294655633,-3.2043976991813E-16));
#12749=CARTESIAN_POINT('Ctrl Pts',(2.21732398879068,0.135390827244206,1.47149945777791E-16));
#12750=CARTESIAN_POINT('Ctrl Pts',(2.2156804758574,0.104112597082251,1.11022302462516E-16));
#12751=CARTESIAN_POINT('Ctrl Pts',(2.21152549973649,0.0250378926516813,
4.83300826707103E-17));
#12752=CARTESIAN_POINT('Ctrl Pts',(2.20269687630619,-0.0537556215354904,
1.12975204580772E-16));
#12753=CARTESIAN_POINT('Ctrl Pts',(2.18938140457229,-0.131948941326607,
2.22044604925031E-16));
#12754=CARTESIAN_POINT('Ctrl Pts',(2.17635609001487,-0.208438352060393,
3.28737276162242E-16));
#12755=CARTESIAN_POINT('Ctrl Pts',(2.15903660233486,-0.284354146944832,
-3.46781305756475E-18));
#12756=CARTESIAN_POINT('Ctrl Pts',(2.13755823881172,-0.359371484419528,
-2.77555756156289E-17));
#12757=CARTESIAN_POINT('Ctrl Pts',(2.1327132344274,-0.376293599019833,-3.32343131345551E-17));
#12758=CARTESIAN_POINT('Ctrl Pts',(2.12765471739374,-0.393175045967983,
4.78722657737561E-16));
#12759=CARTESIAN_POINT('Ctrl Pts',(2.12239384145498,-0.409981702546287,
4.44089209850063E-16));
#12760=CARTESIAN_POINT('Ctrl Pts',(2.09915475041265,-0.484222461478205,
2.91101407450622E-16));
#12761=CARTESIAN_POINT('Ctrl Pts',(2.07194581573642,-0.557102807454745,
-2.6612583612487E-16));
#12762=CARTESIAN_POINT('Ctrl Pts',(2.04097168255273,-0.628331757793453,
-2.22044604925031E-16));
#12763=CARTESIAN_POINT('Ctrl Pts',(2.01002093348238,-0.699506933395764,
-1.77996653123198E-16));
#12764=CARTESIAN_POINT('Ctrl Pts',(1.97530999561803,-0.769034032577632,
-1.121614477549E-16));
#12765=CARTESIAN_POINT('Ctrl Pts',(1.93700033421706,-0.836593525678529,
2.77555756156289E-17));
#12766=CARTESIAN_POINT('Ctrl Pts',(1.89932999797199,-0.903025562104548,
1.65337614298032E-16));
#12767=CARTESIAN_POINT('Ctrl Pts',(1.85817935571419,-0.967555768065582,
3.22342438988347E-17));
#12768=CARTESIAN_POINT('Ctrl Pts',(1.81367086799685,-1.02984130765996,-8.32667268468867E-17));
#12769=CARTESIAN_POINT('Ctrl Pts',(1.79658036652,-1.05375789438347,-1.27617133080496E-16));
#12770=CARTESIAN_POINT('Ctrl Pts',(1.77899449903844,-1.07734305613259,3.71946656281201E-16));
#12771=CARTESIAN_POINT('Ctrl Pts',(1.76091927483634,-1.10057551065294,3.88578058618805E-16));
#12772=CARTESIAN_POINT('Ctrl Pts',(1.75330082146927,-1.11036766423216,3.955879613299E-16));
#12773=CARTESIAN_POINT('Ctrl Pts',(1.74559525034806,-1.120097236073,1.9277708950897E-16));
#12774=CARTESIAN_POINT('Ctrl Pts',(1.73781239012482,-1.12975130031544,1.94289029309402E-16));
#12775=CARTESIAN_POINT('Ctrl Pts',(1.69074076256592,-1.18814018350429,2.03433413910443E-16));
#12776=CARTESIAN_POINT('Ctrl Pts',(1.64076328117284,-1.24387604119422,4.01743023928347E-16));
#12777=CARTESIAN_POINT('Ctrl Pts',(1.58803301465667,-1.29667365960222,3.05311331771918E-16));
#12778=CARTESIAN_POINT('Ctrl Pts',(1.53615694857719,-1.34861598651105,2.10441778383092E-16));
#12779=CARTESIAN_POINT('Ctrl Pts',(1.48161590224946,-1.39771505374416,-1.45218570660009E-16));
#12780=CARTESIAN_POINT('Ctrl Pts',(1.42452885193311,-1.44365737342775,-1.94289029309402E-16));
#12781=CARTESIAN_POINT('Ctrl Pts',(1.36926934746984,-1.48812892705576,-2.4178857979808E-16));
#12782=CARTESIAN_POINT('Ctrl Pts',(1.31162365747817,-1.52964292911451,3.44150135834905E-16));
#12783=CARTESIAN_POINT('Ctrl Pts',(1.2516834907043,-1.56786936325681,3.33066907387547E-16));
#12784=CARTESIAN_POINT('Ctrl Pts',(1.22180547848687,-1.58692386256512,3.27542317571039E-16));
#12785=CARTESIAN_POINT('Ctrl Pts',(1.19135716333746,-1.60516076076372,2.09022357500404E-16));
#12786=CARTESIAN_POINT('Ctrl Pts',(1.160348984669,-1.62253437445177,2.22044604925031E-16));
#12787=CARTESIAN_POINT('Ctrl Pts',(0.159495341662761,2.44078487595691,24.0495));
#12788=CARTESIAN_POINT('Ctrl Pts',(0.553879590005283,2.41556185851724,24.0290607334364));
#12789=CARTESIAN_POINT('Ctrl Pts',(0.942374040131692,2.30021073164513,24.0086214668727));
#12790=CARTESIAN_POINT('Ctrl Pts',(1.27702530809929,2.09669071408131,23.9881822003091));
#12791=CARTESIAN_POINT('Ctrl Pts',(1.96998462930408,1.67526367428817,23.9458587978911));
#12792=CARTESIAN_POINT('Ctrl Pts',(2.43207727388235,0.875789536242101,23.9035353954731));
#12793=CARTESIAN_POINT('Ctrl Pts',(2.45343275118969,0.0650681252545471,
23.8612119930552));
#12794=CARTESIAN_POINT('Ctrl Pts',(2.47478822849703,-0.745653285733007,
23.8188885906372));
#12795=CARTESIAN_POINT('Ctrl Pts',(2.05540653853344,-1.56762196966205,23.7765651882193));
#12796=CARTESIAN_POINT('Ctrl Pts',(1.38635176387791,-2.02548987348432,23.7342417858013));
#12797=CARTESIAN_POINT('Ctrl Pts',(0.717296989222389,-2.48335777730658,
23.6919183833833));
#12798=CARTESIAN_POINT('Ctrl Pts',(-0.201430870125064,-2.57712490102209,
23.6495949809654));
#12799=CARTESIAN_POINT('Ctrl Pts',(-0.94925274522526,-2.26359816468399,
23.6072715785474));
#12800=CARTESIAN_POINT('Ctrl Pts',(-1.69707462032548,-1.95007142834589,
23.5649481761294));
#12801=CARTESIAN_POINT('Ctrl Pts',(-2.27399051117843,-1.22925083195416,
23.5226247737115));
#12802=CARTESIAN_POINT('Ctrl Pts',(-2.41634438138384,-0.430973544622496,
23.4803013712935));
#12803=CARTESIAN_POINT('Ctrl Pts',(-2.44154118278753,-0.289677531771226,
23.4728100795997));
#12804=CARTESIAN_POINT('Ctrl Pts',(-2.4531234108498,-0.145954846202415,
23.4653187879059));
#12805=CARTESIAN_POINT('Ctrl Pts',(-2.45183158050284,-0.00202607996204418,
23.457827496212));
#12806=CARTESIAN_POINT('Origin',(0.,0.,-1.47904511860479));
#12807=CARTESIAN_POINT('',(-1.16034898466913,-1.62253437445168,0.));
#12808=CARTESIAN_POINT('Ctrl Pts',(-1.16284465745828,-1.62479335886122,
1.03432887255117E-15));
#12809=CARTESIAN_POINT('Ctrl Pts',(-0.662089630281565,-1.97916236613021,
0.0393081915296248));
#12810=CARTESIAN_POINT('Ctrl Pts',(0.746426826565863,-2.20908649969502,
0.120955489700587));
#12811=CARTESIAN_POINT('Ctrl Pts',(2.27348886028002,-0.624404468413451,
0.244941894512889));
#12812=CARTESIAN_POINT('Ctrl Pts',(1.75738237739457,1.57205987855945,0.371959214436904));
#12813=CARTESIAN_POINT('Ctrl Pts',(-0.367613798684614,2.32876162996938,
0.498976534360922));
#12814=CARTESIAN_POINT('Ctrl Pts',(-1.80883238148956,1.22105962818686,0.601338502416877));
#12815=CARTESIAN_POINT('Ctrl Pts',(-1.99291933052672,0.27887251148749,0.661361363831493));
#12816=CARTESIAN_POINT('Ctrl Pts',(-1.99183435874083,0.00088002408572329,
0.679045118604771));
#12817=CARTESIAN_POINT('Origin',(0.,0.,0.));
#12818=CARTESIAN_POINT('Ctrl Pts',(-0.875140871775308,1.79252782880723,
-0.263127385183177));
#12819=CARTESIAN_POINT('Ctrl Pts',(-1.47121116518756,1.50151673942109,-0.220788278541838));
#12820=CARTESIAN_POINT('Ctrl Pts',(-2.33993822790823,0.283206897790784,
-0.13611006525916));
#12821=CARTESIAN_POINT('Ctrl Pts',(-1.50537684452792,-1.81659298312073,
-0.00909274533514401));
#12822=CARTESIAN_POINT('Ctrl Pts',(0.709096964461084,-2.24782491398444,
0.117924574588872));
#12823=CARTESIAN_POINT('Ctrl Pts',(2.27348886028002,-0.624404468413451,
0.244941894512889));
#12824=CARTESIAN_POINT('Ctrl Pts',(1.75738237739457,1.57205987855945,0.371959214436904));
#12825=CARTESIAN_POINT('Ctrl Pts',(-0.367613798684614,2.32876162996938,
0.498976534360922));
#12826=CARTESIAN_POINT('Ctrl Pts',(-2.15597060042669,0.954253673420782,
0.625993854284938));
#12827=CARTESIAN_POINT('Ctrl Pts',(-1.97094594256774,-1.29394223767452,
0.753011174208954));
#12828=CARTESIAN_POINT('Ctrl Pts',(0.0182153715595747,-2.3576204698764,
0.88002849413297));
#12829=CARTESIAN_POINT('Ctrl Pts',(1.9906822371454,-1.26332101110348,1.00704581405699));
#12830=CARTESIAN_POINT('Ctrl Pts',(2.14099816144828,0.987384922727256,1.134063133981));
#12831=CARTESIAN_POINT('Ctrl Pts',(0.331555254300241,2.33427609427238,1.26108045390502));
#12832=CARTESIAN_POINT('Ctrl Pts',(-1.78137220841604,1.54450678564102,1.38809777382904));
#12833=CARTESIAN_POINT('Ctrl Pts',(-2.26373025095555,-0.659024375424702,
1.51511509375305));
#12834=CARTESIAN_POINT('Ctrl Pts',(-0.673992169187479,-2.25931816777247,
1.64213241367707));
#12835=CARTESIAN_POINT('Ctrl Pts',(1.53268116536722,-1.79155650545778,1.76914973360108));
#12836=CARTESIAN_POINT('Ctrl Pts',(2.33642193463667,0.316098985050819,1.8961670535251));
#12837=CARTESIAN_POINT('Ctrl Pts',(1.00152929412067,2.13441435022671,2.02318437344912));
#12838=CARTESIAN_POINT('Ctrl Pts',(-1.25010860812744,1.99900333994266,2.15020169337313));
#12839=CARTESIAN_POINT('Ctrl Pts',(-2.35746526350733,0.0338135367837335,
2.27721901329715));
#12840=CARTESIAN_POINT('Ctrl Pts',(-1.30692669699531,-1.96232728509918,
2.40423633322116));
#12841=CARTESIAN_POINT('Ctrl Pts',(0.939901322271841,-2.16226069656491,
2.53125365314518));
#12842=CARTESIAN_POINT('Ctrl Pts',(2.32639490702415,-0.382978510636179,
2.6582709730692));
#12843=CARTESIAN_POINT('Ctrl Pts',(1.58343339573353,1.74686132178264,2.78528829299322));
#12844=CARTESIAN_POINT('Ctrl Pts',(-0.608916736747748,2.27771951988605,
2.91230561291723));
#12845=CARTESIAN_POINT('Ctrl Pts',(-2.24389767923029,0.723677418756311,
3.03932293284125));
#12846=CARTESIAN_POINT('Ctrl Pts',(-1.82493699351161,-1.49277954510288,
3.16634025276526));
#12847=CARTESIAN_POINT('Ctrl Pts',(0.264471544354857,-2.34282748059378,
3.29335757268928));
#12848=CARTESIAN_POINT('Ctrl Pts',(2.11179724612446,-1.04837884014621,3.42037489261329));
#12849=CARTESIAN_POINT('Ctrl Pts',(2.02609885609852,1.2056986466197,3.54739221253732));
#12850=CARTESIAN_POINT('Ctrl Pts',(0.0858200094412126,2.35614531115273,
3.67440953246132));
#12851=CARTESIAN_POINT('Ctrl Pts',(-1.93301379609718,1.34990498381208,3.80142685238535));
#12852=CARTESIAN_POINT('Ctrl Pts',(-2.1824721351227,-0.891964786655331,
3.92844417230936));
#12853=CARTESIAN_POINT('Ctrl Pts',(-0.434214441284883,-2.31737860959731,
4.05546149223338));
#12854=CARTESIAN_POINT('Ctrl Pts',(1.71149948445725,-1.62159036625522,4.18247881215739));
#12855=CARTESIAN_POINT('Ctrl Pts',(2.29060007052677,0.558513310613506,4.30949613208142));
#12856=CARTESIAN_POINT('Ctrl Pts',(0.77301020537091,2.22738434573485,4.43651345200542));
#12857=CARTESIAN_POINT('Ctrl Pts',(-1.4521510674508,1.85742915841551,4.56353077192945));
#12858=CARTESIAN_POINT('Ctrl Pts',(-2.34809240527012,-0.212715437953238,
4.69054809185345));
#12859=CARTESIAN_POINT('Ctrl Pts',(-1.09471794236404,-2.08815191686271,
4.81756541177748));
#12860=CARTESIAN_POINT('Ctrl Pts',(1.16070165538423,-2.05220794960434,4.94458273170149));
#12861=CARTESIAN_POINT('Ctrl Pts',(2.35367822395426,-0.13778468461515,5.07160005162551));
#12862=CARTESIAN_POINT('Ctrl Pts',(1.3922260378406,1.90275917046527,5.19861737154953));
#12863=CARTESIAN_POINT('Ctrl Pts',(-0.843593977493136,2.20162099426043,
5.32563469147353));
#12864=CARTESIAN_POINT('Ctrl Pts',(-2.30723404745788,0.485238963277019,
5.45265201139756));
#12865=CARTESIAN_POINT('Ctrl Pts',(-1.65895783037916,-1.67530436585556,
5.57966933132157));
#12866=CARTESIAN_POINT('Ctrl Pts',(0.507837960106644,-2.30236539400368,
5.70668665124559));
#12867=CARTESIAN_POINT('Ctrl Pts',(2.20978656254498,-0.821966635105482,
5.83370397116961));
#12868=CARTESIAN_POINT('Ctrl Pts',(1.88901699407625,1.41081557877779,5.96072129109363));
#12869=CARTESIAN_POINT('Ctrl Pts',(-0.160855766453599,2.35221411092393,
6.08773861101763));
#12870=CARTESIAN_POINT('Ctrl Pts',(-2.06348992610873,1.14052405765016,6.21475593094166));
#12871=CARTESIAN_POINT('Ctrl Pts',(-2.07731788168555,-1.11513955165281,
6.34177325086566));
#12872=CARTESIAN_POINT('Ctrl Pts',(-0.189682276366992,-2.35006519808776,
6.46879057078969));
#12873=CARTESIAN_POINT('Ctrl Pts',(1.87157814575952,-1.43386925678263,6.5958078907137));
#12874=CARTESIAN_POINT('Ctrl Pts',(2.21969794703782,0.794812446522514,6.72282521063772));
#12875=CARTESIAN_POINT('Ctrl Pts',(0.536027236282382,2.29596615898285,6.84984253056173));
#12876=CARTESIAN_POINT('Ctrl Pts',(-1.63829358942387,1.69551759533295,6.97685985048576));
#12877=CARTESIAN_POINT('Ctrl Pts',(-2.31300976155138,-0.456915357806061,
7.10387717040976));
#12878=CARTESIAN_POINT('Ctrl Pts',(-0.870522872770069,-2.19111289741426,
7.23089449033379));
#12879=CARTESIAN_POINT('Ctrl Pts',(1.3687932043082,-1.91968512133389,7.3579118102578));
#12880=CARTESIAN_POINT('Ctrl Pts',(2.35519059073263,0.108917778877055,7.48492913018183));
#12881=CARTESIAN_POINT('Ctrl Pts',(1.18577488435873,2.03782328106611,7.61194645010582));
#12882=CARTESIAN_POINT('Ctrl Pts',(-1.06903451833457,2.10141642704157,7.73896377002986));
#12883=CARTESIAN_POINT('Ctrl Pts',(-2.34530799262043,0.241487517237905,
7.86598108995386));
#12884=CARTESIAN_POINT('Ctrl Pts',(-1.47481436575085,-1.8394859031278,7.99299840987789));
#12885=CARTESIAN_POINT('Ctrl Pts',(0.745643944080418,-2.23669419230417,
8.1200157298019));
#12886=CARTESIAN_POINT('Ctrl Pts',(2.28358043018348,-0.586554532941333,
8.24703304972591));
#12887=CARTESIAN_POINT('Ctrl Pts',(1.73125186121253,1.60048517465147,8.37405036964994));
#12888=CARTESIAN_POINT('Ctrl Pts',(-0.405770296472382,2.32252799073159,
8.50106768957393));
#12889=CARTESIAN_POINT('Ctrl Pts',(-2.1713724420165,0.918655277719749,8.62808500949798));
#12890=CARTESIAN_POINT('Ctrl Pts',(-1.94941860875359,-1.32610440353548,
8.75510232942198));
#12891=CARTESIAN_POINT('Ctrl Pts',(0.0569267623458949,-2.35702039553327,
8.882119649346));
#12892=CARTESIAN_POINT('Ctrl Pts',(2.01116447809095,-1.23044839115509,9.00913696927002));
#12893=CARTESIAN_POINT('Ctrl Pts',(2.12449185277921,1.02240900265292,9.13615428919402));
#12894=CARTESIAN_POINT('Ctrl Pts',(0.293175184736282,2.33940892369971,9.26317160911806));
#12895=CARTESIAN_POINT('Ctrl Pts',(-1.80649806736613,1.51504142974158,9.39018892904205));
#12896=CARTESIAN_POINT('Ctrl Pts',(-2.25260145507328,-0.696112408905862,
9.51720624896608));
#12897=CARTESIAN_POINT('Ctrl Pts',(-0.636796252956758,-2.27008289131724,
9.64422356889009));
#12898=CARTESIAN_POINT('Ctrl Pts',(1.5618975293753,-1.76614323002478,9.77124088881411));
#12899=CARTESIAN_POINT('Ctrl Pts',(2.33091544739048,0.354427677174692,9.89825820873813));
#12900=CARTESIAN_POINT('Ctrl Pts',(0.966340415661779,2.15057480741536,10.0252755286621));
#12901=CARTESIAN_POINT('Ctrl Pts',(-1.28276996041703,1.97820297994991,10.1522928485862));
#12902=CARTESIAN_POINT('Ctrl Pts',(-2.35770263444618,-0.0049080298005949,
10.2793101685102));
#12903=CARTESIAN_POINT('Ctrl Pts',(-1.27452282778516,-1.98352649659275,
10.4063274884342));
#12904=CARTESIAN_POINT('Ctrl Pts',(0.975285705239301,-2.14653292413298,
10.5333448083582));
#12905=CARTESIAN_POINT('Ctrl Pts',(2.33237086341372,-0.344720113613569,
10.6603621282822));
#12906=CARTESIAN_POINT('Ctrl Pts',(1.5545308633467,1.77263069930924,10.7873794482062));
#12907=CARTESIAN_POINT('Ctrl Pts',(-0.646241956488163,2.2674119905534,10.9143967681303));
#12908=CARTESIAN_POINT('Ctrl Pts',(-2.25548011395016,0.686727935070636,
11.0414140880543));
#12909=CARTESIAN_POINT('Ctrl Pts',(-1.80017471415913,-1.52254944081731,
11.1684314079783));
#12910=CARTESIAN_POINT('Ctrl Pts',(0.302912497167387,-2.33816804791504,
11.2954487279023));
#12911=CARTESIAN_POINT('Ctrl Pts',(2.12873011938496,-1.01355507006492,11.4224660478263));
#12912=CARTESIAN_POINT('Ctrl Pts',(2.00602422063487,1.2388109732551,11.5494833677503));
#12913=CARTESIAN_POINT('Ctrl Pts',(0.0471130923241888,2.35723697530873,
11.6765006876744));
#12914=CARTESIAN_POINT('Ctrl Pts',(-1.95492279271505,1.31797673566501,11.8035180075984));
#12915=CARTESIAN_POINT('Ctrl Pts',(-2.16752890993496,-0.927687569080867,
11.9305353275224));
#12916=CARTESIAN_POINT('Ctrl Pts',(-0.396097208116597,-2.32419723839291,
12.0575526474464));
#12917=CARTESIAN_POINT('Ctrl Pts',(1.737900288011,-1.59326344028923,12.1845699673704));
#12918=CARTESIAN_POINT('Ctrl Pts',(2.28111858791796,0.596056867325744,12.3115872872944));
#12919=CARTESIAN_POINT('Ctrl Pts',(0.736325268973554,2.23977920775732,12.4386046072184));
#12920=CARTESIAN_POINT('Ctrl Pts',(-1.48246006643762,1.83332974465828,12.5656219271425));
#12921=CARTESIAN_POINT('Ctrl Pts',(-2.34428226122129,-0.251249837719779,
12.6926392470665));
#12922=CARTESIAN_POINT('Ctrl Pts',(-1.06027625346291,-2.10584901347975,
12.8196565669905));
#12923=CARTESIAN_POINT('Ctrl Pts',(1.19424884442458,-2.03286878544129,12.9466738869145));
#12924=CARTESIAN_POINT('Ctrl Pts',(2.35562364483704,-0.0991112764303932,
13.0736912068385));
#12925=CARTESIAN_POINT('Ctrl Pts',(1.36078895832842,1.92536729278402,13.2007085267625));
#12926=CARTESIAN_POINT('Ctrl Pts',(-0.879637768350177,2.18746958783955,
13.3277258466866));
#12927=CARTESIAN_POINT('Ctrl Pts',(-2.31489202814179,0.447281454205958,
13.4547431666106));
#12928=CARTESIAN_POINT('Ctrl Pts',(-1.6312203027841,-1.70232374271639,13.5817604865346));
#12929=CARTESIAN_POINT('Ctrl Pts',(0.545581575104675,-2.2937145738163,13.7087778064586));
#12930=CARTESIAN_POINT('Ctrl Pts',(2.22298781706136,-0.785564107140691,
13.8357951263826));
#12931=CARTESIAN_POINT('Ctrl Pts',(1.86559217928514,1.44164892460722,13.9628124463066));
#12932=CARTESIAN_POINT('Ctrl Pts',(-0.199464851904689,2.34925511047346,
14.0898297662307));
#12933=CARTESIAN_POINT('Ctrl Pts',(-2.08194262985648,1.10648121864643,14.2168470861547));
#12934=CARTESIAN_POINT('Ctrl Pts',(-2.05872360451754,-1.1491052699528,14.3438644060787));
#12935=CARTESIAN_POINT('Ctrl Pts',(-0.151061206087832,-2.35286342851562,
14.4708817260027));
#12936=CARTESIAN_POINT('Ctrl Pts',(1.89487438652815,-1.40293865172736,14.5978990459267));
#12937=CARTESIAN_POINT('Ctrl Pts',(2.2063452493004,0.831159697122361,14.7249163658507));
#12938=CARTESIAN_POINT('Ctrl Pts',(0.498247931734623,2.30445976310136,14.8519336857748));
#12939=CARTESIAN_POINT('Ctrl Pts',(-1.66591838462884,1.66838297071943,14.9789510056988));
#12940=CARTESIAN_POINT('Ctrl Pts',(-2.30519381562279,-0.494840654802578,
15.1059683256228));
#12941=CARTESIAN_POINT('Ctrl Pts',(-0.834420476588558,-2.20511411711067,
15.2329856455468));
#12942=CARTESIAN_POINT('Ctrl Pts',(1.40013588510504,-1.89694631038207,15.3600029654708));
#12943=CARTESIAN_POINT('Ctrl Pts',(2.35308417453332,0.147582752352149,15.4870202853949));
#12944=CARTESIAN_POINT('Ctrl Pts',(1.15214746973809,2.05702260785027,15.6140376053188));
#12945=CARTESIAN_POINT('Ctrl Pts',(-1.10340222895637,2.08357608989091,15.7410549252429));
#12946=CARTESIAN_POINT('Ctrl Pts',(-2.34895767021494,0.202937588360042,
15.8680722451669));
#12947=CARTESIAN_POINT('Ctrl Pts',(-1.44440529438039,-1.86345892007226,
15.9950895650909));
#12948=CARTESIAN_POINT('Ctrl Pts',(0.782276957985213,-2.22414670429727,
16.1221068850149));
#12949=CARTESIAN_POINT('Ctrl Pts',(2.2929055224434,-0.548971826580871,16.249124204939));
#12950=CARTESIAN_POINT('Ctrl Pts',(1.704733350654,1.62870193847707,16.3761415248629));
#12951=CARTESIAN_POINT('Ctrl Pts',(-0.443858810723858,2.31555072442255,
16.503158844787));
#12952=CARTESIAN_POINT('Ctrl Pts',(-2.18616681009904,0.882870590546761,
16.630176164711));
#12953=CARTESIAN_POINT('Ctrl Pts',(-1.92737687251849,-1.3579411594439,16.757193484635));
#12954=CARTESIAN_POINT('Ctrl Pts',(0.0956287989740662,-2.355767589139,16.884210804559));
#12955=CARTESIAN_POINT('Ctrl Pts',(2.03110108030785,-1.19725277314494,17.011228124483));
#12956=CARTESIAN_POINT('Ctrl Pts',(2.10741414159636,1.05716197294014,17.138245444407));
#12957=CARTESIAN_POINT('Ctrl Pts',(0.254715166118652,2.34390827153712,17.2652627643311));
#12958=CARTESIAN_POINT('Ctrl Pts',(-1.83113618870942,1.48516869736397,17.3922800842551));
#12959=CARTESIAN_POINT('Ctrl Pts',(-2.2408652858103,-0.733013350547816,
17.5192974041791));
#12960=CARTESIAN_POINT('Ctrl Pts',(-0.599428442729515,-2.28023493159759,
17.6463147241031));
#12961=CARTESIAN_POINT('Ctrl Pts',(1.5906925238854,-1.74025374462637,17.7733320440271));
#12962=CARTESIAN_POINT('Ctrl Pts',(2.32478025773261,0.392660864471763,17.9003493639512));
#12963=CARTESIAN_POINT('Ctrl Pts',(0.930890860039063,2.16615512092895,18.0273666838751));
#12964=CARTESIAN_POINT('Ctrl Pts',(-1.31508529103024,1.95686904992309,18.1543840037992));
#12965=CARTESIAN_POINT('Ctrl Pts',(-2.35730404781258,-0.0436282866660298,
18.2814013237232));
#12966=CARTESIAN_POINT('Ctrl Pts',(-1.24177516838345,-2.00419066768041,
18.4084186436472));
#12967=CARTESIAN_POINT('Ctrl Pts',(1.01040701496368,-2.13022615356754,18.5354359635712));
#12968=CARTESIAN_POINT('Ctrl Pts',(2.33771769089012,-0.306368730340369,
18.6624532834953));
#12969=CARTESIAN_POINT('Ctrl Pts',(1.52520901414179,1.79792192945402,18.7894706034193));
#12970=CARTESIAN_POINT('Ctrl Pts',(-0.683392859853091,2.25649285403983,
18.9164879233433));
#12971=CARTESIAN_POINT('Ctrl Pts',(-2.26645415951258,0.649593214295779,
19.0435052432673));
#12972=CARTESIAN_POINT('Ctrl Pts',(-1.77492685877157,-1.55190864655181,
19.1705225631913));
#12973=CARTESIAN_POINT('Ctrl Pts',(0.341271742863524,-2.33287792195687,
19.2975398831153));
#12974=CARTESIAN_POINT('Ctrl Pts',(2.14508879272012,-0.978457905368288,
19.4245572030393));
#12975=CARTESIAN_POINT('Ctrl Pts',(1.98540848369728,1.27158914516195,19.5515745229634));
#12976=CARTESIAN_POINT('Ctrl Pts',(0.00839346700838828,2.35769280249617,
19.6785918428874));
#12977=CARTESIAN_POINT('Ctrl Pts',(-1.97630447187918,1.2856929787716,19.8056091628114));
#12978=CARTESIAN_POINT('Ctrl Pts',(-2.15200101928721,-0.963160118680454,
19.9326264827354));
#12979=CARTESIAN_POINT('Ctrl Pts',(-0.357873132381371,-2.33038894229026,
20.0596438026594));
#12980=CARTESIAN_POINT('Ctrl Pts',(1.76383231338145,-1.56450675022861,20.1866611225834));
#12981=CARTESIAN_POINT('Ctrl Pts',(2.27102180036648,0.633439644702114,20.3136784425075));
#12982=CARTESIAN_POINT('Ctrl Pts',(0.699441717491183,2.25156991564901,20.4406957624314));
#12983=CARTESIAN_POINT('Ctrl Pts',(-1.51236918924863,1.80873581174778,20.5677130823555));
#12984=CARTESIAN_POINT('Ctrl Pts',(-2.33983977455391,-0.289716465807172,
20.6947304022795));
#12985=CARTESIAN_POINT('Ctrl Pts',(-1.02554856753737,-2.12297808204117,
20.8217477222035));
#12986=CARTESIAN_POINT('Ctrl Pts',(1.22747389894261,-2.0129812788532,20.9487650421275));
#12987=CARTESIAN_POINT('Ctrl Pts',(2.35693366377738,-0.0604111340540538,
21.0757823620516));
#12988=CARTESIAN_POINT('Ctrl Pts',(1.32898482224672,1.94745606972551,21.2027996819756));
#12989=CARTESIAN_POINT('Ctrl Pts',(-0.915444287757947,2.1727281375204,21.3298170018996));
#12990=CARTESIAN_POINT('Ctrl Pts',(-2.32192559293657,0.40920329560084,21.4568343218236));
#12991=CARTESIAN_POINT('Ctrl Pts',(-1.60304277450666,-1.72888393657267,
21.5838516417477));
#12992=CARTESIAN_POINT('Ctrl Pts',(0.583178029368184,-2.28444505330724,
21.7108689616716));
#12993=CARTESIAN_POINT('Ctrl Pts',(2.23558944009154,-0.748949678226114,
21.8378862815957));
#12994=CARTESIAN_POINT('Ctrl Pts',(1.84166415556682,1.47209339446037,21.9649036015196));
#12995=CARTESIAN_POINT('Ctrl Pts',(-0.23802015814085,2.34566244151516,22.0919209214437));
#12996=CARTESIAN_POINT('Ctrl Pts',(-2.09983370816391,1.07213988989037,22.2189382413677));
#12997=CARTESIAN_POINT('Ctrl Pts',(-2.0395740982221,-1.18276097452655,22.3459555612917));
#12998=CARTESIAN_POINT('Ctrl Pts',(-0.112399222395231,-2.35502710849036,
22.4729728812157));
#12999=CARTESIAN_POINT('Ctrl Pts',(1.91765919019992,-1.37162941700542,22.5999902011398));
#13000=CARTESIAN_POINT('Ctrl Pts',(2.19239801962464,0.867282364654784,22.7270075210638));
#13001=CARTESIAN_POINT('Ctrl Pts',(0.460333080665931,2.31233250434551,22.8540248409878));
#13002=CARTESIAN_POINT('Ctrl Pts',(-1.69309162754269,1.64079691360341,22.9810421609118));
#13003=CARTESIAN_POINT('Ctrl Pts',(-2.29676024272747,-0.532629796744884,
23.1080594808358));
#13004=CARTESIAN_POINT('Ctrl Pts',(-0.798085058971124,-2.21852563316919,
23.2350768007599));
#13005=CARTESIAN_POINT('Ctrl Pts',(1.43108576045911,-1.87368610656973,23.3620941206838));
#13006=CARTESIAN_POINT('Ctrl Pts',(2.35037186943588,0.186189415184726,23.4891114406079));
#13007=CARTESIAN_POINT('Ctrl Pts',(1.11815436836127,2.07570231768813,23.6161287605319));
#13008=CARTESIAN_POINT('Ctrl Pts',(-1.13736772283233,2.06510660675428,23.7431460804559));
#13009=CARTESIAN_POINT('Ctrl Pts',(-2.3521729797966,0.164460801615943,23.8701634003799));
#13010=CARTESIAN_POINT('Ctrl Pts',(-1.41322686604255,-1.88717311423397,
23.9971807203039));
#13011=CARTESIAN_POINT('Ctrl Pts',(0.817973374160278,-2.21053272043233,
24.1241980402279));
#13012=CARTESIAN_POINT('Ctrl Pts',(2.30301402245599,-0.512148340557086,
24.2512153601519));
#13013=CARTESIAN_POINT('Ctrl Pts',(1.674912756705,1.65836796725257,24.378232680076));
#13014=CARTESIAN_POINT('Ctrl Pts',(0.24166366648125,2.0882081993032,24.4629108933587));
#13015=CARTESIAN_POINT('Ctrl Pts',(-0.4076525627588,1.95265126189399,24.50525));
#13016=CARTESIAN_POINT('Ctrl Pts',(-0.941790067967272,1.92904360906019,
-0.175418256788786));
#13017=CARTESIAN_POINT('Ctrl Pts',(-1.58325603104951,1.61586962474357,-0.133079150147447));
#13018=CARTESIAN_POINT('Ctrl Pts',(-2.51814382549676,0.304775439156526,
-0.0484009368647695));
#13019=CARTESIAN_POINT('Ctrl Pts',(-1.62002370869527,-1.95494152338182,
0.0786163830592463));
#13020=CARTESIAN_POINT('Ctrl Pts',(0.76310054745868,-2.41901532289923,0.205633702983263));
#13021=CARTESIAN_POINT('Ctrl Pts',(2.44663379040036,-0.671958019230885,
0.332651022907279));
#13022=CARTESIAN_POINT('Ctrl Pts',(1.8912215416169,1.69178520581912,0.459668342831296));
#13023=CARTESIAN_POINT('Ctrl Pts',(-0.395610621803758,2.50611603743205,
0.586685662755312));
#13024=CARTESIAN_POINT('Ctrl Pts',(-2.32016554568208,1.02692796203862,0.713702982679328));
#13025=CARTESIAN_POINT('Ctrl Pts',(-2.12104973390752,-1.39248661246172,
0.840720302603345));
#13026=CARTESIAN_POINT('Ctrl Pts',(0.0196026223576674,-2.53717271604696,
0.967737622527361));
#13027=CARTESIAN_POINT('Ctrl Pts',(2.1422891101168,-1.35953332690082,1.09475494245138));
#13028=CARTESIAN_POINT('Ctrl Pts',(2.30405283197173,1.06258242927079,1.22177226237539));
#13029=CARTESIAN_POINT('Ctrl Pts',(0.35680592182702,2.51205047367911,1.34878958229941));
#13030=CARTESIAN_POINT('Ctrl Pts',(-1.91703839615649,1.66213371759669,1.47580690222343));
#13031=CARTESIAN_POINT('Ctrl Pts',(-2.43613198247962,-0.709214517731593,
1.60282422214744));
#13032=CARTESIAN_POINT('Ctrl Pts',(-0.725322232454721,-2.43138388276806,
1.72984154207146));
#13033=CARTESIAN_POINT('Ctrl Pts',(1.64940747879268,-1.92799831142548,1.85685886199548));
#13034=CARTESIAN_POINT('Ctrl Pts',(2.51435973748759,0.340172530179638,1.98387618191949));
#13035=CARTESIAN_POINT('Ctrl Pts',(1.07780401121893,2.29696760921754,2.11089350184351));
#13036=CARTESIAN_POINT('Ctrl Pts',(-1.34531469045259,2.15124393353062,2.23791082176752));
#13037=CARTESIAN_POINT('Ctrl Pts',(-2.53700568943262,0.0363887165287244,
2.36492814169154));
#13038=CARTESIAN_POINT('Ctrl Pts',(-1.40645994546512,-2.11177469457974,
2.49194546161556));
#13039=CARTESIAN_POINT('Ctrl Pts',(1.011482560961,-2.32693468452654,2.61896278153957));
#13040=CARTESIAN_POINT('Ctrl Pts',(2.50356906901209,-0.412145483309817,
2.74598010146359));
#13041=CARTESIAN_POINT('Ctrl Pts',(1.70402491014309,1.87989922083475,2.8729974213876));
#13042=CARTESIAN_POINT('Ctrl Pts',(-0.655290769044694,2.45118664963297,
3.00001474131162));
#13043=CARTESIAN_POINT('Ctrl Pts',(-2.41478899682385,0.778791423618739,
3.12703206123564));
#13044=CARTESIAN_POINT('Ctrl Pts',(-1.96392099899146,-1.60646702100726,
3.25404938115965));
#13045=CARTESIAN_POINT('Ctrl Pts',(0.284613234013536,-2.521253118607,3.38106670108367));
#13046=CARTESIAN_POINT('Ctrl Pts',(2.27262802607538,-1.12822153662387,3.50808402100769));
#13047=CARTESIAN_POINT('Ctrl Pts',(2.18040299674552,1.29752254404997,3.6351013409317));
#13048=CARTESIAN_POINT('Ctrl Pts',(0.0923559110667471,2.53558521181829,
3.76211866085572));
#13049=CARTESIAN_POINT('Ctrl Pts',(-2.08022874159101,1.45271138333953,3.88913598077973));
#13050=CARTESIAN_POINT('Ctrl Pts',(-2.34868539084933,-0.959895262741452,
4.01615330070375));
#13051=CARTESIAN_POINT('Ctrl Pts',(-0.4672834527091,-2.49386610616313,4.14317062062777));
#13052=CARTESIAN_POINT('Ctrl Pts',(1.84184428790656,-1.74508784871679,4.27018794055178));
#13053=CARTESIAN_POINT('Ctrl Pts',(2.46504816045325,0.601048706245761,4.3972052604758));
#13054=CARTESIAN_POINT('Ctrl Pts',(0.831881308867185,2.3970180367686,4.52422258039981));
#13055=CARTESIAN_POINT('Ctrl Pts',(-1.56274434964838,1.99888771027209,4.65123990032383));
#13056=CARTESIAN_POINT('Ctrl Pts',(-2.52691901072642,-0.228915473186961,
4.77825722024785));
#13057=CARTESIAN_POINT('Ctrl Pts',(-1.17808974371463,-2.24718190994627,
4.90527454017187));
#13058=CARTESIAN_POINT('Ctrl Pts',(1.24909866076361,-2.20850051308883,5.03229186009588));
#13059=CARTESIAN_POINT('Ctrl Pts',(2.5329302355793,-0.148278124898084,5.1593091800199));
#13060=CARTESIAN_POINT('Ctrl Pts',(1.49825553472755,2.0476699766548,5.28632649994391));
#13061=CARTESIAN_POINT('Ctrl Pts',(-0.907840617463509,2.36929259356429,
5.41334381986794));
#13062=CARTESIAN_POINT('Ctrl Pts',(-2.48294895193696,0.522193912938763,
5.54036113979194));
#13063=CARTESIAN_POINT('Ctrl Pts',(-1.78530115346812,-1.80289261245937,
5.66737845971597));
#13064=CARTESIAN_POINT('Ctrl Pts',(0.546514009790199,-2.47770951036197,
5.79439577963998));
#13065=CARTESIAN_POINT('Ctrl Pts',(2.37808003722935,-0.884566174554725,
5.921413099564));
#13066=CARTESIAN_POINT('Ctrl Pts',(2.03288122017812,1.51826082254739,6.04843041948801));
#13067=CARTESIAN_POINT('Ctrl Pts',(-0.173106259925872,2.53135461826462,
6.17544773941203));
#13068=CARTESIAN_POINT('Ctrl Pts',(-2.22064170516612,1.22738437252235,6.30246505933605));
#13069=CARTESIAN_POINT('Ctrl Pts',(-2.23552277362324,-1.20006662700327,
6.42948237926006));
#13070=CARTESIAN_POINT('Ctrl Pts',(-0.204128146351376,-2.52904204799016,
6.55649969918408));
#13071=CARTESIAN_POINT('Ctrl Pts',(2.01411425971366,-1.54307022829594,6.68351701910809));
#13072=CARTESIAN_POINT('Ctrl Pts',(2.38874625540769,0.85534397052349,6.81053433903211));
#13073=CARTESIAN_POINT('Ctrl Pts',(0.576850131872557,2.47082292080873,6.93755165895612));
#13074=CARTESIAN_POINT('Ctrl Pts',(-1.76306316011027,1.82464524609501,7.06456897888015));
#13075=CARTESIAN_POINT('Ctrl Pts',(-2.48916453430101,-0.491713231277311,
7.19158629880415));
#13076=CARTESIAN_POINT('Ctrl Pts',(-0.936820370245068,-2.3579842184648,
7.31860361872818));
#13077=CARTESIAN_POINT('Ctrl Pts',(1.47303809763044,-2.06588497829972,7.44562093865219));
#13078=CARTESIAN_POINT('Ctrl Pts',(2.53455778156296,0.11721276617261,7.57263825857621));
#13079=CARTESIAN_POINT('Ctrl Pts',(1.27608142294691,2.19302033338612,7.69965557850022));
#13080=CARTESIAN_POINT('Ctrl Pts',(-1.15045031508959,2.26145662199066,7.82667289842425));
#13081=CARTESIAN_POINT('Ctrl Pts',(-2.52392254208557,0.259878783642378,
7.95369021834826));
#13082=CARTESIAN_POINT('Ctrl Pts',(-1.58713364505749,-1.97957792808509,
8.08070753827228));
#13083=CARTESIAN_POINT('Ctrl Pts',(0.802430881042418,-2.40703690494862,
8.20772485819628));
#13084=CARTESIAN_POINT('Ctrl Pts',(2.45749391659467,-0.63122549895843,8.33474217812031));
#13085=CARTESIAN_POINT('Ctrl Pts',(1.86310097108385,1.72237532268131,8.46175949804432));
#13086=CARTESIAN_POINT('Ctrl Pts',(-0.436673051640951,2.49940765514666,
8.58877681796835));
#13087=CARTESIAN_POINT('Ctrl Pts',(-2.33674036455467,0.988618454863179,
8.71579413789234));
#13088=CARTESIAN_POINT('Ctrl Pts',(-2.09788291605014,-1.42709819255022,
8.84281145781638));
#13089=CARTESIAN_POINT('Ctrl Pts',(0.061262204872421,-2.53652694109274,
8.96982877774038));
#13090=CARTESIAN_POINT('Ctrl Pts',(2.16433124266297,-1.32415718578578,9.09684609766441));
#13091=CARTESIAN_POINT('Ctrl Pts',(2.28628943174133,1.10027388178719,9.22386341758841));
#13092=CARTESIAN_POINT('Ctrl Pts',(0.315502893378693,2.51757421040668,9.35088073751245));
#13093=CARTESIAN_POINT('Ctrl Pts',(-1.94407779652221,1.63042433179356,9.47789805743645));
#13094=CARTESIAN_POINT('Ctrl Pts',(-2.42415563699242,-0.749127110891748,
9.60491537736048));
#13095=CARTESIAN_POINT('Ctrl Pts',(-0.685293540383725,-2.44296842880613,
9.73193269728448));
#13096=CARTESIAN_POINT('Ctrl Pts',(1.68084890991805,-1.90064960544086,9.85895001720851));
#13097=CARTESIAN_POINT('Ctrl Pts',(2.50843388581605,0.381420268372014,9.98596733713252));
#13098=CARTESIAN_POINT('Ctrl Pts',(1.03993520940162,2.31435881852446,10.1129846570565));
#13099=CARTESIAN_POINT('Ctrl Pts',(-1.38046347413391,2.12885945454773,10.2400019769806));
#13100=CARTESIAN_POINT('Ctrl Pts',(-2.53726113812648,-0.00528181675498858,
10.3670192969046));
#13101=CARTESIAN_POINT('Ctrl Pts',(-1.37158825432365,-2.13458840089526,
10.4940366168286));
#13102=CARTESIAN_POINT('Ctrl Pts',(1.04956175656788,-2.31000911248967,10.6210539367526));
#13103=CARTESIAN_POINT('Ctrl Pts',(2.5100001437748,-0.370973393770508,10.7480712566766));
#13104=CARTESIAN_POINT('Ctrl Pts',(1.67292121150563,1.9076311490248,10.8750885766006));
#13105=CARTESIAN_POINT('Ctrl Pts',(-0.695458612154235,2.44009411691755,
11.0021058965247));
#13106=CARTESIAN_POINT('Ctrl Pts',(-2.42725352948809,0.739027931963853,
11.1291232164487));
#13107=CARTESIAN_POINT('Ctrl Pts',(-1.93727286780878,-1.63850413984437,
11.2561405363727));
#13108=CARTESIAN_POINT('Ctrl Pts',(0.325981782472021,-2.51623883169534,
11.3831578562967));
#13109=CARTESIAN_POINT('Ctrl Pts',(2.29085047730947,-1.0907456491988,11.5101751762207));
#13110=CARTESIAN_POINT('Ctrl Pts',(2.15879951220094,1.3331566474935,11.6371924961447));
#13111=CARTESIAN_POINT('Ctrl Pts',(0.0507011429281111,2.53676001520462,
11.7642098160688));
#13112=CARTESIAN_POINT('Ctrl Pts',(-2.10380628902285,1.41835153572837,11.8912271359927));
#13113=CARTESIAN_POINT('Ctrl Pts',(-2.33260411580082,-0.998338629716504,
12.0182444559168));
#13114=CARTESIAN_POINT('Ctrl Pts',(-0.426263277816043,-2.50120402978659,
12.1452617758408));
#13115=CARTESIAN_POINT('Ctrl Pts',(1.8702557304242,-1.71460359367715,12.2722790957648));
#13116=CARTESIAN_POINT('Ctrl Pts',(2.45484458473353,0.641451514488535,12.3992964156888));
#13117=CARTESIAN_POINT('Ctrl Pts',(0.792402511958804,2.41035686977603,12.5263137356129));
#13118=CARTESIAN_POINT('Ctrl Pts',(-1.59536162891899,1.97295292736753,12.6533310555369));
#13119=CARTESIAN_POINT('Ctrl Pts',(-2.52281869277939,-0.270384585355824,
12.7803483754609));
#13120=CARTESIAN_POINT('Ctrl Pts',(-1.14102503610327,-2.26622678644938,
12.9073656953849));
#13121=CARTESIAN_POINT('Ctrl Pts',(1.28520074497129,-2.1876885120511,13.0343830153089));
#13122=CARTESIAN_POINT('Ctrl Pts',(2.53502381630957,-0.106659417673314,
13.1614003352329));
#13123=CARTESIAN_POINT('Ctrl Pts',(1.46442426229433,2.07199989397656,13.2884176551569));
#13124=CARTESIAN_POINT('Ctrl Pts',(-0.946629440310036,2.35406344081323,
13.415434975081));
#13125=CARTESIAN_POINT('Ctrl Pts',(-2.49119015101862,0.481345626450458,
13.542452295005));
#13126=CARTESIAN_POINT('Ctrl Pts',(-1.75545118434715,-1.83196973774387,
13.669469614929));
#13127=CARTESIAN_POINT('Ctrl Pts',(0.587132112407456,-2.46839985885899,
13.796486934853));
#13128=CARTESIAN_POINT('Ctrl Pts',(2.39228667617082,-0.84539129381056,13.923504254777));
#13129=CARTESIAN_POINT('Ctrl Pts',(2.00767241251555,1.55144238199786,14.050521574701));
#13130=CARTESIAN_POINT('Ctrl Pts',(-0.214655745710225,2.52817026552183,
14.1775388946251));
#13131=CARTESIAN_POINT('Ctrl Pts',(-2.24049973451574,1.19074889051809,14.3045562145491));
#13132=CARTESIAN_POINT('Ctrl Pts',(-2.21551238886959,-1.23661911492606,
14.4315735344731));
#13133=CARTESIAN_POINT('Ctrl Pts',(-0.162565762995435,-2.53205338674698,
14.5585908543971));
#13134=CARTESIAN_POINT('Ctrl Pts',(2.03918470138136,-1.5097840025273,14.6856081743211));
#13135=CARTESIAN_POINT('Ctrl Pts',(2.37437663959469,0.8944593640754,14.8126254942451));
#13136=CARTESIAN_POINT('Ctrl Pts',(0.536193621651962,2.47996338294236,14.9396428141691));
#13137=CARTESIAN_POINT('Ctrl Pts',(-1.79279181133975,1.79544409599081,15.0666601340932));
#13138=CARTESIAN_POINT('Ctrl Pts',(-2.48075333961828,-0.532526852475886,
15.1936774540172));
#13139=CARTESIAN_POINT('Ctrl Pts',(-0.897968478795187,-2.37305174653345,
15.3206947739412));
#13140=CARTESIAN_POINT('Ctrl Pts',(1.50676778210746,-2.04141441932747,15.4477120938652));
#13141=CARTESIAN_POINT('Ctrl Pts',(2.5322909443948,0.158822396315005,15.5747294137892));
#13142=CARTESIAN_POINT('Ctrl Pts',(1.23989300331923,2.21368184727507,15.7017467337132));
#13143=CARTESIAN_POINT('Ctrl Pts',(-1.18743541036541,2.24225759600574,15.8287640536373));
#13144=CARTESIAN_POINT('Ctrl Pts',(-2.52785017273414,0.218392959692267,
15.9557813735613));
#13145=CARTESIAN_POINT('Ctrl Pts',(-1.55440867206576,-2.00537668801696,
16.0827986934853));
#13146=CARTESIAN_POINT('Ctrl Pts',(0.841853801132134,-2.39353382222907,
16.2098160134093));
#13147=CARTESIAN_POINT('Ctrl Pts',(2.46752919155041,-0.590780559498783,
16.3368333333333));
#13148=CARTESIAN_POINT('Ctrl Pts',(1.83456285720209,1.75274102582488,16.4638506532573));
#13149=CARTESIAN_POINT('Ctrl Pts',(-0.477662320434784,2.49189901245456,
16.5908679731814));
#13150=CARTESIAN_POINT('Ctrl Pts',(-2.35266144580155,0.950108468583519,
16.7178852931054));
#13151=CARTESIAN_POINT('Ctrl Pts',(-2.07416251978425,-1.46135958003407,
16.8449026130294));
#13152=CARTESIAN_POINT('Ctrl Pts',(0.10291172083272,-2.53517872315748,16.9719199329534));
#13153=CARTESIAN_POINT('Ctrl Pts',(2.18578618159046,-1.28843344764227,17.0989372528774));
#13154=CARTESIAN_POINT('Ctrl Pts',(2.26791111198236,1.13767357742987,17.2259545728015));
#13155=CARTESIAN_POINT('Ctrl Pts',(0.274113827096781,2.52241622069584,17.3529718927254));
#13156=CARTESIAN_POINT('Ctrl Pts',(-1.97059231403915,1.5982765444331,17.4799892126495));
#13157=CARTESIAN_POINT('Ctrl Pts',(-2.41152566163149,-0.788838363625875,
17.6070065325735));
#13158=CARTESIAN_POINT('Ctrl Pts',(-0.645079863170469,-2.45389363069533,
17.7340238524975));
#13159=CARTESIAN_POINT('Ctrl Pts',(1.71183688078241,-1.87278842217381,17.8610411724215));
#13160=CARTESIAN_POINT('Ctrl Pts',(2.50183145085816,0.422565228257236,17.9880584923455));
#13161=CARTESIAN_POINT('Ctrl Pts',(1.0017858777042,2.33112570143001,18.1150758122696));
#13162=CARTESIAN_POINT('Ctrl Pts',(-1.41523988373396,2.10590076977141,18.2420931321935));
#13163=CARTESIAN_POINT('Ctrl Pts',(-2.5368321958329,-0.0469509405739145,
18.3691104521176));
#13164=CARTESIAN_POINT('Ctrl Pts',(-1.33634659053169,-2.15682631906453,
18.4961277720416));
#13165=CARTESIAN_POINT('Ctrl Pts',(1.08735784373419,-2.29246044683542,18.6231450919656));
#13166=CARTESIAN_POINT('Ctrl Pts',(2.5157541762681,-0.329701236310608,18.7501624118896));
#13167=CARTESIAN_POINT('Ctrl Pts',(1.64136626161557,1.93484851496579,18.8771797318136));
#13168=CARTESIAN_POINT('Ctrl Pts',(-0.735438863258405,2.42834339808939,
19.0041970517377));
#13169=CARTESIAN_POINT('Ctrl Pts',(-2.4390633391421,0.699065095887472,19.1312143716617));
#13170=CARTESIAN_POINT('Ctrl Pts',(-1.91010217997055,-1.6700992912719,19.2582316915857));
#13171=CARTESIAN_POINT('Ctrl Pts',(0.36726240114322,-2.5105458190086,19.3852490115097));
#13172=CARTESIAN_POINT('Ctrl Pts',(2.30845499855749,-1.05297554590326,19.5122663314337));
#13173=CARTESIAN_POINT('Ctrl Pts',(2.13661371684177,1.36843114756956,19.6392836513577));
#13174=CARTESIAN_POINT('Ctrl Pts',(0.00903269875653687,2.53725055739237,
19.7663009712818));
#13175=CARTESIAN_POINT('Ctrl Pts',(-2.12681635942717,1.38360910444733,19.8933182912058));
#13176=CARTESIAN_POINT('Ctrl Pts',(-2.31589364819477,-1.0365127065718,20.0203356111298));
#13177=CARTESIAN_POINT('Ctrl Pts',(-0.385128123413262,-2.50786728300945,
20.1473529310538));
#13178=CARTESIAN_POINT('Ctrl Pts',(1.89816269343304,-1.68365684446206,20.2743702509778));
#13179=CARTESIAN_POINT('Ctrl Pts',(2.44397884352426,0.681681298722785,20.4013875709018));
#13180=CARTESIAN_POINT('Ctrl Pts',(0.752709973788363,2.42304553733211,20.5284048908259));
#13181=CARTESIAN_POINT('Ctrl Pts',(-1.62754857814452,1.94648596359704,20.6554222107499));
#13182=CARTESIAN_POINT('Ctrl Pts',(-2.51803787410739,-0.311780764473142,
20.7824395306739));
#13183=CARTESIAN_POINT('Ctrl Pts',(-1.10365255043497,-2.28466037487492,
20.9094568505979));
#13184=CARTESIAN_POINT('Ctrl Pts',(1.32095616145559,-2.16628640778953,21.0364741705219));
#13185=CARTESIAN_POINT('Ctrl Pts',(2.53643360399821,-0.065011940227747,
21.1634914904459));
#13186=CARTESIAN_POINT('Ctrl Pts',(1.43019797890608,2.09577091348664,21.29050881037));
#13187=CARTESIAN_POINT('Ctrl Pts',(-0.985162921529244,2.33819930745395,
21.417526130294));
#13188=CARTESIAN_POINT('Ctrl Pts',(-2.49875937979054,0.440367501970874,
21.544543450218));
#13189=CARTESIAN_POINT('Ctrl Pts',(-1.72512770486239,-1.86055270945033,
21.671560770142));
#13190=CARTESIAN_POINT('Ctrl Pts',(0.627591846786366,-2.45842438790134,
21.798578090066));
#13191=CARTESIAN_POINT('Ctrl Pts',(2.40584801674221,-0.805988374111369,
21.9255954099901));
#13192=CARTESIAN_POINT('Ctrl Pts',(1.98192207241512,1.58420544935872,22.052612729914));
#13193=CARTESIAN_POINT('Ctrl Pts',(-0.256147356548822,2.52430398518738,
22.1796300498381));
#13194=CARTESIAN_POINT('Ctrl Pts',(-2.25975336601507,1.15379218630468,22.3066473697621));
#13195=CARTESIAN_POINT('Ctrl Pts',(-2.19490448971053,-1.27283797902012,
22.4336646896861));
#13196=CARTESIAN_POINT('Ctrl Pts',(-0.120959350332131,-2.53438184879942,
22.5606820096101));
#13197=CARTESIAN_POINT('Ctrl Pts',(2.06370475579857,-1.47609031131966,22.6876993295342));
#13198=CARTESIAN_POINT('Ctrl Pts',(2.3593672133321,0.933333070706771,22.8147166494581));
#13199=CARTESIAN_POINT('Ctrl Pts',(0.495391241924784,2.48843569837242,22.9417339693822));
#13200=CARTESIAN_POINT('Ctrl Pts',(-1.8220345208464,1.76575713307529,23.0687512893062));
#13201=CARTESIAN_POINT('Ctrl Pts',(-2.47167748058067,-0.573193949289761,
23.1957686092302));
#13202=CARTESIAN_POINT('Ctrl Pts',(-0.858865819404909,-2.38748466016789,
23.3227859291542));
#13203=CARTESIAN_POINT('Ctrl Pts',(1.54007474576711,-2.01638275912753,23.4498032490782));
#13204=CARTESIAN_POINT('Ctrl Pts',(2.5293720748911,0.20036927497846,23.5768205690023));
#13205=CARTESIAN_POINT('Ctrl Pts',(1.20331104687244,2.23378417110109,23.7038378889263));
#13206=CARTESIAN_POINT('Ctrl Pts',(-1.22398765677242,2.22238150937836,23.8308552088503));
#13207=CARTESIAN_POINT('Ctrl Pts',(-2.53131035466268,0.17698584825274,23.9578725287743));
#13208=CARTESIAN_POINT('Ctrl Pts',(-1.52085574922736,-2.03089691367622,
24.0848898486983));
#13209=CARTESIAN_POINT('Ctrl Pts',(0.880268793849252,-2.37888302119466,
24.2119071686224));
#13210=CARTESIAN_POINT('Ctrl Pts',(2.47840753722132,-0.551152661267064,
24.3389244885463));
#13211=CARTESIAN_POINT('Ctrl Pts',(1.80247117904166,1.78466636739888,24.4659418084704));
#13212=CARTESIAN_POINT('Ctrl Pts',(0.260068348103614,2.24724247875885,24.550620021753));
#13213=CARTESIAN_POINT('Ctrl Pts',(-0.438698668031391,2.10136176239249,
24.5929591283944));
#13214=CARTESIAN_POINT('Ctrl Pts',(-1.00843926415924,2.06555938931316,-0.0877091283943953));
#13215=CARTESIAN_POINT('Ctrl Pts',(-1.69530089691146,1.73022251006604,-0.0453700217530565));
#13216=CARTESIAN_POINT('Ctrl Pts',(-2.6963494230853,0.326343980522267,0.0393081915296206));
#13217=CARTESIAN_POINT('Ctrl Pts',(-1.73467057286262,-2.09329006364291,
0.166325511453637));
#13218=CARTESIAN_POINT('Ctrl Pts',(0.817104130456275,-2.59020573181402,
0.293342831377653));
#13219=CARTESIAN_POINT('Ctrl Pts',(2.6197787205207,-0.719511570048316,0.42036015130167));
#13220=CARTESIAN_POINT('Ctrl Pts',(2.02506070583922,1.81151053307878,0.547377471225686));
#13221=CARTESIAN_POINT('Ctrl Pts',(-0.423607444922901,2.68347044489473,
0.674394791149703));
#13222=CARTESIAN_POINT('Ctrl Pts',(-2.48436049093747,1.09960225065647,0.801412111073719));
#13223=CARTESIAN_POINT('Ctrl Pts',(-2.27115352524731,-1.49103098724893,
0.928429430997735));
#13224=CARTESIAN_POINT('Ctrl Pts',(0.0209898731557613,-2.71672496221751,
1.05544675092175));
#13225=CARTESIAN_POINT('Ctrl Pts',(2.29389598308821,-1.45574564269816,1.18246407084577));
#13226=CARTESIAN_POINT('Ctrl Pts',(2.46710750249518,1.13777993581432,1.30948139076978));
#13227=CARTESIAN_POINT('Ctrl Pts',(0.382056589353797,2.68982485308583,1.4364987106938));
#13228=CARTESIAN_POINT('Ctrl Pts',(-2.05270458389693,1.77976064955236,1.56351603061782));
#13229=CARTESIAN_POINT('Ctrl Pts',(-2.60853371400369,-0.759404660038483,
1.69053335054183));
#13230=CARTESIAN_POINT('Ctrl Pts',(-0.776652295721961,-2.60344959776366,
1.81755067046585));
#13231=CARTESIAN_POINT('Ctrl Pts',(1.76613379221813,-2.06444011739318,1.94456799038987));
#13232=CARTESIAN_POINT('Ctrl Pts',(2.69229754033851,0.364246075308452,2.07158531031388));
#13233=CARTESIAN_POINT('Ctrl Pts',(1.1540787283172,2.45952086820838,2.1986026302379));
#13234=CARTESIAN_POINT('Ctrl Pts',(-1.44052077277774,2.30348452711858,2.32561995016191));
#13235=CARTESIAN_POINT('Ctrl Pts',(-2.71654611535792,0.038963896273717,
2.45263727008594));
#13236=CARTESIAN_POINT('Ctrl Pts',(-1.50599319393492,-2.2612221040603,2.57965459000994));
#13237=CARTESIAN_POINT('Ctrl Pts',(1.08306379965016,-2.49160867248817,2.70667190993397));
#13238=CARTESIAN_POINT('Ctrl Pts',(2.68074323100002,-0.441312455983457,
2.83368922985798));
#13239=CARTESIAN_POINT('Ctrl Pts',(1.82461642455265,2.01293711988686,2.960706549782));
#13240=CARTESIAN_POINT('Ctrl Pts',(-0.701664801341637,2.62465377937989,
3.08772386970601));
#13241=CARTESIAN_POINT('Ctrl Pts',(-2.58568031441742,0.833905428481168,
3.21474118963003));
#13242=CARTESIAN_POINT('Ctrl Pts',(-2.1029050044713,-1.72015449691165,3.34175850955404));
#13243=CARTESIAN_POINT('Ctrl Pts',(0.304754923672212,-2.69967875662022,
3.46877582947807));
#13244=CARTESIAN_POINT('Ctrl Pts',(2.43345880602631,-1.20806423310154,3.59579314940208));
#13245=CARTESIAN_POINT('Ctrl Pts',(2.33470713739251,1.38934644148024,3.72281046932609));
#13246=CARTESIAN_POINT('Ctrl Pts',(0.0988918126922846,2.71502511248385,
3.84982778925011));
#13247=CARTESIAN_POINT('Ctrl Pts',(-2.22744368708483,1.55551778286699,3.97684510917413));
#13248=CARTESIAN_POINT('Ctrl Pts',(-2.51489864657596,-1.02782573882757,
4.10386242909814));
#13249=CARTESIAN_POINT('Ctrl Pts',(-0.500352464133315,-2.67035360272895,
4.23087974902216));
#13250=CARTESIAN_POINT('Ctrl Pts',(1.97218909135587,-1.86858533117836,4.35789706894617));
#13251=CARTESIAN_POINT('Ctrl Pts',(2.63949625037973,0.643584101878016,4.48491438887019));
#13252=CARTESIAN_POINT('Ctrl Pts',(0.890752412363458,2.56665172780235,4.61193170879421));
#13253=CARTESIAN_POINT('Ctrl Pts',(-1.67333763184596,2.14034626212867,4.73894902871823));
#13254=CARTESIAN_POINT('Ctrl Pts',(-2.70574561618272,-0.245115508420684,
4.86596634864224));
#13255=CARTESIAN_POINT('Ctrl Pts',(-1.26146154506521,-2.40621190302983,
4.99298366856626));
#13256=CARTESIAN_POINT('Ctrl Pts',(1.33749566614299,-2.36479307657332,5.12000098849026));
#13257=CARTESIAN_POINT('Ctrl Pts',(2.71218224720435,-0.158771565181015,
5.2470183084143));
#13258=CARTESIAN_POINT('Ctrl Pts',(1.60428503161449,2.19258078284432,5.37403562833829));
#13259=CARTESIAN_POINT('Ctrl Pts',(-0.97208725743388,2.53696419286815,5.50105294826233));
#13260=CARTESIAN_POINT('Ctrl Pts',(-2.65866385641605,0.559148862600505,
5.62807026818633));
#13261=CARTESIAN_POINT('Ctrl Pts',(-1.91164447655709,-1.93048085906317,
5.75508758811036));
#13262=CARTESIAN_POINT('Ctrl Pts',(0.585190059473756,-2.65305362672027,
5.88210490803437));
#13263=CARTESIAN_POINT('Ctrl Pts',(2.54637351191372,-0.947165714003964,
6.00912222795839));
#13264=CARTESIAN_POINT('Ctrl Pts',(2.17674544627999,1.62570606631697,6.1361395478824));
#13265=CARTESIAN_POINT('Ctrl Pts',(-0.185356753398145,2.71049512560532,
6.26315686780642));
#13266=CARTESIAN_POINT('Ctrl Pts',(-2.3777934842235,1.31424468739453,6.39017418773043));
#13267=CARTESIAN_POINT('Ctrl Pts',(-2.39372766556092,-1.28499370235373,
6.51719150765445));
#13268=CARTESIAN_POINT('Ctrl Pts',(-0.218574016335755,-2.70801889789258,
6.64420882757846));
#13269=CARTESIAN_POINT('Ctrl Pts',(2.15665037366779,-1.65227119980924,6.7712261475025));
#13270=CARTESIAN_POINT('Ctrl Pts',(2.55779456377756,0.915875494524468,6.8982434674265));
#13271=CARTESIAN_POINT('Ctrl Pts',(0.617673027462724,2.6456796826346,7.02526078735052));
#13272=CARTESIAN_POINT('Ctrl Pts',(-1.88783273079667,1.95377289685707,7.15227810727453));
#13273=CARTESIAN_POINT('Ctrl Pts',(-2.66531930705065,-0.526511104748562,
7.27929542719855));
#13274=CARTESIAN_POINT('Ctrl Pts',(-1.00311786772006,-2.52485553951532,
7.40631274712256));
#13275=CARTESIAN_POINT('Ctrl Pts',(1.57728299095268,-2.21208483526556,7.53333006704659));
#13276=CARTESIAN_POINT('Ctrl Pts',(2.71392497239329,0.125507753468168,7.66034738697059));
#13277=CARTESIAN_POINT('Ctrl Pts',(1.36638796153508,2.34821738570612,7.78736470689462));
#13278=CARTESIAN_POINT('Ctrl Pts',(-1.2318661118446,2.42149681693976,7.91438202681864));
#13279=CARTESIAN_POINT('Ctrl Pts',(-2.70253709155071,0.278270050046848,
8.04139934674264));
#13280=CARTESIAN_POINT('Ctrl Pts',(-1.69945292436414,-2.11966995304237,
8.16841666666667));
#13281=CARTESIAN_POINT('Ctrl Pts',(0.859217818004418,-2.57737961759307,
8.29543398659068));
#13282=CARTESIAN_POINT('Ctrl Pts',(2.63140740300587,-0.675896464975523,
8.42245130651469));
#13283=CARTESIAN_POINT('Ctrl Pts',(1.99495008095517,1.84426547071115,8.54946862643872));
#13284=CARTESIAN_POINT('Ctrl Pts',(-0.467575806809516,2.67628731956173,
8.67648594636272));
#13285=CARTESIAN_POINT('Ctrl Pts',(-2.50210828709286,1.05858163200661,8.80350326628676));
#13286=CARTESIAN_POINT('Ctrl Pts',(-2.24634722334667,-1.52809198156497,
8.93052058621076));
#13287=CARTESIAN_POINT('Ctrl Pts',(0.0655976473989457,-2.71603348665222,
9.05753790613478));
#13288=CARTESIAN_POINT('Ctrl Pts',(2.31749800723498,-1.41786598041648,9.18455522605879));
#13289=CARTESIAN_POINT('Ctrl Pts',(2.44808701070344,1.17813876092146,9.31157254598281));
#13290=CARTESIAN_POINT('Ctrl Pts',(0.337830602021103,2.69573949711365,9.43858986590683));
#13291=CARTESIAN_POINT('Ctrl Pts',(-2.08165752567829,1.74580723384554,9.56560718583084));
#13292=CARTESIAN_POINT('Ctrl Pts',(-2.59570981891155,-0.802141812877639,
9.69262450575486));
#13293=CARTESIAN_POINT('Ctrl Pts',(-0.733790827810694,-2.61585396629502,
9.81964182567887));
#13294=CARTESIAN_POINT('Ctrl Pts',(1.7998002904608,-2.03515598085693,9.9466591456029));
#13295=CARTESIAN_POINT('Ctrl Pts',(2.68595232424161,0.408412859569337,10.0736764655269));
#13296=CARTESIAN_POINT('Ctrl Pts',(1.11353000314147,2.47814282963356,10.2006937854509));
#13297=CARTESIAN_POINT('Ctrl Pts',(-1.47815698785079,2.27951592914556,10.3277111053749));
#13298=CARTESIAN_POINT('Ctrl Pts',(-2.71681964180679,-0.00565560370938429,
10.454728425299));
#13299=CARTESIAN_POINT('Ctrl Pts',(-1.46865368086213,-2.28565030519776,
10.581745745223));
#13300=CARTESIAN_POINT('Ctrl Pts',(1.12383780789645,-2.47348530084635,10.708763065147));
#13301=CARTESIAN_POINT('Ctrl Pts',(2.68762942413589,-0.397226673927448,
10.835780385071));
#13302=CARTESIAN_POINT('Ctrl Pts',(1.79131155966456,2.04263159874036,10.962797704995));
#13303=CARTESIAN_POINT('Ctrl Pts',(-0.744675267820305,2.6127762432817,11.089815024919));
#13304=CARTESIAN_POINT('Ctrl Pts',(-2.59902694502602,0.791327928857071,
11.2168323448431));
#13305=CARTESIAN_POINT('Ctrl Pts',(-2.07437102145842,-1.75445883887142,
11.3438496647671));
#13306=CARTESIAN_POINT('Ctrl Pts',(0.349051067776654,-2.69430961547564,
11.4708669846911));
#13307=CARTESIAN_POINT('Ctrl Pts',(2.45297083523399,-1.16793622833267,11.5978843046151));
#13308=CARTESIAN_POINT('Ctrl Pts',(2.31157480376701,1.42750232173191,11.7249016245391));
#13309=CARTESIAN_POINT('Ctrl Pts',(0.0542891935320357,2.7162830551005,11.8519189444631));
#13310=CARTESIAN_POINT('Ctrl Pts',(-2.25268978533066,1.51872633579173,11.9789362643872));
#13311=CARTESIAN_POINT('Ctrl Pts',(-2.49767932166667,-1.06898969035214,
12.1059535843112));
#13312=CARTESIAN_POINT('Ctrl Pts',(-0.456429347515495,-2.67821082118026,
12.2329709042352));
#13313=CARTESIAN_POINT('Ctrl Pts',(2.00261117283739,-1.83594374706507,12.3599882241592));
#13314=CARTESIAN_POINT('Ctrl Pts',(2.62857058154909,0.686846161651322,12.4870055440832));
#13315=CARTESIAN_POINT('Ctrl Pts',(0.848479754944057,2.58093453179474,12.6140228640072));
#13316=CARTESIAN_POINT('Ctrl Pts',(-1.70826319140036,2.11257611007679,12.7410401839312));
#13317=CARTESIAN_POINT('Ctrl Pts',(-2.70135512433749,-0.289519332991871,
12.8680575038553));
#13318=CARTESIAN_POINT('Ctrl Pts',(-1.22177381874362,-2.42660455941901,
12.9950748237793));
#13319=CARTESIAN_POINT('Ctrl Pts',(1.37615264551801,-2.34250823866091,13.1220921437033));
#13320=CARTESIAN_POINT('Ctrl Pts',(2.7144239877821,-0.11420755891623,13.2491094636273));
#13321=CARTESIAN_POINT('Ctrl Pts',(1.56805956626024,2.21863249516909,13.3761267835513));
#13322=CARTESIAN_POINT('Ctrl Pts',(-1.0136211122699,2.52065729378692,13.5031441034754));
#13323=CARTESIAN_POINT('Ctrl Pts',(-2.66748827389544,0.515409798694957,
13.6301614233994));
#13324=CARTESIAN_POINT('Ctrl Pts',(-1.8796820659102,-1.96161573277134,13.7571787433234));
#13325=CARTESIAN_POINT('Ctrl Pts',(0.628682649710236,-2.64308514390169,
13.8841960632474));
#13326=CARTESIAN_POINT('Ctrl Pts',(2.56158553528029,-0.905218480480427,
14.0112133831714));
#13327=CARTESIAN_POINT('Ctrl Pts',(2.14975264574595,1.66123583938849,14.1382307030954));
#13328=CARTESIAN_POINT('Ctrl Pts',(-0.229846639515761,2.70708542057022,
14.2652480230195));
#13329=CARTESIAN_POINT('Ctrl Pts',(-2.399056839175,1.27501656238973,14.3922653429435));
#13330=CARTESIAN_POINT('Ctrl Pts',(-2.37230117322164,-1.32413295989931,
14.5192826628675));
#13331=CARTESIAN_POINT('Ctrl Pts',(-0.174070319903033,-2.71124334497834,
14.6462999827915));
#13332=CARTESIAN_POINT('Ctrl Pts',(2.18349501623457,-1.61662935332725,14.7733173027155));
#13333=CARTESIAN_POINT('Ctrl Pts',(2.54240802988898,0.957759031028439,14.9003346226395));
#13334=CARTESIAN_POINT('Ctrl Pts',(0.574139311569299,2.65546700278335,15.0273519425636));
#13335=CARTESIAN_POINT('Ctrl Pts',(-1.91966523805065,1.92250522126218,15.1543692624876));
#13336=CARTESIAN_POINT('Ctrl Pts',(-2.65631286361378,-0.570213050149194,
15.2813865824116));
#13337=CARTESIAN_POINT('Ctrl Pts',(-0.961516481001816,-2.54098937595623,
15.4084039023356));
#13338=CARTESIAN_POINT('Ctrl Pts',(1.61339967910989,-2.18588252827287,15.5354212222596));
#13339=CARTESIAN_POINT('Ctrl Pts',(2.71149771425628,0.17006204027786,15.6624385421836));
#13340=CARTESIAN_POINT('Ctrl Pts',(1.32763853690037,2.37034108669987,15.7894558621077));
#13341=CARTESIAN_POINT('Ctrl Pts',(-1.27146859177446,2.40093910212058,15.9164731820316));
#13342=CARTESIAN_POINT('Ctrl Pts',(-2.70674267525333,0.233848331024494,
16.0434905019557));
#13343=CARTESIAN_POINT('Ctrl Pts',(-1.66441204975114,-2.14729445596166,
16.1705078218797));
#13344=CARTESIAN_POINT('Ctrl Pts',(0.901430644279058,-2.56292094016088,
16.2975251418037));
#13345=CARTESIAN_POINT('Ctrl Pts',(2.64215286065742,-0.632589292416696,
16.4245424617277));
#13346=CARTESIAN_POINT('Ctrl Pts',(1.96439236375018,1.87678011317268,16.5515597816518));
#13347=CARTESIAN_POINT('Ctrl Pts',(-0.511465830145711,2.66824730048656,
16.6785771015757));
#13348=CARTESIAN_POINT('Ctrl Pts',(-2.51915608150405,1.01734634662028,16.8055944214998));
#13349=CARTESIAN_POINT('Ctrl Pts',(-2.22094816705002,-1.56477800062425,
16.9326117414238));
#13350=CARTESIAN_POINT('Ctrl Pts',(0.110194642691373,-2.71458985717596,
17.0596290613478));
#13351=CARTESIAN_POINT('Ctrl Pts',(2.34047128287306,-1.3796141221396,17.1866463812718));
#13352=CARTESIAN_POINT('Ctrl Pts',(2.42840808236836,1.2181851819196,17.3136637011959));
#13353=CARTESIAN_POINT('Ctrl Pts',(0.293512488074909,2.70092416985456,17.4406810211198));
#13354=CARTESIAN_POINT('Ctrl Pts',(-2.11004843936889,1.71138439150223,17.5676983410439));
#13355=CARTESIAN_POINT('Ctrl Pts',(-2.58218603745268,-0.844663376703935,
17.6947156609679));
#13356=CARTESIAN_POINT('Ctrl Pts',(-0.690731283611418,-2.62755232979307,
17.8217329808919));
#13357=CARTESIAN_POINT('Ctrl Pts',(1.83298123767942,-2.00532309972126,17.9487503008159));
#13358=CARTESIAN_POINT('Ctrl Pts',(2.67888264398372,0.45246959204271,18.0757676207399));
#13359=CARTESIAN_POINT('Ctrl Pts',(1.07268089536934,2.49609628193107,18.2027849406639));
#13360=CARTESIAN_POINT('Ctrl Pts',(-1.51539447643767,2.25493248961973,18.329802260588));
#13361=CARTESIAN_POINT('Ctrl Pts',(-2.71636034385321,-0.050273594481799,
18.456819580512));
#13362=CARTESIAN_POINT('Ctrl Pts',(-1.43091801267993,-2.30946197044866,
18.583836900436));
#13363=CARTESIAN_POINT('Ctrl Pts',(1.16430867250469,-2.45469474010331,18.71085422036));
#13364=CARTESIAN_POINT('Ctrl Pts',(2.69379066164609,-0.353033742280847,
18.837871540284));
#13365=CARTESIAN_POINT('Ctrl Pts',(1.75752350908935,2.07177510047756,18.9648888602081));
#13366=CARTESIAN_POINT('Ctrl Pts',(-0.78748486666372,2.60019394213895,19.091906180132));
#13367=CARTESIAN_POINT('Ctrl Pts',(-2.61167251877161,0.748536977479163,
19.2189235000561));
#13368=CARTESIAN_POINT('Ctrl Pts',(-2.04527750116953,-1.78828993599198,
19.3459408199801));
#13369=CARTESIAN_POINT('Ctrl Pts',(0.393253059422915,-2.68821371606033,
19.4729581399041));
#13370=CARTESIAN_POINT('Ctrl Pts',(2.47182120439486,-1.12749318643823,19.5999754598281));
#13371=CARTESIAN_POINT('Ctrl Pts',(2.28781894998626,1.46527314997717,19.7269927797521));
#13372=CARTESIAN_POINT('Ctrl Pts',(0.00967193050468428,2.71680831228858,
19.8540100996762));
#13373=CARTESIAN_POINT('Ctrl Pts',(-2.27732824697515,1.48152523012306,19.9810274196002));
#13374=CARTESIAN_POINT('Ctrl Pts',(-2.47978627710233,-1.10986529446316,
20.1080447395242));
#13375=CARTESIAN_POINT('Ctrl Pts',(-0.412383114445153,-2.68534562372864,
20.2350620594482));
#13376=CARTESIAN_POINT('Ctrl Pts',(2.03249307348463,-1.80280693869551,20.3620793793722));
#13377=CARTESIAN_POINT('Ctrl Pts',(2.61693588668204,0.729922952743455,20.4890966992963));
#13378=CARTESIAN_POINT('Ctrl Pts',(0.805978230085543,2.59452115901522,20.6161140192202));
#13379=CARTESIAN_POINT('Ctrl Pts',(-1.74272796704041,2.08423611544629,20.7431313391443));
#13380=CARTESIAN_POINT('Ctrl Pts',(-2.69623597366087,-0.333845063139111,
20.8701486590683));
#13381=CARTESIAN_POINT('Ctrl Pts',(-1.18175653333257,-2.44634266770867,
20.9971659789923));
#13382=CARTESIAN_POINT('Ctrl Pts',(1.41443842396857,-2.31959153672586,21.1241832989163));
#13383=CARTESIAN_POINT('Ctrl Pts',(2.71593354421905,-0.0696127464014399,
21.2512006188403));
#13384=CARTESIAN_POINT('Ctrl Pts',(1.53141113556543,2.24408575724777,21.3782179387644));
#13385=CARTESIAN_POINT('Ctrl Pts',(-1.05488155530054,2.50367047738749,21.5052352586884));
#13386=CARTESIAN_POINT('Ctrl Pts',(-2.67559316664451,0.471531708340905,
21.6322525786124));
#13387=CARTESIAN_POINT('Ctrl Pts',(-1.84721263521812,-1.99222148232799,
21.7592698985364));
#13388=CARTESIAN_POINT('Ctrl Pts',(0.67200566420455,-2.63240372249544,21.8862872184604));
#13389=CARTESIAN_POINT('Ctrl Pts',(2.57610659339288,-0.863027069996625,
22.0133045383844));
#13390=CARTESIAN_POINT('Ctrl Pts',(2.12217998926342,1.69631750425708,22.1403218583085));
#13391=CARTESIAN_POINT('Ctrl Pts',(-0.274274554956796,2.70294552885961,
22.2673391782324));
#13392=CARTESIAN_POINT('Ctrl Pts',(-2.41967302386623,1.23544448271899,22.3943564981565));
#13393=CARTESIAN_POINT('Ctrl Pts',(-2.35023488119896,-1.36291498351369,
22.5213738180805));
#13394=CARTESIAN_POINT('Ctrl Pts',(-0.129519478269032,-2.71373658910848,
22.6483911380045));
#13395=CARTESIAN_POINT('Ctrl Pts',(2.20975032139722,-1.58055120563391,22.7754084579285));
#13396=CARTESIAN_POINT('Ctrl Pts',(2.52633640703956,0.999383776758762,22.9024257778525));
#13397=CARTESIAN_POINT('Ctrl Pts',(0.530449403183637,2.66453889239932,23.0294430977766));
#13398=CARTESIAN_POINT('Ctrl Pts',(-1.95097741415011,1.89071735254717,23.1564604177006));
#13399=CARTESIAN_POINT('Ctrl Pts',(-2.64659471843386,-0.613758101834641,
23.2834777376246));
#13400=CARTESIAN_POINT('Ctrl Pts',(-0.9196465798387,-2.55644368716658,23.4104950575486));
#13401=CARTESIAN_POINT('Ctrl Pts',(1.64906373107512,-2.15907941168533,23.5375123774727));
#13402=CARTESIAN_POINT('Ctrl Pts',(2.70837228034631,0.214549134772193,23.6645296973966));
#13403=CARTESIAN_POINT('Ctrl Pts',(1.28846772538361,2.39186602451404,23.7915470173207));
#13404=CARTESIAN_POINT('Ctrl Pts',(-1.31060759071252,2.37965641200244,23.9185643372446));
#13405=CARTESIAN_POINT('Ctrl Pts',(-2.71044772952875,0.189510894889534,
24.0455816571687));
#13406=CARTESIAN_POINT('Ctrl Pts',(-1.62848463241217,-2.17462071311847,
24.1725989770927));
#13407=CARTESIAN_POINT('Ctrl Pts',(0.942564213538227,-2.54723332195699,
24.2996162970167));
#13408=CARTESIAN_POINT('Ctrl Pts',(2.65380105198664,-0.590156981977038,
24.4266336169407));
#13409=CARTESIAN_POINT('Ctrl Pts',(1.93002960137832,1.91096476754518,24.5536509368648));
#13410=CARTESIAN_POINT('Ctrl Pts',(0.278473029725979,2.4062767582145,24.6383291501474));
#13411=CARTESIAN_POINT('Ctrl Pts',(-0.469744773303982,2.25007226289099,
24.6806682567888));
#13412=CARTESIAN_POINT('Ctrl Pts',(-1.0750884603512,2.20207516956613,-4.71844785465692E-15));
#13413=CARTESIAN_POINT('Ctrl Pts',(-1.8073457627734,1.84457539538852,0.0423391066413341));
#13414=CARTESIAN_POINT('Ctrl Pts',(-2.87455502067384,0.347912521888007,
0.127017319924011));
#13415=CARTESIAN_POINT('Ctrl Pts',(-1.84931743702996,-2.231638603904,0.254034639848028));
#13416=CARTESIAN_POINT('Ctrl Pts',(0.871107713453866,-2.76139614072881,
0.381051959772044));
#13417=CARTESIAN_POINT('Ctrl Pts',(2.79292365064105,-0.76706512086575,0.508069279696061));
#13418=CARTESIAN_POINT('Ctrl Pts',(2.15889987006154,1.93123586033844,0.635086599620076));
#13419=CARTESIAN_POINT('Ctrl Pts',(-0.451604268042042,2.8608248523574,0.762103919544093));
#13420=CARTESIAN_POINT('Ctrl Pts',(-2.64855543619286,1.17227653927431,0.88912123946811));
#13421=CARTESIAN_POINT('Ctrl Pts',(-2.4212573165871,-1.58957536203614,1.01613855939212));
#13422=CARTESIAN_POINT('Ctrl Pts',(0.0223771239538552,-2.89627720838807,
1.14315587931614));
#13423=CARTESIAN_POINT('Ctrl Pts',(2.44550285605961,-1.5519579584955,1.27017319924016));
#13424=CARTESIAN_POINT('Ctrl Pts',(2.63016217301863,1.21297744235786,1.39719051916418));
#13425=CARTESIAN_POINT('Ctrl Pts',(0.407307256880577,2.86759923249254,1.52420783908819));
#13426=CARTESIAN_POINT('Ctrl Pts',(-2.18837077163737,1.89738758150803,1.65122515901221));
#13427=CARTESIAN_POINT('Ctrl Pts',(-2.78093544552777,-0.809594802345376,
1.77824247893622));
#13428=CARTESIAN_POINT('Ctrl Pts',(-0.8279823589892,-2.77551531275925,1.90525979886024));
#13429=CARTESIAN_POINT('Ctrl Pts',(1.88286010564359,-2.20088192336089,2.03227711878425));
#13430=CARTESIAN_POINT('Ctrl Pts',(2.87023534318944,0.388319620437272,2.15929443870827));
#13431=CARTESIAN_POINT('Ctrl Pts',(1.23035344541546,2.62207412719922,2.28631175863229));
#13432=CARTESIAN_POINT('Ctrl Pts',(-1.53572685510289,2.45572512070654,2.41332907855631));
#13433=CARTESIAN_POINT('Ctrl Pts',(-2.89608654128322,0.0415390760187077,
2.54034639848032));
#13434=CARTESIAN_POINT('Ctrl Pts',(-1.60552644240473,-2.41066951354087,
2.66736371840434));
#13435=CARTESIAN_POINT('Ctrl Pts',(1.15464503833931,-2.65628266044979,2.79438103832835));
#13436=CARTESIAN_POINT('Ctrl Pts',(2.85791739298796,-0.470479428657096,
2.92139835825237));
#13437=CARTESIAN_POINT('Ctrl Pts',(1.94520793896221,2.14597501893897,3.04841567817639));
#13438=CARTESIAN_POINT('Ctrl Pts',(-0.748038833638585,2.79812090912681,
3.1754329981004));
#13439=CARTESIAN_POINT('Ctrl Pts',(-2.75657163201098,0.889019433343594,
3.30245031802442));
#13440=CARTESIAN_POINT('Ctrl Pts',(-2.24188900995115,-1.83384197281603,
3.42946763794843));
#13441=CARTESIAN_POINT('Ctrl Pts',(0.324896613330893,-2.87810439463344,
3.55648495787245));
#13442=CARTESIAN_POINT('Ctrl Pts',(2.59428958597723,-1.2879069295792,3.68350227779647));
#13443=CARTESIAN_POINT('Ctrl Pts',(2.48901127803951,1.48117033891052,3.81051959772048));
#13444=CARTESIAN_POINT('Ctrl Pts',(0.105427714317817,2.8944650131494,3.9375369176445));
#13445=CARTESIAN_POINT('Ctrl Pts',(-2.37465863257865,1.65832418239444,4.06455423756852));
#13446=CARTESIAN_POINT('Ctrl Pts',(-2.68111190230259,-1.09575621491369,
4.19157155749253));
#13447=CARTESIAN_POINT('Ctrl Pts',(-0.533421475557533,-2.84684109929477,
4.31858887741655));
#13448=CARTESIAN_POINT('Ctrl Pts',(2.10253389480519,-1.99208281363993,4.44560619734056));
#13449=CARTESIAN_POINT('Ctrl Pts',(2.8139443403062,0.68611949751027,4.57262351726459));
#13450=CARTESIAN_POINT('Ctrl Pts',(0.949623515859734,2.7362854188361,4.69964083718859));
#13451=CARTESIAN_POINT('Ctrl Pts',(-1.78393091404354,2.28180481398525,4.82665815711262));
#13452=CARTESIAN_POINT('Ctrl Pts',(-2.88457222163901,-0.261315543654406,
4.95367547703663));
#13453=CARTESIAN_POINT('Ctrl Pts',(-1.34483334641579,-2.56524189611339,
5.08069279696065));
#13454=CARTESIAN_POINT('Ctrl Pts',(1.42589267152236,-2.52108564005781,5.20771011688467));
#13455=CARTESIAN_POINT('Ctrl Pts',(2.89143425882939,-0.169265005463949,
5.33472743680867));
#13456=CARTESIAN_POINT('Ctrl Pts',(1.71031452850143,2.33749158903385,5.4617447567327));
#13457=CARTESIAN_POINT('Ctrl Pts',(-1.03633389740425,2.704635792172,5.58876207665671));
#13458=CARTESIAN_POINT('Ctrl Pts',(-2.83437876089513,0.596103812262253,
5.71577939658073));
#13459=CARTESIAN_POINT('Ctrl Pts',(-2.03798779964606,-2.05806910566698,
5.84279671650474));
#13460=CARTESIAN_POINT('Ctrl Pts',(0.62386610915731,-2.82839774307856,5.96981403642876));
#13461=CARTESIAN_POINT('Ctrl Pts',(2.7146669865981,-1.00976525345321,6.09683135635278));
#13462=CARTESIAN_POINT('Ctrl Pts',(2.32060967238186,1.73315131008656,6.2238486762768));
#13463=CARTESIAN_POINT('Ctrl Pts',(-0.197607246870416,2.88963563294601,
6.35086599620081));
#13464=CARTESIAN_POINT('Ctrl Pts',(-2.53494526328089,1.40110500226672,6.47788331612483));
#13465=CARTESIAN_POINT('Ctrl Pts',(-2.5519325574986,-1.36992077770418,6.60490063604884));
#13466=CARTESIAN_POINT('Ctrl Pts',(-0.233019886320138,-2.88699574779499,
6.73191795597286));
#13467=CARTESIAN_POINT('Ctrl Pts',(2.29918648762192,-1.76147217132255,6.85893527589687));
#13468=CARTESIAN_POINT('Ctrl Pts',(2.72684287214744,0.976407018525444,6.98595259582089));
#13469=CARTESIAN_POINT('Ctrl Pts',(0.658495923052897,2.82053644446047,7.11296991574491));
#13470=CARTESIAN_POINT('Ctrl Pts',(-2.01260230148307,2.08290054761913,7.23998723566893));
#13471=CARTESIAN_POINT('Ctrl Pts',(-2.84147407980028,-0.561308978219811,
7.36700455559294));
#13472=CARTESIAN_POINT('Ctrl Pts',(-1.06941536519506,-2.69172686056585,
7.49402187551696));
#13473=CARTESIAN_POINT('Ctrl Pts',(1.68152788427493,-2.35828469223139,7.62103919544097));
#13474=CARTESIAN_POINT('Ctrl Pts',(2.89329216322361,0.133802740763723,7.74805651536499));
#13475=CARTESIAN_POINT('Ctrl Pts',(1.45669450012326,2.50341443802613,7.87507383528901));
#13476=CARTESIAN_POINT('Ctrl Pts',(-1.31328190859961,2.58153701188885,8.00209115521302));
#13477=CARTESIAN_POINT('Ctrl Pts',(-2.88115164101586,0.296661316451321,
8.12910847513705));
#13478=CARTESIAN_POINT('Ctrl Pts',(-1.81177220367078,-2.25976197799966,
8.25612579506105));
#13479=CARTESIAN_POINT('Ctrl Pts',(0.91600475496642,-2.74772233023752,8.38314311498508));
#13480=CARTESIAN_POINT('Ctrl Pts',(2.80532088941706,-0.72056743099262,8.51016043490908));
#13481=CARTESIAN_POINT('Ctrl Pts',(2.12679919082649,1.96615561874099,8.63717775483311));
#13482=CARTESIAN_POINT('Ctrl Pts',(-0.498478561978086,2.8531669839768,8.76419507475712));
#13483=CARTESIAN_POINT('Ctrl Pts',(-2.66747620963103,1.12854480915004,8.89121239468115));
#13484=CARTESIAN_POINT('Ctrl Pts',(-2.39481153064322,-1.62908577057971,
9.01822971460514));
#13485=CARTESIAN_POINT('Ctrl Pts',(0.0699330899254719,-2.89554003221169,
9.14524703452918));
#13486=CARTESIAN_POINT('Ctrl Pts',(2.47066477180699,-1.51157477504718,9.27226435445317));
#13487=CARTESIAN_POINT('Ctrl Pts',(2.60988458966556,1.25600364005573,9.39928167437721));
#13488=CARTESIAN_POINT('Ctrl Pts',(0.360158310663512,2.87390478382062,9.52629899430121));
#13489=CARTESIAN_POINT('Ctrl Pts',(-2.21923725483436,1.86119013589752,9.65331631422524));
#13490=CARTESIAN_POINT('Ctrl Pts',(-2.76726400083069,-0.855156514863526,
9.78033363414925));
#13491=CARTESIAN_POINT('Ctrl Pts',(-0.782288115237663,-2.78873950378391,
9.90735095407327));
#13492=CARTESIAN_POINT('Ctrl Pts',(1.91875167100355,-2.16966235627301,10.0343682739973));
#13493=CARTESIAN_POINT('Ctrl Pts',(2.86347076266717,0.435405450766662,10.1613855939213));
#13494=CARTESIAN_POINT('Ctrl Pts',(1.18712479688131,2.64192684074267,10.2884029138453));
#13495=CARTESIAN_POINT('Ctrl Pts',(-1.57585050156767,2.43017240374339,10.4154202337693));
#13496=CARTESIAN_POINT('Ctrl Pts',(-2.89637814548709,-0.00602939066377948,
10.5424375536933));
#13497=CARTESIAN_POINT('Ctrl Pts',(-1.56571910740061,-2.43671220950026,
10.6694548736174));
#13498=CARTESIAN_POINT('Ctrl Pts',(1.19811385922502,-2.63696148920304,10.7964721935414));
#13499=CARTESIAN_POINT('Ctrl Pts',(2.86525870449697,-0.423479954084387,
10.9234895134654));
#13500=CARTESIAN_POINT('Ctrl Pts',(1.9097019078235,2.17763204845591,11.0505068333894));
#13501=CARTESIAN_POINT('Ctrl Pts',(-0.793891923486379,2.78545836964585,
11.1775241533134));
#13502=CARTESIAN_POINT('Ctrl Pts',(-2.77080036056394,0.843627925750284,
11.3045414732374));
#13503=CARTESIAN_POINT('Ctrl Pts',(-2.21146917510807,-1.87041353789847,
11.4315587931615));
#13504=CARTESIAN_POINT('Ctrl Pts',(0.372120353081287,-2.87238039925594,
11.5585761130855));
#13505=CARTESIAN_POINT('Ctrl Pts',(2.61509119315851,-1.24512680746655,11.6855934330095));
#13506=CARTESIAN_POINT('Ctrl Pts',(2.46435009533307,1.52184799597032,11.8126107529335));
#13507=CARTESIAN_POINT('Ctrl Pts',(0.0578772441359576,2.89580609499639,
11.9396280728575));
#13508=CARTESIAN_POINT('Ctrl Pts',(-2.40157328163847,1.61910113585509,12.0666453927815));
#13509=CARTESIAN_POINT('Ctrl Pts',(-2.66275452753254,-1.13964075098778,
12.1936627127056));
#13510=CARTESIAN_POINT('Ctrl Pts',(-0.48659541721494,-2.85521761257394,
12.3206800326296));
#13511=CARTESIAN_POINT('Ctrl Pts',(2.13496661525059,-1.95728390045299,12.4476973525536));
#13512=CARTESIAN_POINT('Ctrl Pts',(2.80229657836465,0.732240808814111,12.5747146724776));
#13513=CARTESIAN_POINT('Ctrl Pts',(0.90455699792931,2.75151219381346,12.7017319924016));
#13514=CARTESIAN_POINT('Ctrl Pts',(-1.82116475388173,2.25219929278605,12.8287493123256));
#13515=CARTESIAN_POINT('Ctrl Pts',(-2.8798915558956,-0.308654080627915,
12.9557666322497));
#13516=CARTESIAN_POINT('Ctrl Pts',(-1.30252260138397,-2.58698233238864,
13.0827839521737));
#13517=CARTESIAN_POINT('Ctrl Pts',(1.46710454606473,-2.49732796527072,13.2098012720977));
#13518=CARTESIAN_POINT('Ctrl Pts',(2.89382415925463,-0.12175570015915,13.3368185920217));
#13519=CARTESIAN_POINT('Ctrl Pts',(1.67169487022615,2.36526509636163,13.4638359119457));
#13520=CARTESIAN_POINT('Ctrl Pts',(-1.08061278422976,2.68725114676061,13.5908532318697));
#13521=CARTESIAN_POINT('Ctrl Pts',(-2.84378639677227,0.549473970939458,
13.7178705517938));
#13522=CARTESIAN_POINT('Ctrl Pts',(-2.00391294747326,-2.09126172779881,
13.8448878717178));
#13523=CARTESIAN_POINT('Ctrl Pts',(0.670233187013017,-2.81777042894438,
13.9719051916418));
#13524=CARTESIAN_POINT('Ctrl Pts',(2.73088439438974,-0.965045667150298,
14.0989225115658));
#13525=CARTESIAN_POINT('Ctrl Pts',(2.29183287897636,1.77102929677913,14.2259398314898));
#13526=CARTESIAN_POINT('Ctrl Pts',(-0.245037533321299,2.88600057561859,
14.3529571514138));
#13527=CARTESIAN_POINT('Ctrl Pts',(-2.55761394383426,1.35928423426138,14.4799744713379));
#13528=CARTESIAN_POINT('Ctrl Pts',(-2.52908995757369,-1.41164680487256,
14.6069917912619));
#13529=CARTESIAN_POINT('Ctrl Pts',(-0.185574876810634,-2.8904333032097,
14.7340091111859));
#13530=CARTESIAN_POINT('Ctrl Pts',(2.32780533108778,-1.72347470412719,14.8610264311099));
#13531=CARTESIAN_POINT('Ctrl Pts',(2.71043942018326,1.02105869798148,14.9880437510339));
#13532=CARTESIAN_POINT('Ctrl Pts',(0.612085001486641,2.83097062262435,15.1150610709579));
#13533=CARTESIAN_POINT('Ctrl Pts',(-2.04653866476156,2.04956634653356,15.242078390882));
#13534=CARTESIAN_POINT('Ctrl Pts',(-2.83187238760927,-0.607899247822501,
15.369095710806));
#13535=CARTESIAN_POINT('Ctrl Pts',(-1.02506448320845,-2.70892700537901,
15.49611303073));
#13536=CARTESIAN_POINT('Ctrl Pts',(1.72003157611233,-2.33035063721826,15.623130350654));
#13537=CARTESIAN_POINT('Ctrl Pts',(2.89070448411775,0.181301684240713,15.750147670578));
#13538=CARTESIAN_POINT('Ctrl Pts',(1.41538407048151,2.52700032612467,15.877164990502));
#13539=CARTESIAN_POINT('Ctrl Pts',(-1.3555017731835,2.55962060823541,16.004182310426));
#13540=CARTESIAN_POINT('Ctrl Pts',(-2.88563517777252,0.249303702356721,
16.1311996303501));
#13541=CARTESIAN_POINT('Ctrl Pts',(-1.77441542743651,-2.28921222390636,
16.2582169502741));
#13542=CARTESIAN_POINT('Ctrl Pts',(0.961007487425978,-2.73230805809268,
16.3852342701981));
#13543=CARTESIAN_POINT('Ctrl Pts',(2.81677652976444,-0.67439802533461,16.5122515901221));
#13544=CARTESIAN_POINT('Ctrl Pts',(2.09422187029827,2.00081920052048,16.6392689100461));
#13545=CARTESIAN_POINT('Ctrl Pts',(-0.545269339856637,2.84459558851857,
16.7662862299701));
#13546=CARTESIAN_POINT('Ctrl Pts',(-2.68565071720656,1.08458422465704,16.8933035498942));
#13547=CARTESIAN_POINT('Ctrl Pts',(-2.36773381431579,-1.66819642121442,
17.0203208698181));
#13548=CARTESIAN_POINT('Ctrl Pts',(0.117477564550026,-2.89400099119444,
17.1473381897422));
#13549=CARTESIAN_POINT('Ctrl Pts',(2.49515638415566,-1.47079479663692,17.2743555096662));
#13550=CARTESIAN_POINT('Ctrl Pts',(2.58890505275436,1.29869678640933,17.4013728295902));
#13551=CARTESIAN_POINT('Ctrl Pts',(0.312911149053036,2.87943211901328,17.5283901495142));
#13552=CARTESIAN_POINT('Ctrl Pts',(-2.24950456469862,1.82449223857137,17.6554074694383));
#13553=CARTESIAN_POINT('Ctrl Pts',(-2.75284641327388,-0.900488389781994,
17.7824247893623));
#13554=CARTESIAN_POINT('Ctrl Pts',(-0.73638270405237,-2.80121102889081,
17.9094421092863));
#13555=CARTESIAN_POINT('Ctrl Pts',(1.95412559457642,-2.13785777726871,18.0364594292103));
#13556=CARTESIAN_POINT('Ctrl Pts',(2.85593383710927,0.482373955828185,18.1634767491343));
#13557=CARTESIAN_POINT('Ctrl Pts',(1.14357591303448,2.66106686243213,18.2904940690583));
#13558=CARTESIAN_POINT('Ctrl Pts',(-1.61554906914139,2.40396420946806,18.4175113889823));
#13559=CARTESIAN_POINT('Ctrl Pts',(-2.89588849187353,-0.0535962483896853,
18.5445287089064));
#13560=CARTESIAN_POINT('Ctrl Pts',(-1.52548943482816,-2.46209762183279,
18.6715460288304));
#13561=CARTESIAN_POINT('Ctrl Pts',(1.2412595012752,-2.61692903337118,18.7985633487544));
#13562=CARTESIAN_POINT('Ctrl Pts',(2.87182714702407,-0.376366248251089,
18.9255806686784));
#13563=CARTESIAN_POINT('Ctrl Pts',(1.87368075656313,2.20870168598933,19.0525979886024));
#13564=CARTESIAN_POINT('Ctrl Pts',(-0.839530870069032,2.77204448618851,
19.1796153085265));
#13565=CARTESIAN_POINT('Ctrl Pts',(-2.78428169840113,0.798008859070859,
19.3066326284505));
#13566=CARTESIAN_POINT('Ctrl Pts',(-2.18045282236851,-1.90648058071206,
19.4336499483745));
#13567=CARTESIAN_POINT('Ctrl Pts',(0.41924371770261,-2.86588161311206,19.5606672682985));
#13568=CARTESIAN_POINT('Ctrl Pts',(2.63518741023224,-1.2020108269732,19.6876845882225));
#13569=CARTESIAN_POINT('Ctrl Pts',(2.43902418313076,1.56211515238478,19.8147019081465));
#13570=CARTESIAN_POINT('Ctrl Pts',(0.0103111622528317,2.89636606718479,
19.9417192280705));
#13571=CARTESIAN_POINT('Ctrl Pts',(-2.42784013452314,1.57944135579879,20.0687365479946));
#13572=CARTESIAN_POINT('Ctrl Pts',(-2.64367890600989,-1.18321788235451,
20.1957538679186));
#13573=CARTESIAN_POINT('Ctrl Pts',(-0.439638105477045,-2.86282396444784,
20.3227711878426));
#13574=CARTESIAN_POINT('Ctrl Pts',(2.16682345353623,-1.92195703292896,20.4497885077666));
#13575=CARTESIAN_POINT('Ctrl Pts',(2.78989292983982,0.778164606764122,20.5768058276906));
#13576=CARTESIAN_POINT('Ctrl Pts',(0.859246486382724,2.76599678069832,20.7038231476147));
#13577=CARTESIAN_POINT('Ctrl Pts',(-1.85790735593631,2.22198626729555,20.8308404675387));
#13578=CARTESIAN_POINT('Ctrl Pts',(-2.87443407321436,-0.355909361805081,
20.9578577874627));
#13579=CARTESIAN_POINT('Ctrl Pts',(-1.25986051623017,-2.60802496054242,
21.0848751073868));
#13580=CARTESIAN_POINT('Ctrl Pts',(1.50792068648154,-2.47289666566219,21.2118924273106));
#13581=CARTESIAN_POINT('Ctrl Pts',(2.89543348443989,-0.0742135525751324,
21.3389097472348));
#13582=CARTESIAN_POINT('Ctrl Pts',(1.63262429222479,2.3924006010089,21.4659270671587));
#13583=CARTESIAN_POINT('Ctrl Pts',(-1.12460018907184,2.66914164732104,21.5929443870828));
#13584=CARTESIAN_POINT('Ctrl Pts',(-2.85242695349848,0.502695914710937,
21.7199617070067));
#13585=CARTESIAN_POINT('Ctrl Pts',(-1.96929756557384,-2.12389025520565,
21.8469790269308));
#13586=CARTESIAN_POINT('Ctrl Pts',(0.716419481622734,-2.80638305708953,
21.9739963468548));
#13587=CARTESIAN_POINT('Ctrl Pts',(2.74636517004355,-0.920065765881881,
22.1010136667789));
#13588=CARTESIAN_POINT('Ctrl Pts',(2.26243790611172,1.80842955915543,22.2280309867028));
#13589=CARTESIAN_POINT('Ctrl Pts',(-0.292401753364768,2.88158707253183,
22.3550483066269));
#13590=CARTESIAN_POINT('Ctrl Pts',(-2.57959268171739,1.3170967791333,22.4820656265509));
#13591=CARTESIAN_POINT('Ctrl Pts',(-2.50556527268738,-1.45299198800726,
22.6090829464749));
#13592=CARTESIAN_POINT('Ctrl Pts',(-0.138079606205935,-2.89309132941754,
22.7361002663989));
#13593=CARTESIAN_POINT('Ctrl Pts',(2.35579588699587,-1.68501209994816,22.8631175863229));
#13594=CARTESIAN_POINT('Ctrl Pts',(2.69330560074701,1.06543448281075,22.9901349062469));
#13595=CARTESIAN_POINT('Ctrl Pts',(0.565507564442487,2.84064208642623,23.117152226171));
#13596=CARTESIAN_POINT('Ctrl Pts',(-2.07992030745382,2.01567757201905,23.2441695460949));
#13597=CARTESIAN_POINT('Ctrl Pts',(-2.82151195628706,-0.65432225437952,
23.371186866019));
#13598=CARTESIAN_POINT('Ctrl Pts',(-0.980427340272484,-2.72540271416528,
23.498204185943));
#13599=CARTESIAN_POINT('Ctrl Pts',(1.75805271638312,-2.30177606424313,23.6252215058671));
#13600=CARTESIAN_POINT('Ctrl Pts',(2.88737248580153,0.228728994565927,23.752238825791));
#13601=CARTESIAN_POINT('Ctrl Pts',(1.37362440389478,2.54994787792699,23.8792561457151));
#13602=CARTESIAN_POINT('Ctrl Pts',(-1.39722752465262,2.53693131462652,24.0062734656391));
#13603=CARTESIAN_POINT('Ctrl Pts',(-2.88958510439483,0.202035941526333,
24.1332907855631));
#13604=CARTESIAN_POINT('Ctrl Pts',(-1.73611351559699,-2.31834451256072,
24.2603081054871));
#13605=CARTESIAN_POINT('Ctrl Pts',(1.0048596332272,-2.71558362271932,24.3873254254111));
#13606=CARTESIAN_POINT('Ctrl Pts',(2.82919456675196,-0.629161302687018,
24.5143427453351));
#13607=CARTESIAN_POINT('Ctrl Pts',(2.05758802371498,2.03726316769148,24.6413600652592));
#13608=CARTESIAN_POINT('Ctrl Pts',(0.296877711348344,2.56531103767014,24.7260382785418));
#13609=CARTESIAN_POINT('Ctrl Pts',(-0.500790878576573,2.39878276338949,
24.7683773851832));
#13610=CARTESIAN_POINT('Ctrl Pts',(-2.45061074833635,-0.00223305219117096,
23.342172503788));
#13611=CARTESIAN_POINT('Ctrl Pts',(-2.45232391003785,-0.188294688285105,
23.351843957865));
#13612=CARTESIAN_POINT('Ctrl Pts',(-2.43292514735263,-0.37400280173149,
23.361515411942));
#13613=CARTESIAN_POINT('Ctrl Pts',(-2.39106591214575,-0.55450235994407,
23.371186866019));
#13614=CARTESIAN_POINT('Ctrl Pts',(-2.20781708428219,-1.34468240764144,
23.4135259726603));
#13615=CARTESIAN_POINT('Ctrl Pts',(-1.59412221227735,-2.03504256090335,
23.4558650793016));
#13616=CARTESIAN_POINT('Ctrl Pts',(-0.830861433498997,-2.30961819588062,
23.498204185943));
#13617=CARTESIAN_POINT('Ctrl Pts',(-0.0676006547206245,-2.58419383085789,
23.5405432925843));
#13618=CARTESIAN_POINT('Ctrl Pts',(0.84522603083126,-2.44298494755051,23.5828823992257));
#13619=CARTESIAN_POINT('Ctrl Pts',(1.48985933517694,-1.95062966276197,23.625221505867));
#13620=CARTESIAN_POINT('Ctrl Pts',(2.13449263952259,-1.45827437797344,23.6675606125084));
#13621=CARTESIAN_POINT('Ctrl Pts',(2.51093256266206,-0.614772691703766,
23.7098997191497));
#13622=CARTESIAN_POINT('Ctrl Pts',(2.44686117724734,0.193847965324576,23.752238825791));
#13623=CARTESIAN_POINT('Ctrl Pts',(2.38278979183262,1.00246862235294,23.7945779324324));
#13624=CARTESIAN_POINT('Ctrl Pts',(1.87820709786369,1.77620825013998,23.8369170390737));
#13625=CARTESIAN_POINT('Ctrl Pts',(1.16410709612132,2.16090863681675,23.8792561457151));
#13626=CARTESIAN_POINT('Ctrl Pts',(0.450007094378972,2.5456090234935,23.9215952523564));
#13627=CARTESIAN_POINT('Ctrl Pts',(-0.473610215136808,2.54127016906001,
23.9639343589977));
#13628=CARTESIAN_POINT('Ctrl Pts',(-1.18414513318507,2.14995151299324,24.0062734656391));
#13629=CARTESIAN_POINT('Ctrl Pts',(-1.42595437674378,2.01677794782373,24.0206823104261));
#13630=CARTESIAN_POINT('Ctrl Pts',(-1.6430849072501,1.83878527106171,24.035091155213));
#13631=CARTESIAN_POINT('Ctrl Pts',(-1.82655445601566,1.63000783787709,24.0495));
#13632=CARTESIAN_POINT('Ctrl Pts',(-1.1628446574583,-1.62479335886121,-9.36750677027476E-17));
#13633=CARTESIAN_POINT('Ctrl Pts',(-1.20471710970498,-1.6016342897335,-9.84898357583373E-17));
#13634=CARTESIAN_POINT('Ctrl Pts',(-1.24562209910426,-1.57691188235754,
-1.47679554909033E-16));
#13635=CARTESIAN_POINT('Ctrl Pts',(-1.2854610045556,-1.55064518989967,-1.64798730217797E-16));
#13636=CARTESIAN_POINT('Ctrl Pts',(-1.34528284791422,-1.51120329399511,
-1.79293118691912E-16));
#13637=CARTESIAN_POINT('Ctrl Pts',(-1.40270227022668,-1.46828195181486,
-2.83591590275869E-17));
#13638=CARTESIAN_POINT('Ctrl Pts',(-1.45763752553965,-1.42222527204903,
7.28583859910259E-17));
#13639=CARTESIAN_POINT('Ctrl Pts',(-1.48804755094941,-1.39673008150174,
1.28888490855271E-16));
#13640=CARTESIAN_POINT('Ctrl Pts',(-1.51769605100349,-1.37027322214852,
-3.8021251132136E-16));
#13641=CARTESIAN_POINT('Ctrl Pts',(-1.54656641082207,-1.34290698199124,
-3.67761376907083E-16));
#13642=CARTESIAN_POINT('Ctrl Pts',(-1.55885125016836,-1.33126217167516,
-3.62463203038807E-16));
#13643=CARTESIAN_POINT('Ctrl Pts',(-1.57099516808733,-1.31945265506341,
-7.47886777659616E-16));
#13644=CARTESIAN_POINT('Ctrl Pts',(-1.58299675523336,-1.30748225159357,
-7.49400541621981E-16));
#13645=CARTESIAN_POINT('Ctrl Pts',(-1.59344058720201,-1.29706555579204,
-7.50717825433759E-16));
#13646=CARTESIAN_POINT('Ctrl Pts',(-1.60377038195195,-1.28653323791471,
-4.4644076430482E-16));
#13647=CARTESIAN_POINT('Ctrl Pts',(-1.61398372332283,-1.27589015849519,
-4.57966997657877E-16));
#13648=CARTESIAN_POINT('Ctrl Pts',(-1.66603051092346,-1.22165344263028,
-5.16704231377666E-16));
#13649=CARTESIAN_POINT('Ctrl Pts',(-1.71507034489567,-1.16452912219097,
-1.54529368863996E-16));
#13650=CARTESIAN_POINT('Ctrl Pts',(-1.76101022097129,-1.10489021342489,
-2.35922392732846E-16));
#13651=CARTESIAN_POINT('Ctrl Pts',(-1.79846063902999,-1.05627227500952,
-3.02274395205222E-16));
#13652=CARTESIAN_POINT('Ctrl Pts',(-1.83385070502955,-1.00598204477662,
-3.07161165321323E-16));
#13653=CARTESIAN_POINT('Ctrl Pts',(-1.86711657018502,-0.954199806015946,
-2.42861286636753E-16));
#13654=CARTESIAN_POINT('Ctrl Pts',(-1.88036622467999,-0.933575157615885,
-2.17250914783866E-16));
#13655=CARTESIAN_POINT('Ctrl Pts',(-1.89327874453011,-0.912713625458099,
-5.33570700749379E-16));
#13656=CARTESIAN_POINT('Ctrl Pts',(-1.90584944825313,-0.891625897229556,
-5.68989300120393E-16));
#13657=CARTESIAN_POINT('Ctrl Pts',(-1.91458650894537,-0.876969218856263,
-5.93606414576128E-16));
#13658=CARTESIAN_POINT('Ctrl Pts',(-1.92315966451329,-0.862200842946139,
-7.8088903438659E-16));
#13659=CARTESIAN_POINT('Ctrl Pts',(-1.93155555809178,-0.847345668566372,
-7.63278329429795E-16));
#13660=CARTESIAN_POINT('Ctrl Pts',(-1.96982617330085,-0.779632011022089,
-6.83004263702097E-16));
#13661=CARTESIAN_POINT('Ctrl Pts',(-2.00447064936929,-0.710029521402437,
-3.10624695463674E-16));
#13662=CARTESIAN_POINT('Ctrl Pts',(-2.03539350763164,-0.638916805331437,
-3.33066907387547E-16));
#13663=CARTESIAN_POINT('Ctrl Pts',(-2.06690570609391,-0.566448794677043,
-3.55936831961706E-16));
#13664=CARTESIAN_POINT('Ctrl Pts',(-2.09455376203166,-0.492411684095305,
-4.04707542421149E-16));
#13665=CARTESIAN_POINT('Ctrl Pts',(-2.1182014521557,-0.417165542608831,
-3.05311331771918E-16));
#13666=CARTESIAN_POINT('Ctrl Pts',(-2.13556664588564,-0.361910089856805,
-2.32321773599738E-16));
#13667=CARTESIAN_POINT('Ctrl Pts',(-2.1507739922553,-0.306001765547992,
-4.24436518415042E-16));
#13668=CARTESIAN_POINT('Ctrl Pts',(-2.16375453913393,-0.249573411217413,
-3.7470027081099E-16));
#13669=CARTESIAN_POINT('Ctrl Pts',(-2.17348994929291,-0.20725214546948,
-3.37398085107951E-16));
#13670=CARTESIAN_POINT('Ctrl Pts',(-2.18197253287921,-0.164638180799305,
-2.06086771920563E-16));
#13671=CARTESIAN_POINT('Ctrl Pts',(-2.18916775342387,-0.12178566500651,
-1.80411241501588E-16));
#13672=CARTESIAN_POINT('Ctrl Pts',(-2.1911236200848,-0.110137126027669,
-1.73431898250564E-16));
#13673=CARTESIAN_POINT('Ctrl Pts',(-2.1929844738391,-0.0984700252994666,
-5.62880969893907E-16));
#13674=CARTESIAN_POINT('Ctrl Pts',(-2.19474912408356,-0.086788305589102,
-5.55111512312578E-16));
#13675=CARTESIAN_POINT('Ctrl Pts',(-2.20686349029083,-0.00659301989632839,
-5.01773999869121E-16));
#13676=CARTESIAN_POINT('Ctrl Pts',(-2.21439544409116,0.0739404855027051,
-3.28643147674851E-16));
#13677=CARTESIAN_POINT('Ctrl Pts',(-2.21721959193008,0.154432844333648,
-4.16333634234434E-16));
#13678=CARTESIAN_POINT('Ctrl Pts',(-2.21852422549391,0.19161681590748,-4.56842827987537E-16));
#13679=CARTESIAN_POINT('Ctrl Pts',(-2.21882361008786,0.228792448646571,
-4.07756221638516E-16));
#13680=CARTESIAN_POINT('Ctrl Pts',(-2.21810211756152,0.26592419994786,-4.44089209850063E-16));
#13681=CARTESIAN_POINT('Ctrl Pts',(-2.21659417953099,0.343530520017813,
-5.19153256660931E-16));
#13682=CARTESIAN_POINT('Ctrl Pts',(-2.21063041400095,0.420944765509284,
-3.26957043112244E-16));
#13683=CARTESIAN_POINT('Ctrl Pts',(-2.20044401683584,0.497916376546012,
-3.33066907387547E-16));
#13684=CARTESIAN_POINT('Ctrl Pts',(-2.19004534119325,0.576492030320754,
-3.39304097611847E-16));
#13685=CARTESIAN_POINT('Ctrl Pts',(-2.17524608828998,0.654607181552501,
-1.21848361755045E-16));
#13686=CARTESIAN_POINT('Ctrl Pts',(-2.15624041704135,0.731997413041652,
-1.38777878078145E-16));
#13687=CARTESIAN_POINT('Ctrl Pts',(-2.1530491332955,0.744992175742075,-1.4162055011851E-16));
#13688=CARTESIAN_POINT('Ctrl Pts',(-2.14973861875141,0.757968425128774,
-2.74413855480096E-16));
#13689=CARTESIAN_POINT('Ctrl Pts',(-2.14631128719358,0.770918735048493,
-2.77555756156289E-16));
#13690=CARTESIAN_POINT('Ctrl Pts',(-2.1256470659196,0.848999324928004,-2.96499044746354E-16));
#13691=CARTESIAN_POINT('Ctrl Pts',(-2.100810416393,0.925878399842031,-5.72875657946036E-16));
#13692=CARTESIAN_POINT('Ctrl Pts',(-2.07208060636904,1.00128708760705,-4.71844785465692E-16));
#13693=CARTESIAN_POINT('Ctrl Pts',(-2.04275443716757,1.07826107159141,-3.68716764136624E-16));
#13694=CARTESIAN_POINT('Ctrl Pts',(-2.00937162894103,1.15370380486668,-4.21201560705881E-16));
#13695=CARTESIAN_POINT('Ctrl Pts',(-1.97217365940411,1.22733228755951,-4.71844785465692E-16));
#13696=CARTESIAN_POINT('Ctrl Pts',(-1.93463599538849,1.301633150744,-5.22950487722222E-16));
#13697=CARTESIAN_POINT('Ctrl Pts',(-1.89321286071335,1.37408738698341,-2.7977493126578E-16));
#13698=CARTESIAN_POINT('Ctrl Pts',(-1.84810028796748,1.44439403673038,-1.94289029309402E-16));
#13699=CARTESIAN_POINT('Ctrl Pts',(-1.82057954912994,1.48728431827401,-1.42138707595646E-16));
#13700=CARTESIAN_POINT('Ctrl Pts',(-1.79168476892488,1.52937510966431,-4.41214674814833E-16));
#13701=CARTESIAN_POINT('Ctrl Pts',(-1.7614518395478,1.57059399934622,-4.9960036108132E-16));
#13702=CARTESIAN_POINT('Ctrl Pts',(-1.75330578858498,1.58170014032886,-5.15331975107013E-16));
#13703=CARTESIAN_POINT('Ctrl Pts',(-1.74506709433522,1.59273671109622,-3.76832932046581E-17));
#13704=CARTESIAN_POINT('Ctrl Pts',(-1.73674048345306,1.60369766068764,-2.77555756156289E-17));
#13705=CARTESIAN_POINT('Ctrl Pts',(-1.68479340016487,1.67207954731607,3.41803043909498E-17));
#13706=CARTESIAN_POINT('Ctrl Pts',(-1.62938511172315,1.73757860209274,-5.37469459706135E-16));
#13707=CARTESIAN_POINT('Ctrl Pts',(-1.57077056839118,1.79989799981718,-4.44089209850063E-16));
#13708=CARTESIAN_POINT('Ctrl Pts',(-1.51209289484641,1.86228451803112,-3.50608385721631E-16));
#13709=CARTESIAN_POINT('Ctrl Pts',(-1.45020161829715,1.92148546079072,4.07133896698368E-17));
#13710=CARTESIAN_POINT('Ctrl Pts',(-1.38530359897227,1.97718510495395,1.94289029309402E-16));
#13711=CARTESIAN_POINT('Ctrl Pts',(-1.32180103027288,2.03168708385566,3.44562453802459E-16));
#13712=CARTESIAN_POINT('Ctrl Pts',(-1.25541907256516,2.08283749691017,-1.49241330947029E-16));
#13713=CARTESIAN_POINT('Ctrl Pts',(-1.18631234985499,2.13031087324772,-2.22044604925031E-16));
#13714=CARTESIAN_POINT('Ctrl Pts',(-1.14998501104135,2.15526620840483,-2.60315110265489E-16));
#13715=CARTESIAN_POINT('Ctrl Pts',(-1.11290413210694,2.1792049027253,-6.37841755674301E-18));
#13716=CARTESIAN_POINT('Ctrl Pts',(-1.07508846035128,2.20207516956609,0.));
#13717=CARTESIAN_POINT('Origin',(0.,0.,0.));
#13718=CARTESIAN_POINT('Origin',(-1.15470053837925,-2.,-5.));
#13719=CARTESIAN_POINT('',(-1.15470053837925,-2.,-5.));
#13720=CARTESIAN_POINT('',(1.15470053837925,-2.,-5.));
#13721=CARTESIAN_POINT('',(-0.577350269189627,-2.,-5.));
#13722=CARTESIAN_POINT('',(-1.15470053837925,-2.,-2.));
#13723=CARTESIAN_POINT('',(-1.15470053837925,-2.,-5.));
#13724=CARTESIAN_POINT('',(1.15470053837925,-2.,-2.));
#13725=CARTESIAN_POINT('',(-1.15470053837925,-2.,-2.));
#13726=CARTESIAN_POINT('',(1.15470053837925,-2.,-5.));
#13727=CARTESIAN_POINT('Origin',(-2.3094010767585,2.82820063659975E-16,
-5.));
#13728=CARTESIAN_POINT('',(-2.3094010767585,2.82820063659975E-16,-5.));
#13729=CARTESIAN_POINT('',(-2.02072594216369,-0.5,-5.));
#13730=CARTESIAN_POINT('',(-2.3094010767585,2.77555756156289E-16,-2.));
#13731=CARTESIAN_POINT('',(-2.3094010767585,2.82820063659975E-16,-5.));
#13732=CARTESIAN_POINT('',(-2.3094010767585,2.82820063659975E-16,-2.));
#13733=CARTESIAN_POINT('Origin',(-1.15470053837925,2.,-5.));
#13734=CARTESIAN_POINT('',(-1.15470053837925,2.,-5.));
#13735=CARTESIAN_POINT('',(-1.44337567297406,1.5,-5.));
#13736=CARTESIAN_POINT('',(-1.15470053837925,2.,-2.));
#13737=CARTESIAN_POINT('',(-1.15470053837925,2.,-5.));
#13738=CARTESIAN_POINT('',(-1.15470053837925,2.,-2.));
#13739=CARTESIAN_POINT('Origin',(1.15470053837925,2.,-5.));
#13740=CARTESIAN_POINT('',(1.15470053837925,2.,-5.));
#13741=CARTESIAN_POINT('',(0.577350269189626,2.,-5.));
#13742=CARTESIAN_POINT('',(1.15470053837925,2.,-2.));
#13743=CARTESIAN_POINT('',(1.15470053837925,2.,-5.));
#13744=CARTESIAN_POINT('',(1.15470053837925,2.,-2.));
#13745=CARTESIAN_POINT('Origin',(2.3094010767585,0.,-5.));
#13746=CARTESIAN_POINT('',(2.3094010767585,0.,-5.));
#13747=CARTESIAN_POINT('',(2.02072594216369,0.5,-5.));
#13748=CARTESIAN_POINT('',(2.3094010767585,0.,-2.));
#13749=CARTESIAN_POINT('',(2.3094010767585,0.,-5.));
#13750=CARTESIAN_POINT('',(2.3094010767585,0.,-2.));
#13751=CARTESIAN_POINT('Origin',(1.15470053837925,-2.,-5.));
#13752=CARTESIAN_POINT('',(1.44337567297406,-1.5,-5.));
#13753=CARTESIAN_POINT('',(1.15470053837925,-2.,-2.));
#13754=CARTESIAN_POINT('Origin',(0.,0.,-2.));
#13755=CARTESIAN_POINT('Origin',(0.,0.,0.));
#13756=CARTESIAN_POINT('',(-4.,-4.89858719658941E-16,0.));
#13757=CARTESIAN_POINT('Origin',(0.,0.,0.));
#13758=CARTESIAN_POINT('Origin',(0.,0.,-5.));
#13759=CARTESIAN_POINT('',(-4.,-4.89858719658941E-16,-5.));
#13760=CARTESIAN_POINT('',(-4.,-4.89858719658941E-16,-5.));
#13761=CARTESIAN_POINT('Origin',(0.,0.,-5.));
#13762=CARTESIAN_POINT('Origin',(0.,0.,-5.));
#13763=CARTESIAN_POINT('Origin',(0.,0.,25.));
#13790=UNCERTAINTY_MEASURE_WITH_UNIT(LENGTH_MEASURE(0.01),#13802,
'DISTANCE_ACCURACY_VALUE',
'Maximum model space distance between geometric entities at asserted c
onnectivities');
#13792=UNCERTAINTY_MEASURE_WITH_UNIT(LENGTH_MEASURE(0.01),#13802,
'DISTANCE_ACCURACY_VALUE',
'Maximum model space distance between geometric entities at asserted c
onnectivities');
#13799=(
GEOMETRIC_REPRESENTATION_CONTEXT(3)
GLOBAL_UNCERTAINTY_ASSIGNED_CONTEXT((#13790))
GLOBAL_UNIT_ASSIGNED_CONTEXT((#13802,#13804,#13805))
REPRESENTATION_CONTEXT('','3D')
);
#13801=(
GEOMETRIC_REPRESENTATION_CONTEXT(3)
GLOBAL_UNCERTAINTY_ASSIGNED_CONTEXT((#13792))
GLOBAL_UNIT_ASSIGNED_CONTEXT((#13802,#13804,#13805))
REPRESENTATION_CONTEXT('','3D')
);
#13802=(
LENGTH_UNIT()
NAMED_UNIT(*)
SI_UNIT(.MILLI.,.METRE.)
);
#13804=(
NAMED_UNIT(*)
PLANE_ANGLE_UNIT()
SI_UNIT($,.RADIAN.)
);
#13805=(
NAMED_UNIT(*)
SI_UNIT($,.STERADIAN.)
SOLID_ANGLE_UNIT()
);
#13812=SHAPE_DEFINITION_REPRESENTATION(#13820,#13839);
#13820=PRODUCT_DEFINITION_SHAPE('',$,#13848);
#13839=SHAPE_REPRESENTATION('',(#3941),#13799);
#13841=PRODUCT_DEFINITION_CONTEXT('part definition',#13867,'design');
#13848=PRODUCT_DEFINITION('Socket head cap screw M5x25',
'Socket head cap screw M5x25',#13856,#13841);
#13856=PRODUCT_DEFINITION_FORMATION('',$,#13875);
#13867=APPLICATION_CONTEXT(
'Core Data for Automotive Mechanical Design Process');
#13868=PRODUCT_CONTEXT('part definition',#13867,'mechanical');
#13875=PRODUCT('Socket head cap screw M5x25',
'Socket head cap screw M5x25',$,(#13868));
#13882=PRESENTATION_STYLE_ASSIGNMENT((#13889));
#13889=SURFACE_STYLE_USAGE(.BOTH.,#13896);
#13896=SURFACE_SIDE_STYLE('',(#13903));
#13903=SURFACE_STYLE_FILL_AREA(#13910);
#13910=FILL_AREA_STYLE('Dark gray',(#13917));
#13917=FILL_AREA_STYLE_COLOUR('Dark gray',#13924);
#13924=COLOUR_RGB('Dark gray',0.250980392156863,0.282352941176471,0.32156862745098);
ENDSEC;
END-ISO-10303-21;
